ISO-10303-21;
HEADER;
/* Generated by software containing ST-Developer
 * from STEP Tools, Inc. (www.steptools.com) 
 */

FILE_DESCRIPTION(
/* description */ (''),
/* implementation_level */ '2;1');

FILE_NAME(
/* name */ '02_Wheel_Stud_1-2-20_UNF_Knurled.step',
/* time_stamp */ '2026-10-25T01:26:34-07:00',
/* author */ (''),
/* organization */ (''),
/* preprocessor_version */ 'ST-DEVELOPER v20.2',
/* originating_system */ 'Autodesk Translation Framework v15.15.0.0',
/* authorisation */ '');

FILE_SCHEMA (('AUTOMOTIVE_DESIGN { 1 0 10303 214 3 1 1 }'));
ENDSEC;

DATA;
#10=MECHANICAL_DESIGN_GEOMETRIC_PRESENTATION_REPRESENTATION('',(#332),#71628);
#267=(
BOUNDED_CURVE()
B_SPLINE_CURVE(2,(#66650,#66651,#66652),.UNSPECIFIED.,.F.,.F.)
B_SPLINE_CURVE_WITH_KNOTS((3,3),(0.0318913416068047,0.0878632526191407),
 .UNSPECIFIED.)
CURVE()
GEOMETRIC_REPRESENTATION_ITEM()
RATIONAL_B_SPLINE_CURVE((1.,1.,1.))
REPRESENTATION_ITEM('')
);
#268=(
BOUNDED_CURVE()
B_SPLINE_CURVE(2,(#66656,#66657,#66658),.UNSPECIFIED.,.F.,.F.)
B_SPLINE_CURVE_WITH_KNOTS((3,3),(0.,0.0559719110123359),.UNSPECIFIED.)
CURVE()
GEOMETRIC_REPRESENTATION_ITEM()
RATIONAL_B_SPLINE_CURVE((1.,1.,1.))
REPRESENTATION_ITEM('')
);
#269=(
BOUNDED_CURVE()
B_SPLINE_CURVE(2,(#66674,#66675,#66676),.UNSPECIFIED.,.F.,.F.)
B_SPLINE_CURVE_WITH_KNOTS((3,3),(0.149824701143017,0.201007744174973),
 .UNSPECIFIED.)
CURVE()
GEOMETRIC_REPRESENTATION_ITEM()
RATIONAL_B_SPLINE_CURVE((1.0015789381359,1.00105916711486,1.))
REPRESENTATION_ITEM('')
);
#270=(
BOUNDED_CURVE()
B_SPLINE_CURVE(2,(#66679,#66680,#66681),.UNSPECIFIED.,.F.,.F.)
B_SPLINE_CURVE_WITH_KNOTS((3,3),(0.,0.0619069470426676),.UNSPECIFIED.)
CURVE()
GEOMETRIC_REPRESENTATION_ITEM()
RATIONAL_B_SPLINE_CURVE((1.,1.00126373727763,1.00175959622219))
REPRESENTATION_ITEM('')
);
#271=(
BOUNDED_CURVE()
B_SPLINE_CURVE(2,(#66690,#66691,#66692),.UNSPECIFIED.,.F.,.F.)
B_SPLINE_CURVE_WITH_KNOTS((3,3),(0.,0.0544904914367116),.UNSPECIFIED.)
CURVE()
GEOMETRIC_REPRESENTATION_ITEM()
RATIONAL_B_SPLINE_CURVE((1.,1.00018612804858,1.00011392668297))
REPRESENTATION_ITEM('')
);
#272=(
BOUNDED_CURVE()
B_SPLINE_CURVE(2,(#66696,#66697,#66698),.UNSPECIFIED.,.F.,.F.)
B_SPLINE_CURVE_WITH_KNOTS((3,3),(0.024031026287471,0.0785215177241609),
 .UNSPECIFIED.)
CURVE()
GEOMETRIC_REPRESENTATION_ITEM()
RATIONAL_B_SPLINE_CURVE((1.00011392668297,1.00018612804858,1.))
REPRESENTATION_ITEM('')
);
#273=(
BOUNDED_CURVE()
B_SPLINE_CURVE(2,(#66699,#66700,#66701),.UNSPECIFIED.,.F.,.F.)
B_SPLINE_CURVE_WITH_KNOTS((3,3),(0.,0.051183043031955),.UNSPECIFIED.)
CURVE()
GEOMETRIC_REPRESENTATION_ITEM()
RATIONAL_B_SPLINE_CURVE((1.,1.00105916711486,1.0015789381359))
REPRESENTATION_ITEM('')
);
#274=(
BOUNDED_CURVE()
B_SPLINE_CURVE(2,(#66711,#66712,#66713),.UNSPECIFIED.,.F.,.F.)
B_SPLINE_CURVE_WITH_KNOTS((3,3),(0.141860012781432,0.2037669598241),
 .UNSPECIFIED.)
CURVE()
GEOMETRIC_REPRESENTATION_ITEM()
RATIONAL_B_SPLINE_CURVE((1.00175959622219,1.00126373727763,1.))
REPRESENTATION_ITEM('')
);
#287=B_SPLINE_SURFACE_WITH_KNOTS('',3,3,((#66937,#66938,#66939,#66940,#66941,
#66942,#66943,#66944,#66945,#66946,#66947,#66948,#66949,#66950,#66951,#66952,
#66953,#66954,#66955,#66956,#66957,#66958,#66959,#66960,#66961,#66962,#66963,
#66964,#66965,#66966,#66967,#66968,#66969,#66970,#66971,#66972,#66973,#66974,
#66975,#66976,#66977,#66978,#66979,#66980,#66981,#66982,#66983,#66984,#66985,
#66986,#66987,#66988,#66989,#66990,#66991,#66992,#66993,#66994,#66995,#66996,
#66997,#66998,#66999,#67000,#67001,#67002,#67003,#67004,#67005,#67006,#67007,
#67008,#67009,#67010,#67011,#67012,#67013,#67014,#67015,#67016,#67017,#67018,
#67019,#67020,#67021,#67022,#67023,#67024,#67025,#67026,#67027,#67028,#67029,
#67030,#67031,#67032,#67033,#67034,#67035,#67036,#67037,#67038,#67039,#67040,
#67041,#67042,#67043,#67044,#67045,#67046,#67047,#67048,#67049,#67050,#67051,
#67052,#67053,#67054,#67055,#67056,#67057,#67058,#67059,#67060,#67061,#67062,
#67063,#67064,#67065,#67066,#67067,#67068,#67069,#67070,#67071,#67072,#67073,
#67074,#67075,#67076,#67077,#67078,#67079,#67080,#67081,#67082,#67083,#67084,
#67085,#67086,#67087,#67088,#67089,#67090,#67091,#67092,#67093,#67094,#67095,
#67096,#67097,#67098,#67099,#67100,#67101,#67102,#67103,#67104,#67105,#67106,
#67107,#67108,#67109,#67110,#67111,#67112,#67113,#67114,#67115,#67116,#67117,
#67118,#67119,#67120,#67121,#67122,#67123,#67124,#67125,#67126,#67127,#67128,
#67129,#67130,#67131,#67132,#67133,#67134,#67135,#67136,#67137,#67138,#67139,
#67140,#67141,#67142,#67143,#67144,#67145,#67146,#67147,#67148,#67149,#67150,
#67151,#67152,#67153,#67154,#67155,#67156,#67157,#67158,#67159,#67160,#67161,
#67162,#67163,#67164,#67165,#67166,#67167,#67168,#67169,#67170,#67171,#67172,
#67173,#67174,#67175,#67176,#67177,#67178,#67179,#67180,#67181,#67182,#67183,
#67184,#67185,#67186,#67187,#67188,#67189,#67190,#67191,#67192,#67193,#67194,
#67195,#67196,#67197,#67198,#67199,#67200,#67201,#67202,#67203,#67204,#67205,
#67206,#67207,#67208,#67209,#67210,#67211,#67212,#67213,#67214,#67215,#67216,
#67217,#67218,#67219,#67220,#67221,#67222,#67223,#67224,#67225,#67226,#67227,
#67228,#67229,#67230,#67231,#67232,#67233,#67234,#67235,#67236,#67237,#67238,
#67239,#67240,#67241,#67242,#67243,#67244,#67245,#67246,#67247,#67248,#67249,
#67250,#67251,#67252,#67253,#67254,#67255,#67256,#67257,#67258,#67259,#67260,
#67261,#67262,#67263,#67264,#67265,#67266,#67267,#67268,#67269,#67270,#67271,
#67272,#67273,#67274,#67275,#67276,#67277,#67278,#67279,#67280,#67281,#67282,
#67283,#67284,#67285,#67286,#67287,#67288,#67289,#67290,#67291,#67292,#67293,
#67294,#67295,#67296,#67297,#67298,#67299,#67300,#67301,#67302,#67303,#67304,
#67305),(#67306,#67307,#67308,#67309,#67310,#67311,#67312,#67313,#67314,
#67315,#67316,#67317,#67318,#67319,#67320,#67321,#67322,#67323,#67324,#67325,
#67326,#67327,#67328,#67329,#67330,#67331,#67332,#67333,#67334,#67335,#67336,
#67337,#67338,#67339,#67340,#67341,#67342,#67343,#67344,#67345,#67346,#67347,
#67348,#67349,#67350,#67351,#67352,#67353,#67354,#67355,#67356,#67357,#67358,
#67359,#67360,#67361,#67362,#67363,#67364,#67365,#67366,#67367,#67368,#67369,
#67370,#67371,#67372,#67373,#67374,#67375,#67376,#67377,#67378,#67379,#67380,
#67381,#67382,#67383,#67384,#67385,#67386,#67387,#67388,#67389,#67390,#67391,
#67392,#67393,#67394,#67395,#67396,#67397,#67398,#67399,#67400,#67401,#67402,
#67403,#67404,#67405,#67406,#67407,#67408,#67409,#67410,#67411,#67412,#67413,
#67414,#67415,#67416,#67417,#67418,#67419,#67420,#67421,#67422,#67423,#67424,
#67425,#67426,#67427,#67428,#67429,#67430,#67431,#67432,#67433,#67434,#67435,
#67436,#67437,#67438,#67439,#67440,#67441,#67442,#67443,#67444,#67445,#67446,
#67447,#67448,#67449,#67450,#67451,#67452,#67453,#67454,#67455,#67456,#67457,
#67458,#67459,#67460,#67461,#67462,#67463,#67464,#67465,#67466,#67467,#67468,
#67469,#67470,#67471,#67472,#67473,#67474,#67475,#67476,#67477,#67478,#67479,
#67480,#67481,#67482,#67483,#67484,#67485,#67486,#67487,#67488,#67489,#67490,
#67491,#67492,#67493,#67494,#67495,#67496,#67497,#67498,#67499,#67500,#67501,
#67502,#67503,#67504,#67505,#67506,#67507,#67508,#67509,#67510,#67511,#67512,
#67513,#67514,#67515,#67516,#67517,#67518,#67519,#67520,#67521,#67522,#67523,
#67524,#67525,#67526,#67527,#67528,#67529,#67530,#67531,#67532,#67533,#67534,
#67535,#67536,#67537,#67538,#67539,#67540,#67541,#67542,#67543,#67544,#67545,
#67546,#67547,#67548,#67549,#67550,#67551,#67552,#67553,#67554,#67555,#67556,
#67557,#67558,#67559,#67560,#67561,#67562,#67563,#67564,#67565,#67566,#67567,
#67568,#67569,#67570,#67571,#67572,#67573,#67574,#67575,#67576,#67577,#67578,
#67579,#67580,#67581,#67582,#67583,#67584,#67585,#67586,#67587,#67588,#67589,
#67590,#67591,#67592,#67593,#67594,#67595,#67596,#67597,#67598,#67599,#67600,
#67601,#67602,#67603,#67604,#67605,#67606,#67607,#67608,#67609,#67610,#67611,
#67612,#67613,#67614,#67615,#67616,#67617,#67618,#67619,#67620,#67621,#67622,
#67623,#67624,#67625,#67626,#67627,#67628,#67629,#67630,#67631,#67632,#67633,
#67634,#67635,#67636,#67637,#67638,#67639,#67640,#67641,#67642,#67643,#67644,
#67645,#67646,#67647,#67648,#67649,#67650,#67651,#67652,#67653,#67654,#67655,
#67656,#67657,#67658,#67659,#67660,#67661,#67662,#67663,#67664,#67665,#67666,
#67667,#67668,#67669,#67670,#67671,#67672,#67673,#67674),(#67675,#67676,
#67677,#67678,#67679,#67680,#67681,#67682,#67683,#67684,#67685,#67686,#67687,
#67688,#67689,#67690,#67691,#67692,#67693,#67694,#67695,#67696,#67697,#67698,
#67699,#67700,#67701,#67702,#67703,#67704,#67705,#67706,#67707,#67708,#67709,
#67710,#67711,#67712,#67713,#67714,#67715,#67716,#67717,#67718,#67719,#67720,
#67721,#67722,#67723,#67724,#67725,#67726,#67727,#67728,#67729,#67730,#67731,
#67732,#67733,#67734,#67735,#67736,#67737,#67738,#67739,#67740,#67741,#67742,
#67743,#67744,#67745,#67746,#67747,#67748,#67749,#67750,#67751,#67752,#67753,
#67754,#67755,#67756,#67757,#67758,#67759,#67760,#67761,#67762,#67763,#67764,
#67765,#67766,#67767,#67768,#67769,#67770,#67771,#67772,#67773,#67774,#67775,
#67776,#67777,#67778,#67779,#67780,#67781,#67782,#67783,#67784,#67785,#67786,
#67787,#67788,#67789,#67790,#67791,#67792,#67793,#67794,#67795,#67796,#67797,
#67798,#67799,#67800,#67801,#67802,#67803,#67804,#67805,#67806,#67807,#67808,
#67809,#67810,#67811,#67812,#67813,#67814,#67815,#67816,#67817,#67818,#67819,
#67820,#67821,#67822,#67823,#67824,#67825,#67826,#67827,#67828,#67829,#67830,
#67831,#67832,#67833,#67834,#67835,#67836,#67837,#67838,#67839,#67840,#67841,
#67842,#67843,#67844,#67845,#67846,#67847,#67848,#67849,#67850,#67851,#67852,
#67853,#67854,#67855,#67856,#67857,#67858,#67859,#67860,#67861,#67862,#67863,
#67864,#67865,#67866,#67867,#67868,#67869,#67870,#67871,#67872,#67873,#67874,
#67875,#67876,#67877,#67878,#67879,#67880,#67881,#67882,#67883,#67884,#67885,
#67886,#67887,#67888,#67889,#67890,#67891,#67892,#67893,#67894,#67895,#67896,
#67897,#67898,#67899,#67900,#67901,#67902,#67903,#67904,#67905,#67906,#67907,
#67908,#67909,#67910,#67911,#67912,#67913,#67914,#67915,#67916,#67917,#67918,
#67919,#67920,#67921,#67922,#67923,#67924,#67925,#67926,#67927,#67928,#67929,
#67930,#67931,#67932,#67933,#67934,#67935,#67936,#67937,#67938,#67939,#67940,
#67941,#67942,#67943,#67944,#67945,#67946,#67947,#67948,#67949,#67950,#67951,
#67952,#67953,#67954,#67955,#67956,#67957,#67958,#67959,#67960,#67961,#67962,
#67963,#67964,#67965,#67966,#67967,#67968,#67969,#67970,#67971,#67972,#67973,
#67974,#67975,#67976,#67977,#67978,#67979,#67980,#67981,#67982,#67983,#67984,
#67985,#67986,#67987,#67988,#67989,#67990,#67991,#67992,#67993,#67994,#67995,
#67996,#67997,#67998,#67999,#68000,#68001,#68002,#68003,#68004,#68005,#68006,
#68007,#68008,#68009,#68010,#68011,#68012,#68013,#68014,#68015,#68016,#68017,
#68018,#68019,#68020,#68021,#68022,#68023,#68024,#68025,#68026,#68027,#68028,
#68029,#68030,#68031,#68032,#68033,#68034,#68035,#68036,#68037,#68038,#68039,
#68040,#68041,#68042,#68043),(#68044,#68045,#68046,#68047,#68048,#68049,
#68050,#68051,#68052,#68053,#68054,#68055,#68056,#68057,#68058,#68059,#68060,
#68061,#68062,#68063,#68064,#68065,#68066,#68067,#68068,#68069,#68070,#68071,
#68072,#68073,#68074,#68075,#68076,#68077,#68078,#68079,#68080,#68081,#68082,
#68083,#68084,#68085,#68086,#68087,#68088,#68089,#68090,#68091,#68092,#68093,
#68094,#68095,#68096,#68097,#68098,#68099,#68100,#68101,#68102,#68103,#68104,
#68105,#68106,#68107,#68108,#68109,#68110,#68111,#68112,#68113,#68114,#68115,
#68116,#68117,#68118,#68119,#68120,#68121,#68122,#68123,#68124,#68125,#68126,
#68127,#68128,#68129,#68130,#68131,#68132,#68133,#68134,#68135,#68136,#68137,
#68138,#68139,#68140,#68141,#68142,#68143,#68144,#68145,#68146,#68147,#68148,
#68149,#68150,#68151,#68152,#68153,#68154,#68155,#68156,#68157,#68158,#68159,
#68160,#68161,#68162,#68163,#68164,#68165,#68166,#68167,#68168,#68169,#68170,
#68171,#68172,#68173,#68174,#68175,#68176,#68177,#68178,#68179,#68180,#68181,
#68182,#68183,#68184,#68185,#68186,#68187,#68188,#68189,#68190,#68191,#68192,
#68193,#68194,#68195,#68196,#68197,#68198,#68199,#68200,#68201,#68202,#68203,
#68204,#68205,#68206,#68207,#68208,#68209,#68210,#68211,#68212,#68213,#68214,
#68215,#68216,#68217,#68218,#68219,#68220,#68221,#68222,#68223,#68224,#68225,
#68226,#68227,#68228,#68229,#68230,#68231,#68232,#68233,#68234,#68235,#68236,
#68237,#68238,#68239,#68240,#68241,#68242,#68243,#68244,#68245,#68246,#68247,
#68248,#68249,#68250,#68251,#68252,#68253,#68254,#68255,#68256,#68257,#68258,
#68259,#68260,#68261,#68262,#68263,#68264,#68265,#68266,#68267,#68268,#68269,
#68270,#68271,#68272,#68273,#68274,#68275,#68276,#68277,#68278,#68279,#68280,
#68281,#68282,#68283,#68284,#68285,#68286,#68287,#68288,#68289,#68290,#68291,
#68292,#68293,#68294,#68295,#68296,#68297,#68298,#68299,#68300,#68301,#68302,
#68303,#68304,#68305,#68306,#68307,#68308,#68309,#68310,#68311,#68312,#68313,
#68314,#68315,#68316,#68317,#68318,#68319,#68320,#68321,#68322,#68323,#68324,
#68325,#68326,#68327,#68328,#68329,#68330,#68331,#68332,#68333,#68334,#68335,
#68336,#68337,#68338,#68339,#68340,#68341,#68342,#68343,#68344,#68345,#68346,
#68347,#68348,#68349,#68350,#68351,#68352,#68353,#68354,#68355,#68356,#68357,
#68358,#68359,#68360,#68361,#68362,#68363,#68364,#68365,#68366,#68367,#68368,
#68369,#68370,#68371,#68372,#68373,#68374,#68375,#68376,#68377,#68378,#68379,
#68380,#68381,#68382,#68383,#68384,#68385,#68386,#68387,#68388,#68389,#68390,
#68391,#68392,#68393,#68394,#68395,#68396,#68397,#68398,#68399,#68400,#68401,
#68402,#68403,#68404,#68405,#68406,#68407,#68408,#68409,#68410,#68411,#68412)),
 .UNSPECIFIED.,.F.,.F.,.F.,(4,4),(4,1,1,1,1,1,1,1,1,1,1,1,1,1,1,1,1,1,1,
1,1,1,1,1,1,1,1,1,1,1,1,1,1,1,1,1,1,1,1,1,1,1,1,1,1,1,1,1,1,1,1,1,1,1,1,
1,1,1,1,1,1,1,1,1,1,1,1,1,1,1,1,1,1,1,1,1,1,1,1,1,1,1,1,1,1,1,1,1,1,1,1,
1,1,1,1,1,1,1,1,1,1,1,1,1,1,1,1,1,1,1,1,1,1,1,1,1,1,1,1,1,1,1,1,1,1,1,1,
1,1,1,1,1,1,1,1,1,1,1,1,1,1,1,1,1,1,1,1,1,1,1,1,1,1,1,1,1,1,1,1,1,1,1,1,
1,1,1,1,1,1,1,1,1,1,1,1,1,1,1,1,1,1,1,1,1,1,1,1,1,1,1,1,1,1,1,1,1,1,1,1,
1,1,1,1,1,1,1,1,1,1,1,1,1,1,1,1,1,1,1,1,1,1,1,1,1,1,1,1,1,1,1,1,1,1,1,1,
1,1,1,1,1,1,1,1,1,1,1,1,1,1,1,1,1,1,1,1,1,1,1,1,1,1,1,1,1,1,1,1,1,1,1,1,
1,1,1,1,1,1,1,1,1,1,1,1,1,1,1,1,1,1,1,1,1,1,1,1,1,1,1,1,1,1,1,1,1,1,1,1,
1,1,1,1,1,1,1,1,1,1,1,1,1,1,1,1,1,1,1,1,1,1,1,1,1,1,1,1,1,1,1,1,1,1,1,1,
1,1,1,1,1,1,1,1,1,1,1,1,1,1,1,1,1,1,1,1,1,1,1,4),(0.,0.0813890674476615),
(8.31473274985811,8.81229131725278,9.30984988464746,9.80740845204213,10.3049670194368,
10.8025255868315,11.3000841542261,11.7976427216208,12.2952012890155,12.7927598564102,
13.2903184238048,13.7878769911995,14.2854355585942,14.7829941259888,15.2805526933835,
15.7781112607782,16.2756698281729,16.7732283955675,17.2707869629622,17.7683455303569,
18.2659040977515,18.7634626651462,19.2610212325409,19.7585797999356,20.2561383673302,
20.7536969347249,21.2512555021196,21.7488140695142,22.2463726369089,22.7439312043036,
23.2414897716983,23.7390483390929,24.2366069064876,24.7341654738823,25.231724041277,
25.7292826086716,26.2268411760663,26.724399743461,27.2219583108556,27.7195168782503,
28.217075445645,28.7146340130397,29.2121925804343,29.709751147829,30.2073097152237,
30.7048682826183,31.202426850013,31.6999854174077,32.1975439848024,32.695102552197,
33.1926611195917,33.6902196869864,34.187778254381,34.6853368217757,35.1828953891704,
35.6804539565651,36.1780125239597,36.6755710913544,37.1731296587491,37.6706882261438,
38.1682467935384,38.6658053609331,39.1633639283278,39.6609224957224,40.1584810631171,
40.6560396305118,41.1535981979065,41.6511567653011,42.1487153326958,42.6462739000905,
43.1438324674851,43.6413910348798,44.1389496022745,44.6365081696692,45.1340667370638,
45.6316253044585,46.1291838718532,46.6267424392478,47.1243010066425,47.6218595740372,
48.1194181414319,48.6169767088265,49.1145352762212,49.6120938436159,50.1096524110105,
50.6072109784052,51.1047695457999,51.6023281131946,52.0998866805892,52.5974452479839,
53.0950038153786,53.5925623827733,54.0901209501679,54.5876795175626,55.0852380849573,
55.5827966523519,56.0803552197466,56.5779137871413,57.075472354536,57.5730309219306,
58.0705894893253,58.56814805672,59.0657066241146,59.5632651915093,60.060823758904,
60.5583823262987,61.0559408936933,61.553499461088,62.0510580284827,62.5486165958773,
63.046175163272,63.5437337306667,64.0412922980614,64.538850865456,65.0364094328507,
65.5339680002454,66.03152656764,66.5290851350347,67.0266437024294,67.5242022698241,
68.0217608372187,68.5193194046134,69.0168779720081,69.5144365394028,70.0119951067974,
70.5095536741921,71.0071122415868,71.5046708089814,72.0022293763761,72.4997879437708,
72.9973465111654,73.4949050785601,73.9924636459548,74.4900222133495,74.9875807807441,
75.4851393481388,75.9826979155335,76.4802564829282,76.9778150503228,77.4753736177175,
77.9729321851122,78.4704907525068,78.9680493199015,79.4656078872962,79.9631664546908,
80.4607250220855,80.9582835894802,81.4558421568749,81.9534007242695,82.4509592916642,
82.9485178590589,83.4460764264536,83.9436349938482,84.4411935612429,84.9387521286376,
85.4363106960323,85.9338692634269,86.4314278308216,86.9289863982163,87.4265449656109,
87.9241035330056,88.4216621004003,88.9192206677949,89.4167792351896,89.9143378025843,
90.411896369979,90.9094549373736,91.4070135047683,91.904572072163,92.4021306395577,
92.8996892069523,93.397247774347,93.8948063417417,94.3923649091363,94.889923476531,
95.3874820439257,95.8850406113204,96.382599178715,96.8801577461097,97.3777163135044,
97.875274880899,98.3728334482937,98.8703920156884,99.3679505830831,99.8655091504777,
100.363067717872,100.860626285267,101.358184852662,101.855743420056,102.353301987451,
102.850860554846,103.34841912224,103.845977689635,104.34353625703,104.841094824424,
105.338653391819,105.836211959214,106.333770526608,106.831329094003,107.328887661398,
107.826446228792,108.324004796187,108.821563363582,109.319121930977,109.816680498371,
110.314239065766,110.811797633161,111.309356200555,111.80691476795,112.304473335345,
112.802031902739,113.299590470134,113.797149037529,114.294707604923,114.792266172318,
115.289824739713,115.787383307107,116.284941874502,116.782500441897,117.280059009291,
117.777617576686,118.275176144081,118.772734711475,119.27029327887,119.767851846265,
120.265410413659,120.762968981054,121.260527548449,121.758086115843,122.255644683238,
122.753203250633,123.250761818027,123.748320385422,124.245878952817,124.743437520211,
125.240996087606,125.738554655001,126.236113222395,126.73367178979,127.231230357185,
127.728788924579,128.226347491974,128.723906059369,129.221464626763,129.719023194158,
130.216581761553,130.714140328947,131.211698896342,131.709257463737,132.206816031131,
132.704374598526,133.201933165921,133.699491733315,134.19705030071,134.694608868105,
135.192167435499,135.689726002894,136.187284570289,136.684843137683,137.182401705078,
137.679960272473,138.177518839867,138.675077407262,139.172635974657,139.670194542051,
140.167753109446,140.665311676841,141.162870244235,141.66042881163,142.157987379025,
142.65554594642,143.153104513814,143.650663081209,144.148221648604,144.645780215998,
145.143338783393,145.640897350788,146.138455918182,146.636014485577,147.133573052972,
147.631131620366,148.128690187761,148.626248755156,149.12380732255,149.621365889945,
150.11892445734,150.616483024734,151.114041592129,151.611600159524,152.109158726918,
152.606717294313,153.104275861708,153.601834429102,154.099392996497,154.596951563892,
155.094510131286,155.592068698681,156.089627266076,156.58718583347,157.084744400865,
157.58230296826,158.079861535654,158.577420103049,159.074978670444,159.572537237838,
160.070095805233,160.567654372628,161.065212940022,161.562771507417,162.060330074812,
162.557888642206,163.055447209601,163.553005776996,164.05056434439,164.548122911785,
165.04568147918,165.543240046574,166.040798613969,166.538357181364,167.035915748758,
167.533474316153,168.031032883548,168.528591450942,169.026150018337,169.523708585732,
170.021267153126,170.518825720521,171.016384287916,171.51394285531,172.011501422705,
172.5090599901,173.006618557495,173.504177124889,174.001735692284,174.499294259679,
174.996852827073,175.494411394468,175.991969961863,176.489528529257,176.987087096652,
177.484645664047,177.982204231441,178.479762798836,178.977321366231,179.474879933625,
179.97243850102,180.469997068415,180.967555635809,181.465114203204,181.962672770599,
182.460231337993,182.957789905388,183.455348472783,183.952907040177,184.450465607572,
184.948024174967,185.445582742361,185.943141309756,186.440699877151,186.938258444545,
187.43581701194,187.933375579335,188.430934146729,188.928492714124,189.426051281519,
189.923609848913,190.421168416308),.UNSPECIFIED.);
#288=B_SPLINE_SURFACE_WITH_KNOTS('',3,3,((#68690,#68691,#68692,#68693,#68694,
#68695,#68696,#68697,#68698,#68699,#68700,#68701,#68702,#68703,#68704,#68705,
#68706,#68707,#68708,#68709,#68710,#68711,#68712,#68713,#68714,#68715,#68716,
#68717,#68718,#68719,#68720,#68721,#68722,#68723,#68724,#68725,#68726,#68727,
#68728,#68729,#68730,#68731,#68732,#68733,#68734,#68735,#68736,#68737,#68738,
#68739,#68740,#68741,#68742,#68743,#68744,#68745,#68746,#68747,#68748,#68749,
#68750,#68751,#68752,#68753,#68754,#68755,#68756,#68757,#68758,#68759,#68760,
#68761,#68762,#68763,#68764,#68765,#68766,#68767,#68768,#68769,#68770,#68771,
#68772,#68773,#68774,#68775,#68776,#68777,#68778,#68779,#68780,#68781,#68782,
#68783,#68784,#68785,#68786,#68787,#68788,#68789,#68790,#68791,#68792,#68793,
#68794,#68795,#68796,#68797,#68798,#68799,#68800,#68801,#68802,#68803,#68804,
#68805,#68806,#68807,#68808,#68809,#68810,#68811,#68812,#68813,#68814,#68815,
#68816,#68817,#68818,#68819,#68820,#68821,#68822,#68823,#68824,#68825,#68826,
#68827,#68828,#68829,#68830,#68831,#68832,#68833,#68834,#68835,#68836,#68837,
#68838,#68839,#68840,#68841,#68842,#68843,#68844,#68845,#68846,#68847,#68848,
#68849,#68850,#68851,#68852,#68853,#68854,#68855,#68856,#68857,#68858,#68859,
#68860,#68861,#68862,#68863,#68864,#68865,#68866,#68867,#68868,#68869,#68870,
#68871,#68872,#68873,#68874,#68875,#68876,#68877,#68878,#68879,#68880,#68881,
#68882,#68883,#68884,#68885,#68886,#68887,#68888,#68889,#68890,#68891,#68892,
#68893,#68894,#68895,#68896,#68897,#68898,#68899,#68900,#68901,#68902,#68903,
#68904,#68905,#68906,#68907,#68908,#68909,#68910,#68911,#68912,#68913,#68914,
#68915,#68916,#68917,#68918,#68919,#68920,#68921,#68922,#68923,#68924,#68925,
#68926,#68927,#68928,#68929,#68930,#68931,#68932,#68933,#68934,#68935,#68936,
#68937,#68938,#68939,#68940,#68941,#68942,#68943,#68944,#68945,#68946,#68947,
#68948,#68949,#68950,#68951,#68952,#68953,#68954,#68955,#68956,#68957,#68958,
#68959,#68960,#68961,#68962,#68963,#68964,#68965,#68966,#68967,#68968,#68969,
#68970,#68971,#68972,#68973,#68974,#68975,#68976,#68977,#68978,#68979,#68980,
#68981,#68982,#68983,#68984,#68985,#68986,#68987,#68988,#68989,#68990,#68991,
#68992,#68993,#68994,#68995,#68996,#68997,#68998,#68999,#69000,#69001,#69002,
#69003,#69004,#69005,#69006,#69007,#69008,#69009,#69010,#69011,#69012,#69013,
#69014,#69015,#69016,#69017,#69018,#69019,#69020,#69021,#69022,#69023,#69024,
#69025,#69026,#69027,#69028,#69029,#69030,#69031,#69032,#69033,#69034,#69035,
#69036,#69037,#69038,#69039,#69040,#69041,#69042,#69043,#69044,#69045,#69046,
#69047,#69048,#69049,#69050,#69051,#69052,#69053,#69054,#69055,#69056,#69057,
#69058),(#69059,#69060,#69061,#69062,#69063,#69064,#69065,#69066,#69067,
#69068,#69069,#69070,#69071,#69072,#69073,#69074,#69075,#69076,#69077,#69078,
#69079,#69080,#69081,#69082,#69083,#69084,#69085,#69086,#69087,#69088,#69089,
#69090,#69091,#69092,#69093,#69094,#69095,#69096,#69097,#69098,#69099,#69100,
#69101,#69102,#69103,#69104,#69105,#69106,#69107,#69108,#69109,#69110,#69111,
#69112,#69113,#69114,#69115,#69116,#69117,#69118,#69119,#69120,#69121,#69122,
#69123,#69124,#69125,#69126,#69127,#69128,#69129,#69130,#69131,#69132,#69133,
#69134,#69135,#69136,#69137,#69138,#69139,#69140,#69141,#69142,#69143,#69144,
#69145,#69146,#69147,#69148,#69149,#69150,#69151,#69152,#69153,#69154,#69155,
#69156,#69157,#69158,#69159,#69160,#69161,#69162,#69163,#69164,#69165,#69166,
#69167,#69168,#69169,#69170,#69171,#69172,#69173,#69174,#69175,#69176,#69177,
#69178,#69179,#69180,#69181,#69182,#69183,#69184,#69185,#69186,#69187,#69188,
#69189,#69190,#69191,#69192,#69193,#69194,#69195,#69196,#69197,#69198,#69199,
#69200,#69201,#69202,#69203,#69204,#69205,#69206,#69207,#69208,#69209,#69210,
#69211,#69212,#69213,#69214,#69215,#69216,#69217,#69218,#69219,#69220,#69221,
#69222,#69223,#69224,#69225,#69226,#69227,#69228,#69229,#69230,#69231,#69232,
#69233,#69234,#69235,#69236,#69237,#69238,#69239,#69240,#69241,#69242,#69243,
#69244,#69245,#69246,#69247,#69248,#69249,#69250,#69251,#69252,#69253,#69254,
#69255,#69256,#69257,#69258,#69259,#69260,#69261,#69262,#69263,#69264,#69265,
#69266,#69267,#69268,#69269,#69270,#69271,#69272,#69273,#69274,#69275,#69276,
#69277,#69278,#69279,#69280,#69281,#69282,#69283,#69284,#69285,#69286,#69287,
#69288,#69289,#69290,#69291,#69292,#69293,#69294,#69295,#69296,#69297,#69298,
#69299,#69300,#69301,#69302,#69303,#69304,#69305,#69306,#69307,#69308,#69309,
#69310,#69311,#69312,#69313,#69314,#69315,#69316,#69317,#69318,#69319,#69320,
#69321,#69322,#69323,#69324,#69325,#69326,#69327,#69328,#69329,#69330,#69331,
#69332,#69333,#69334,#69335,#69336,#69337,#69338,#69339,#69340,#69341,#69342,
#69343,#69344,#69345,#69346,#69347,#69348,#69349,#69350,#69351,#69352,#69353,
#69354,#69355,#69356,#69357,#69358,#69359,#69360,#69361,#69362,#69363,#69364,
#69365,#69366,#69367,#69368,#69369,#69370,#69371,#69372,#69373,#69374,#69375,
#69376,#69377,#69378,#69379,#69380,#69381,#69382,#69383,#69384,#69385,#69386,
#69387,#69388,#69389,#69390,#69391,#69392,#69393,#69394,#69395,#69396,#69397,
#69398,#69399,#69400,#69401,#69402,#69403,#69404,#69405,#69406,#69407,#69408,
#69409,#69410,#69411,#69412,#69413,#69414,#69415,#69416,#69417,#69418,#69419,
#69420,#69421,#69422,#69423,#69424,#69425,#69426,#69427),(#69428,#69429,
#69430,#69431,#69432,#69433,#69434,#69435,#69436,#69437,#69438,#69439,#69440,
#69441,#69442,#69443,#69444,#69445,#69446,#69447,#69448,#69449,#69450,#69451,
#69452,#69453,#69454,#69455,#69456,#69457,#69458,#69459,#69460,#69461,#69462,
#69463,#69464,#69465,#69466,#69467,#69468,#69469,#69470,#69471,#69472,#69473,
#69474,#69475,#69476,#69477,#69478,#69479,#69480,#69481,#69482,#69483,#69484,
#69485,#69486,#69487,#69488,#69489,#69490,#69491,#69492,#69493,#69494,#69495,
#69496,#69497,#69498,#69499,#69500,#69501,#69502,#69503,#69504,#69505,#69506,
#69507,#69508,#69509,#69510,#69511,#69512,#69513,#69514,#69515,#69516,#69517,
#69518,#69519,#69520,#69521,#69522,#69523,#69524,#69525,#69526,#69527,#69528,
#69529,#69530,#69531,#69532,#69533,#69534,#69535,#69536,#69537,#69538,#69539,
#69540,#69541,#69542,#69543,#69544,#69545,#69546,#69547,#69548,#69549,#69550,
#69551,#69552,#69553,#69554,#69555,#69556,#69557,#69558,#69559,#69560,#69561,
#69562,#69563,#69564,#69565,#69566,#69567,#69568,#69569,#69570,#69571,#69572,
#69573,#69574,#69575,#69576,#69577,#69578,#69579,#69580,#69581,#69582,#69583,
#69584,#69585,#69586,#69587,#69588,#69589,#69590,#69591,#69592,#69593,#69594,
#69595,#69596,#69597,#69598,#69599,#69600,#69601,#69602,#69603,#69604,#69605,
#69606,#69607,#69608,#69609,#69610,#69611,#69612,#69613,#69614,#69615,#69616,
#69617,#69618,#69619,#69620,#69621,#69622,#69623,#69624,#69625,#69626,#69627,
#69628,#69629,#69630,#69631,#69632,#69633,#69634,#69635,#69636,#69637,#69638,
#69639,#69640,#69641,#69642,#69643,#69644,#69645,#69646,#69647,#69648,#69649,
#69650,#69651,#69652,#69653,#69654,#69655,#69656,#69657,#69658,#69659,#69660,
#69661,#69662,#69663,#69664,#69665,#69666,#69667,#69668,#69669,#69670,#69671,
#69672,#69673,#69674,#69675,#69676,#69677,#69678,#69679,#69680,#69681,#69682,
#69683,#69684,#69685,#69686,#69687,#69688,#69689,#69690,#69691,#69692,#69693,
#69694,#69695,#69696,#69697,#69698,#69699,#69700,#69701,#69702,#69703,#69704,
#69705,#69706,#69707,#69708,#69709,#69710,#69711,#69712,#69713,#69714,#69715,
#69716,#69717,#69718,#69719,#69720,#69721,#69722,#69723,#69724,#69725,#69726,
#69727,#69728,#69729,#69730,#69731,#69732,#69733,#69734,#69735,#69736,#69737,
#69738,#69739,#69740,#69741,#69742,#69743,#69744,#69745,#69746,#69747,#69748,
#69749,#69750,#69751,#69752,#69753,#69754,#69755,#69756,#69757,#69758,#69759,
#69760,#69761,#69762,#69763,#69764,#69765,#69766,#69767,#69768,#69769,#69770,
#69771,#69772,#69773,#69774,#69775,#69776,#69777,#69778,#69779,#69780,#69781,
#69782,#69783,#69784,#69785,#69786,#69787,#69788,#69789,#69790,#69791,#69792,
#69793,#69794,#69795,#69796),(#69797,#69798,#69799,#69800,#69801,#69802,
#69803,#69804,#69805,#69806,#69807,#69808,#69809,#69810,#69811,#69812,#69813,
#69814,#69815,#69816,#69817,#69818,#69819,#69820,#69821,#69822,#69823,#69824,
#69825,#69826,#69827,#69828,#69829,#69830,#69831,#69832,#69833,#69834,#69835,
#69836,#69837,#69838,#69839,#69840,#69841,#69842,#69843,#69844,#69845,#69846,
#69847,#69848,#69849,#69850,#69851,#69852,#69853,#69854,#69855,#69856,#69857,
#69858,#69859,#69860,#69861,#69862,#69863,#69864,#69865,#69866,#69867,#69868,
#69869,#69870,#69871,#69872,#69873,#69874,#69875,#69876,#69877,#69878,#69879,
#69880,#69881,#69882,#69883,#69884,#69885,#69886,#69887,#69888,#69889,#69890,
#69891,#69892,#69893,#69894,#69895,#69896,#69897,#69898,#69899,#69900,#69901,
#69902,#69903,#69904,#69905,#69906,#69907,#69908,#69909,#69910,#69911,#69912,
#69913,#69914,#69915,#69916,#69917,#69918,#69919,#69920,#69921,#69922,#69923,
#69924,#69925,#69926,#69927,#69928,#69929,#69930,#69931,#69932,#69933,#69934,
#69935,#69936,#69937,#69938,#69939,#69940,#69941,#69942,#69943,#69944,#69945,
#69946,#69947,#69948,#69949,#69950,#69951,#69952,#69953,#69954,#69955,#69956,
#69957,#69958,#69959,#69960,#69961,#69962,#69963,#69964,#69965,#69966,#69967,
#69968,#69969,#69970,#69971,#69972,#69973,#69974,#69975,#69976,#69977,#69978,
#69979,#69980,#69981,#69982,#69983,#69984,#69985,#69986,#69987,#69988,#69989,
#69990,#69991,#69992,#69993,#69994,#69995,#69996,#69997,#69998,#69999,#70000,
#70001,#70002,#70003,#70004,#70005,#70006,#70007,#70008,#70009,#70010,#70011,
#70012,#70013,#70014,#70015,#70016,#70017,#70018,#70019,#70020,#70021,#70022,
#70023,#70024,#70025,#70026,#70027,#70028,#70029,#70030,#70031,#70032,#70033,
#70034,#70035,#70036,#70037,#70038,#70039,#70040,#70041,#70042,#70043,#70044,
#70045,#70046,#70047,#70048,#70049,#70050,#70051,#70052,#70053,#70054,#70055,
#70056,#70057,#70058,#70059,#70060,#70061,#70062,#70063,#70064,#70065,#70066,
#70067,#70068,#70069,#70070,#70071,#70072,#70073,#70074,#70075,#70076,#70077,
#70078,#70079,#70080,#70081,#70082,#70083,#70084,#70085,#70086,#70087,#70088,
#70089,#70090,#70091,#70092,#70093,#70094,#70095,#70096,#70097,#70098,#70099,
#70100,#70101,#70102,#70103,#70104,#70105,#70106,#70107,#70108,#70109,#70110,
#70111,#70112,#70113,#70114,#70115,#70116,#70117,#70118,#70119,#70120,#70121,
#70122,#70123,#70124,#70125,#70126,#70127,#70128,#70129,#70130,#70131,#70132,
#70133,#70134,#70135,#70136,#70137,#70138,#70139,#70140,#70141,#70142,#70143,
#70144,#70145,#70146,#70147,#70148,#70149,#70150,#70151,#70152,#70153,#70154,
#70155,#70156,#70157,#70158,#70159,#70160,#70161,#70162,#70163,#70164,#70165)),
 .UNSPECIFIED.,.F.,.F.,.F.,(4,4),(4,1,1,1,1,1,1,1,1,1,1,1,1,1,1,1,1,1,1,
1,1,1,1,1,1,1,1,1,1,1,1,1,1,1,1,1,1,1,1,1,1,1,1,1,1,1,1,1,1,1,1,1,1,1,1,
1,1,1,1,1,1,1,1,1,1,1,1,1,1,1,1,1,1,1,1,1,1,1,1,1,1,1,1,1,1,1,1,1,1,1,1,
1,1,1,1,1,1,1,1,1,1,1,1,1,1,1,1,1,1,1,1,1,1,1,1,1,1,1,1,1,1,1,1,1,1,1,1,
1,1,1,1,1,1,1,1,1,1,1,1,1,1,1,1,1,1,1,1,1,1,1,1,1,1,1,1,1,1,1,1,1,1,1,1,
1,1,1,1,1,1,1,1,1,1,1,1,1,1,1,1,1,1,1,1,1,1,1,1,1,1,1,1,1,1,1,1,1,1,1,1,
1,1,1,1,1,1,1,1,1,1,1,1,1,1,1,1,1,1,1,1,1,1,1,1,1,1,1,1,1,1,1,1,1,1,1,1,
1,1,1,1,1,1,1,1,1,1,1,1,1,1,1,1,1,1,1,1,1,1,1,1,1,1,1,1,1,1,1,1,1,1,1,1,
1,1,1,1,1,1,1,1,1,1,1,1,1,1,1,1,1,1,1,1,1,1,1,1,1,1,1,1,1,1,1,1,1,1,1,1,
1,1,1,1,1,1,1,1,1,1,1,1,1,1,1,1,1,1,1,1,1,1,1,1,1,1,1,1,1,1,1,1,1,1,1,1,
1,1,1,1,1,1,1,1,1,1,1,1,1,1,1,1,1,1,1,1,1,1,1,4),(0.,0.0813890674476615),
(11.6630985309706,12.1606570983653,12.65821566576,13.1557742331546,13.6533328005493,
14.150891367944,14.6484499353386,15.1460085027333,15.643567070128,16.1411256375227,
16.6386842049173,17.136242772312,17.6338013397067,18.1313599071013,18.628918474496,
19.1264770418907,19.6240356092854,20.12159417668,20.6191527440747,21.1167113114694,
21.6142698788641,22.1118284462587,22.6093870136534,23.1069455810481,23.6045041484427,
24.1020627158374,24.5996212832321,25.0971798506268,25.5947384180214,26.0922969854161,
26.5898555528108,27.0874141202054,27.5849726876001,28.0825312549948,28.5800898223895,
29.0776483897841,29.5752069571788,30.0727655245735,30.5703240919681,31.0678826593628,
31.5654412267575,32.0629997941522,32.5605583615468,33.0581169289415,33.5556754963362,
34.0532340637308,34.5507926311255,35.0483511985202,35.5459097659149,36.0434683333095,
36.5410269007042,37.0385854680989,37.5361440354935,38.0337026028882,38.5312611702829,
39.0288197376776,39.5263783050722,40.0239368724669,40.5214954398616,41.0190540072562,
41.5166125746509,42.0141711420456,42.5117297094403,43.0092882768349,43.5068468442296,
44.0044054116243,44.501963979019,44.9995225464136,45.4970811138083,45.994639681203,
46.4921982485976,46.9897568159923,47.487315383387,47.9848739507816,48.4824325181763,
48.979991085571,49.4775496529657,49.9751082203603,50.472666787755,50.9702253551497,
51.4677839225444,51.965342489939,52.4629010573337,52.9604596247284,53.458018192123,
53.9555767595177,54.4531353269124,54.9506938943071,55.4482524617017,55.9458110290964,
56.4433695964911,56.9409281638857,57.4384867312804,57.9360452986751,58.4336038660698,
58.9311624334644,59.4287210008591,59.9262795682538,60.4238381356484,60.9213967030431,
61.4189552704378,61.9165138378325,62.4140724052271,62.9116309726218,63.4091895400165,
63.9067481074111,64.4043066748058,64.9018652422005,65.3994238095952,65.8969823769898,
66.3945409443845,66.8920995117792,67.3896580791738,67.8872166465685,68.3847752139632,
68.8823337813579,69.3798923487525,69.8774509161472,70.3750094835419,70.8725680509366,
71.3701266183312,71.8676851857259,72.3652437531206,72.8628023205152,73.3603608879099,
73.8579194553046,74.3554780226992,74.8530365900939,75.3505951574886,75.8481537248833,
76.3457122922779,76.8432708596726,77.3408294270673,77.838387994462,78.3359465618566,
78.8335051292513,79.331063696646,79.8286222640406,80.3261808314353,80.82373939883,
81.3212979662247,81.8188565336193,82.316415101014,82.8139736684087,83.3115322358033,
83.809090803198,84.3066493705927,84.8042079379874,85.301766505382,85.7993250727767,
86.2968836401714,86.794442207566,87.2920007749607,87.7895593423554,88.2871179097501,
88.7846764771447,89.2822350445394,89.7797936119341,90.2773521793287,90.7749107467234,
91.2724693141181,91.7700278815128,92.2675864489074,92.7651450163021,93.2627035836968,
93.7602621510915,94.2578207184861,94.7553792858808,95.2529378532755,95.7504964206701,
96.2480549880648,96.7456135554595,97.2431721228542,97.7407306902488,98.2382892576435,
98.7358478250382,99.2334063924328,99.7309649598275,100.228523527222,100.726082094617,
101.223640662012,101.721199229406,102.218757796801,102.716316364196,103.21387493159,
103.711433498985,104.20899206638,104.706550633774,105.204109201169,105.701667768564,
106.199226335958,106.696784903353,107.194343470748,107.691902038142,108.189460605537,
108.687019172932,109.184577740326,109.682136307721,110.179694875116,110.67725344251,
111.174812009905,111.6723705773,112.169929144694,112.667487712089,113.165046279484,
113.662604846878,114.160163414273,114.657721981668,115.155280549062,115.652839116457,
116.150397683852,116.647956251246,117.145514818641,117.643073386036,118.14063195343,
118.638190520825,119.13574908822,119.633307655614,120.130866223009,120.628424790404,
121.125983357798,121.623541925193,122.121100492588,122.618659059982,123.116217627377,
123.613776194772,124.111334762166,124.608893329561,125.106451896956,125.60401046435,
126.101569031745,126.59912759914,127.096686166534,127.594244733929,128.091803301324,
128.589361868718,129.086920436113,129.584479003508,130.082037570902,130.579596138297,
131.077154705692,131.574713273087,132.072271840481,132.569830407876,133.067388975271,
133.564947542665,134.06250611006,134.560064677455,135.057623244849,135.555181812244,
136.052740379639,136.550298947033,137.047857514428,137.545416081823,138.042974649217,
138.540533216612,139.038091784007,139.535650351401,140.033208918796,140.530767486191,
141.028326053585,141.52588462098,142.023443188375,142.521001755769,143.018560323164,
143.516118890559,144.013677457953,144.511236025348,145.008794592743,145.506353160137,
146.003911727532,146.501470294927,146.999028862321,147.496587429716,147.994145997111,
148.491704564505,148.9892631319,149.486821699295,149.984380266689,150.481938834084,
150.979497401479,151.477055968873,151.974614536268,152.472173103663,152.969731671057,
153.467290238452,153.964848805847,154.462407373241,154.959965940636,155.457524508031,
155.955083075425,156.45264164282,156.950200210215,157.447758777609,157.945317345004,
158.442875912399,158.940434479793,159.437993047188,159.935551614583,160.433110181977,
160.930668749372,161.428227316767,161.925785884161,162.423344451556,162.920903018951,
163.418461586346,163.91602015374,164.413578721135,164.91113728853,165.408695855924,
165.906254423319,166.403812990714,166.901371558108,167.398930125503,167.896488692898,
168.394047260292,168.891605827687,169.389164395082,169.886722962476,170.384281529871,
170.881840097266,171.37939866466,171.876957232055,172.37451579945,172.872074366844,
173.369632934239,173.867191501634,174.364750069028,174.862308636423,175.359867203818,
175.857425771212,176.354984338607,176.852542906002,177.350101473396,177.847660040791,
178.345218608186,178.84277717558,179.340335742975,179.83789431037,180.335452877764,
180.833011445159,181.330570012554,181.828128579948,182.325687147343,182.823245714738,
183.320804282132,183.818362849527,184.315921416922,184.813479984316,185.311038551711,
185.808597119106,186.3061556865,186.803714253895,187.30127282129,187.798831388684,
188.296389956079,188.793948523474,189.291507090868,189.789065658263,190.286624225658,
190.784182793052,191.281741360447,191.779299927842,192.276858495236,192.774417062631,
193.271975630026,193.76953419742),.UNSPECIFIED.);
#306=SHAPE_REPRESENTATION_RELATIONSHIP('SRR','None',#71694,#319);
#319=ADVANCED_BREP_SHAPE_REPRESENTATION('',(#345),#71626);
#332=STYLED_ITEM('',(#71825),#345);
#345=MANIFOLD_SOLID_BREP('Body1',#34219);
#682=B_SPLINE_CURVE_WITH_KNOTS('',3,(#63099,#63100,#63101,#63102,#63103,
#63104,#63105,#63106,#63107,#63108,#63109,#63110,#63111,#63112,#63113,#63114),
 .UNSPECIFIED.,.F.,.F.,(4,3,3,3,3,4),(-4.04486473697844,-3.98046853915737,
-3.4829099717627,-2.98535140436803,-2.48779283697336,-2.01331729429997),
 .UNSPECIFIED.);
#683=B_SPLINE_CURVE_WITH_KNOTS('',3,(#63117,#63118,#63119,#63120,#63121,
#63122,#63123,#63124,#63125,#63126),.UNSPECIFIED.,.F.,.F.,(4,3,3,4),(0.,
0.497558567394675,0.995117134789351,1.11004521091141),.UNSPECIFIED.);
#684=B_SPLINE_CURVE_WITH_KNOTS('',3,(#63131,#63132,#63133,#63134,#63135,
#63136,#63137,#63138,#63139,#63140,#63141,#63142,#63143,#63144,#63145,#63146,
#63147,#63148,#63149,#63150,#63151,#63152,#63153,#63154,#63155,#63156,#63157,
#63158,#63159,#63160,#63161,#63162,#63163,#63164,#63165,#63166,#63167,#63168,
#63169,#63170),.UNSPECIFIED.,.F.,.F.,(4,3,3,3,3,3,3,3,3,3,3,3,3,4),(-10.328050044158,
-9.95117134789344,-9.45361278049877,-8.95605421310409,-8.45849564570942,
-7.96093707831475,-7.46337851092008,-6.96581994352541,-6.46826137613073,
-5.97070280873606,-5.47314424134139,-4.97558567394672,-4.47802710655205,
-4.04486473697844),.UNSPECIFIED.);
#685=B_SPLINE_CURVE_WITH_KNOTS('',3,(#63171,#63172,#63173,#63174,#63175,
#63176,#63177,#63178,#63179,#63180,#63181,#63182,#63183,#63184,#63185,#63186,
#63187,#63188,#63189,#63190,#63191,#63192,#63193,#63194,#63195,#63196,#63197,
#63198,#63199,#63200,#63201,#63202,#63203,#63204,#63205,#63206,#63207,#63208,
#63209,#63210),.UNSPECIFIED.,.F.,.F.,(4,3,3,3,3,3,3,3,3,3,3,3,3,4),(1.11004521091141,
1.49267570218402,1.99023426957869,2.48779283697337,2.98535140436804,3.48290997176271,
3.98046853915738,4.47802710655206,4.97558567394673,5.4731442413414,5.97070280873607,
6.46826137613074,6.96581994352541,7.39323051809098),.UNSPECIFIED.);
#686=B_SPLINE_CURVE_WITH_KNOTS('',3,(#63215,#63216,#63217,#63218,#63219,
#63220,#63221,#63222,#63223,#63224,#63225,#63226,#63227,#63228,#63229,#63230,
#63231,#63232,#63233,#63234,#63235,#63236,#63237,#63238,#63239,#63240,#63241,
#63242,#63243,#63244,#63245,#63246,#63247,#63248,#63249,#63250,#63251,#63252,
#63253,#63254,#63255,#63256,#63257),.UNSPECIFIED.,.F.,.F.,(4,3,3,3,3,3,
3,3,3,3,3,3,3,3,4),(-16.6112353513376,-16.4194327240242,-15.9218741566295,
-15.4243155892348,-14.9267570218402,-14.4291984544455,-13.9316398870508,
-13.4340813196561,-12.9365227522615,-12.4389641848668,-11.9414056174721,
-11.4438470500775,-10.9462884826828,-10.4487299152881,-10.328050044158),
 .UNSPECIFIED.);
#687=B_SPLINE_CURVE_WITH_KNOTS('',3,(#63258,#63259,#63260,#63261,#63262,
#63263,#63264,#63265,#63266,#63267,#63268,#63269,#63270,#63271,#63272,#63273,
#63274,#63275,#63276,#63277,#63278,#63279,#63280,#63281,#63282,#63283,#63284,
#63285,#63286,#63287,#63288,#63289,#63290,#63291,#63292,#63293,#63294,#63295,
#63296,#63297,#63298,#63299,#63300),.UNSPECIFIED.,.F.,.F.,(4,3,3,3,3,3,
3,3,3,3,3,3,3,3,4),(7.39323051809098,7.46337851092009,7.96093707831476,
8.45849564570943,8.9560542131041,9.45361278049877,9.95117134789344,10.4487299152881,
10.9462884826828,11.4438470500775,11.9414056174721,12.4389641848668,12.9365227522615,
13.4340813196561,13.6764158252706),.UNSPECIFIED.);
#688=B_SPLINE_CURVE_WITH_KNOTS('',3,(#63305,#63306,#63307,#63308,#63309,
#63310,#63311,#63312,#63313,#63314,#63315,#63316,#63317,#63318,#63319,#63320,
#63321,#63322,#63323,#63324,#63325,#63326,#63327,#63328,#63329,#63330,#63331,
#63332,#63333,#63334,#63335,#63336,#63337,#63338,#63339,#63340,#63341,#63342,
#63343,#63344,#63345,#63346,#63347),.UNSPECIFIED.,.F.,.F.,(4,3,3,3,3,3,
3,3,3,3,3,3,3,3,4),(-22.8944206585172,-22.8876941001549,-22.3901355327602,
-21.8925769653656,-21.3950183979709,-20.8974598305762,-20.3999012631815,
-19.9023426957869,-19.4047841283922,-18.9072255609975,-18.4096669936029,
-17.9121084262082,-17.4145498588135,-16.9169912914188,-16.6112353513376),
 .UNSPECIFIED.);
#689=B_SPLINE_CURVE_WITH_KNOTS('',3,(#63348,#63349,#63350,#63351,#63352,
#63353,#63354,#63355,#63356,#63357,#63358,#63359,#63360,#63361,#63362,#63363,
#63364,#63365,#63366,#63367,#63368,#63369,#63370,#63371,#63372,#63373,#63374,
#63375,#63376,#63377,#63378,#63379,#63380,#63381,#63382,#63383,#63384,#63385,
#63386,#63387,#63388,#63389,#63390),.UNSPECIFIED.,.F.,.F.,(4,3,3,3,3,3,
3,3,3,3,3,3,3,3,4),(13.6764158252706,13.9316398870508,14.4291984544455,
14.9267570218402,15.4243155892348,15.9218741566295,16.4194327240242,16.9169912914188,
17.4145498588135,17.9121084262082,18.4096669936029,18.9072255609975,19.4047841283922,
19.9023426957869,19.9596011324502),.UNSPECIFIED.);
#690=B_SPLINE_CURVE_WITH_KNOTS('',3,(#63395,#63396,#63397,#63398,#63399,
#63400,#63401,#63402,#63403,#63404,#63405,#63406,#63407,#63408,#63409,#63410,
#63411,#63412,#63413,#63414,#63415,#63416,#63417,#63418,#63419,#63420,#63421,
#63422,#63423,#63424,#63425,#63426,#63427,#63428,#63429,#63430,#63431,#63432,
#63433,#63434),.UNSPECIFIED.,.F.,.F.,(4,3,3,3,3,3,3,3,3,3,3,3,3,4),(-29.1776059656968,
-28.858396908891,-28.3608383414963,-27.8632797741016,-27.3657212067069,
-26.8681626393123,-26.3706040719176,-25.8730455045229,-25.3754869371283,
-24.8779283697336,-24.3803698023389,-23.8828112349442,-23.3852526675496,
-22.8944206585172),.UNSPECIFIED.);
#691=B_SPLINE_CURVE_WITH_KNOTS('',3,(#63435,#63436,#63437,#63438,#63439,
#63440,#63441,#63442,#63443,#63444,#63445,#63446,#63447,#63448,#63449,#63450,
#63451,#63452,#63453,#63454,#63455,#63456,#63457,#63458,#63459,#63460,#63461,
#63462,#63463,#63464,#63465,#63466,#63467,#63468,#63469,#63470,#63471,#63472,
#63473,#63474),.UNSPECIFIED.,.F.,.F.,(4,3,3,3,3,3,3,3,3,3,3,3,3,4),(19.9596011324502,
20.3999012631816,20.8974598305762,21.3950183979709,21.8925769653656,22.3901355327602,
22.8876941001549,23.3852526675496,23.8828112349443,24.3803698023389,24.8779283697336,
25.3754869371283,25.8730455045229,26.2427864396298),.UNSPECIFIED.);
#692=B_SPLINE_CURVE_WITH_KNOTS('',3,(#63479,#63480,#63481,#63482,#63483,
#63484,#63485,#63486,#63487,#63488,#63489,#63490,#63491,#63492,#63493,#63494,
#63495,#63496,#63497,#63498,#63499,#63500,#63501,#63502,#63503,#63504,#63505,
#63506,#63507,#63508,#63509,#63510,#63511,#63512,#63513,#63514,#63515,#63516,
#63517,#63518,#63519,#63520,#63521),.UNSPECIFIED.,.F.,.F.,(4,3,3,3,3,3,
3,3,3,3,3,3,3,3,4),(-35.4607912728764,-35.3266582850217,-34.829099717627,
-34.3315411502324,-33.8339825828377,-33.336424015443,-32.8388654480483,
-32.3413068806537,-31.843748313259,-31.3461897458643,-30.8486311784696,
-30.351072611075,-29.8535140436803,-29.3559554762856,-29.1776059656968),
 .UNSPECIFIED.);
#693=B_SPLINE_CURVE_WITH_KNOTS('',3,(#63522,#63523,#63524,#63525,#63526,
#63527,#63528,#63529,#63530,#63531,#63532,#63533,#63534,#63535,#63536,#63537,
#63538,#63539,#63540,#63541,#63542,#63543,#63544,#63545,#63546,#63547,#63548,
#63549,#63550,#63551,#63552,#63553,#63554,#63555,#63556,#63557,#63558,#63559,
#63560,#63561,#63562,#63563,#63564),.UNSPECIFIED.,.F.,.F.,(4,3,3,3,3,3,
3,3,3,3,3,3,3,3,4),(26.2427864396298,26.3706040719176,26.8681626393123,
27.365721206707,27.8632797741016,28.3608383414963,28.858396908891,29.3559554762856,
29.8535140436803,30.351072611075,30.8486311784697,31.3461897458643,31.843748313259,
32.3413068806537,32.5259717468093),.UNSPECIFIED.);
#694=B_SPLINE_CURVE_WITH_KNOTS('',3,(#63569,#63570,#63571,#63572,#63573,
#63574,#63575,#63576,#63577,#63578,#63579,#63580,#63581,#63582,#63583,#63584,
#63585,#63586,#63587,#63588,#63589,#63590,#63591,#63592,#63593,#63594,#63595,
#63596,#63597,#63598,#63599,#63600,#63601,#63602,#63603,#63604,#63605,#63606,
#63607,#63608),.UNSPECIFIED.,.F.,.F.,(4,3,3,3,3,3,3,3,3,3,3,3,3,4),(-41.743976580056,
-41.2973610937578,-40.7998025263631,-40.3022439589684,-39.8046853915737,
-39.3071268241791,-38.8095682567844,-38.3120096893897,-37.8144511219951,
-37.3168925546004,-36.8193339872057,-36.321775419811,-35.8242168524164,
-35.4607912728764),.UNSPECIFIED.);
#695=B_SPLINE_CURVE_WITH_KNOTS('',3,(#63609,#63610,#63611,#63612,#63613,
#63614,#63615,#63616,#63617,#63618,#63619,#63620,#63621,#63622,#63623,#63624,
#63625,#63626,#63627,#63628,#63629,#63630,#63631,#63632,#63633,#63634,#63635,
#63636,#63637,#63638,#63639,#63640,#63641,#63642,#63643,#63644,#63645,#63646,
#63647,#63648),.UNSPECIFIED.,.F.,.F.,(4,3,3,3,3,3,3,3,3,3,3,3,3,4),(32.5259717468093,
32.8388654480483,33.336424015443,33.8339825828377,34.3315411502324,34.829099717627,
35.3266582850217,35.8242168524164,36.3217754198111,36.8193339872057,37.3168925546004,
37.8144511219951,38.3120096893898,38.8091570539889),.UNSPECIFIED.);
#696=B_SPLINE_CURVE_WITH_KNOTS('',3,(#63653,#63654,#63655,#63656,#63657,
#63658,#63659,#63660,#63661,#63662,#63663,#63664,#63665,#63666,#63667,#63668,
#63669,#63670,#63671,#63672,#63673,#63674,#63675,#63676,#63677,#63678,#63679,
#63680,#63681,#63682,#63683,#63684,#63685,#63686,#63687,#63688,#63689,#63690,
#63691,#63692,#63693,#63694,#63695),.UNSPECIFIED.,.F.,.F.,(4,3,3,3,3,3,
3,3,3,3,3,3,3,3,4),(-48.0271618872356,-47.7656224698885,-47.2680639024938,
-46.7705053350992,-46.2729467677045,-45.7753882003098,-45.2778296329151,
-44.7802710655205,-44.2827124981258,-43.7851539307311,-43.2875953633364,
-42.7900367959418,-42.2924782285471,-41.7949196611524,-41.743976580056),
 .UNSPECIFIED.);
#697=B_SPLINE_CURVE_WITH_KNOTS('',3,(#63696,#63697,#63698,#63699,#63700,
#63701,#63702,#63703,#63704,#63705,#63706,#63707,#63708,#63709,#63710,#63711,
#63712,#63713,#63714,#63715,#63716,#63717,#63718,#63719,#63720,#63721,#63722,
#63723,#63724,#63725,#63726,#63727,#63728,#63729,#63730,#63731,#63732,#63733,
#63734,#63735),.UNSPECIFIED.,.F.,.F.,(4,3,3,3,3,3,3,3,3,3,3,3,3,4),(38.8091570539889,
39.3071268241791,39.8046853915738,40.3022439589684,40.7998025263631,41.2973610937578,
41.7949196611524,42.2924782285471,42.7900367959418,43.2875953633364,43.7851539307311,
44.2827124981258,44.7802710655205,45.0923423611685),.UNSPECIFIED.);
#698=B_SPLINE_CURVE_WITH_KNOTS('',3,(#63740,#63741,#63742,#63743,#63744,
#63745,#63746,#63747,#63748,#63749,#63750,#63751,#63752,#63753,#63754,#63755,
#63756,#63757,#63758,#63759,#63760,#63761,#63762,#63763,#63764,#63765,#63766,
#63767,#63768,#63769,#63770,#63771,#63772,#63773,#63774,#63775,#63776,#63777,
#63778,#63779,#63780,#63781,#63782),.UNSPECIFIED.,.F.,.F.,(4,3,3,3,3,3,
3,3,3,3,3,3,3,3,4),(-54.3103471944151,-54.2338838460192,-53.7363252786246,
-53.2387667112299,-52.7412081438352,-52.2436495764405,-51.7460910090459,
-51.2485324416512,-50.7509738742565,-50.2534153068619,-49.7558567394672,
-49.2582981720725,-48.7607396046778,-48.2631810372832,-48.0271618872356),
 .UNSPECIFIED.);
#699=B_SPLINE_CURVE_WITH_KNOTS('',3,(#63783,#63784,#63785,#63786,#63787,
#63788,#63789,#63790,#63791,#63792,#63793,#63794,#63795,#63796,#63797,#63798,
#63799,#63800,#63801,#63802,#63803,#63804,#63805,#63806,#63807,#63808,#63809,
#63810,#63811,#63812,#63813,#63814,#63815,#63816,#63817,#63818,#63819,#63820,
#63821,#63822,#63823,#63824,#63825),.UNSPECIFIED.,.F.,.F.,(4,3,3,3,3,3,
3,3,3,3,3,3,3,3,4),(45.0923423611685,45.2778296329151,45.7753882003098,
46.2729467677045,46.7705053350991,47.2680639024938,47.7656224698885,48.2631810372832,
48.7607396046778,49.2582981720725,49.7558567394672,50.2534153068619,50.7509738742565,
51.2485324416512,51.3755276683481),.UNSPECIFIED.);
#700=B_SPLINE_CURVE_WITH_KNOTS('',3,(#63830,#63831,#63832,#63833,#63834,
#63835,#63836,#63837,#63838,#63839,#63840,#63841,#63842,#63843,#63844,#63845,
#63846,#63847,#63848,#63849,#63850,#63851,#63852,#63853,#63854,#63855,#63856,
#63857,#63858,#63859,#63860,#63861,#63862,#63863,#63864,#63865,#63866,#63867,
#63868,#63869),.UNSPECIFIED.,.F.,.F.,(4,3,3,3,3,3,3,3,3,3,3,3,3,4),(-60.5935325015948,
-60.2045866547553,-59.7070280873606,-59.2094695199659,-58.7119109525713,
-58.2143523851766,-57.7167938177819,-57.2192352503872,-56.7216766829926,
-56.2241181155979,-55.7265595482032,-55.2290009808086,-54.7314424134139,
-54.3103471944151),.UNSPECIFIED.);
#701=B_SPLINE_CURVE_WITH_KNOTS('',3,(#63870,#63871,#63872,#63873,#63874,
#63875,#63876,#63877,#63878,#63879,#63880,#63881,#63882,#63883,#63884,#63885,
#63886,#63887,#63888,#63889,#63890,#63891,#63892,#63893,#63894,#63895,#63896,
#63897,#63898,#63899,#63900,#63901,#63902,#63903,#63904,#63905,#63906,#63907,
#63908,#63909),.UNSPECIFIED.,.F.,.F.,(4,3,3,3,3,3,3,3,3,3,3,3,3,4),(51.3755276683481,
51.7460910090459,52.2436495764406,52.7412081438352,53.2387667112299,53.7363252786246,
54.2338838460192,54.7314424134139,55.2290009808086,55.7265595482033,56.2241181155979,
56.7216766829926,57.2192352503873,57.6587129755277),.UNSPECIFIED.);
#702=B_SPLINE_CURVE_WITH_KNOTS('',3,(#63914,#63915,#63916,#63917,#63918,
#63919,#63920,#63921,#63922,#63923,#63924,#63925,#63926,#63927,#63928,#63929,
#63930,#63931,#63932,#63933,#63934,#63935,#63936,#63937,#63938,#63939,#63940,
#63941,#63942,#63943,#63944,#63945,#63946,#63947,#63948,#63949,#63950,#63951,
#63952,#63953,#63954,#63955,#63956),.UNSPECIFIED.,.F.,.F.,(4,3,3,3,3,3,
3,3,3,3,3,3,3,3,4),(-66.8767178087743,-66.672848030886,-66.1752894634913,
-65.6777308960967,-65.180172328702,-64.6826137613073,-64.1850551939127,
-63.687496626518,-63.1899380591233,-62.6923794917286,-62.194820924334,-61.6972623569393,
-61.1997037895446,-60.70214522215,-60.5935325015948),.UNSPECIFIED.);
#703=B_SPLINE_CURVE_WITH_KNOTS('',3,(#63957,#63958,#63959,#63960,#63961,
#63962,#63963,#63964,#63965,#63966,#63967,#63968,#63969,#63970,#63971,#63972,
#63973,#63974,#63975,#63976,#63977,#63978,#63979,#63980,#63981,#63982,#63983,
#63984,#63985,#63986,#63987,#63988,#63989,#63990,#63991,#63992,#63993,#63994,
#63995,#63996,#63997,#63998,#63999),.UNSPECIFIED.,.F.,.F.,(4,3,3,3,3,3,
3,3,3,3,3,3,3,3,4),(57.6587129755277,57.7167938177819,58.2143523851766,
58.7119109525713,59.2094695199659,59.7070280873606,60.2045866547553,60.70214522215,
61.1997037895446,61.6972623569393,62.194820924334,62.6923794917287,63.1899380591233,
63.687496626518,63.9418982827073),.UNSPECIFIED.);
#704=B_SPLINE_CURVE_WITH_KNOTS('',3,(#64004,#64005,#64006,#64007,#64008,
#64009,#64010,#64011,#64012,#64013,#64014,#64015,#64016,#64017,#64018,#64019,
#64020,#64021,#64022,#64023,#64024,#64025,#64026,#64027,#64028,#64029,#64030,
#64031,#64032,#64033,#64034,#64035,#64036,#64037,#64038,#64039,#64040,#64041,
#64042,#64043,#64044,#64045,#64046),.UNSPECIFIED.,.F.,.F.,(4,3,3,3,3,3,
3,3,3,3,3,3,3,3,4),(-73.1599031159539,-73.1411094070167,-72.6435508396221,
-72.1459922722274,-71.6484337048327,-71.150875137438,-70.6533165700434,
-70.1557580026487,-69.658199435254,-69.1606408678594,-68.6630823004647,
-68.16552373307,-67.6679651656754,-67.1704065982807,-66.8767178087743),
 .UNSPECIFIED.);
#705=B_SPLINE_CURVE_WITH_KNOTS('',3,(#64047,#64048,#64049,#64050,#64051,
#64052,#64053,#64054,#64055,#64056,#64057,#64058,#64059,#64060,#64061,#64062,
#64063,#64064,#64065,#64066,#64067,#64068,#64069,#64070,#64071,#64072,#64073,
#64074,#64075,#64076,#64077,#64078,#64079,#64080,#64081,#64082,#64083,#64084,
#64085,#64086,#64087,#64088,#64089),.UNSPECIFIED.,.F.,.F.,(4,3,3,3,3,3,
3,3,3,3,3,3,3,3,4),(63.9418982827073,64.1850551939127,64.6826137613073,
65.180172328702,65.6777308960967,66.1752894634914,66.672848030886,67.1704065982807,
67.6679651656754,68.16552373307,68.6630823004647,69.1606408678594,69.6581994352541,
70.1557580026487,70.2250835898869),.UNSPECIFIED.);
#706=B_SPLINE_CURVE_WITH_KNOTS('',3,(#64094,#64095,#64096,#64097,#64098,
#64099,#64100,#64101,#64102,#64103,#64104,#64105,#64106,#64107,#64108,#64109,
#64110,#64111,#64112,#64113,#64114,#64115,#64116,#64117,#64118,#64119,#64120,
#64121,#64122,#64123,#64124,#64125,#64126,#64127,#64128,#64129,#64130,#64131,
#64132,#64133),.UNSPECIFIED.,.F.,.F.,(4,3,3,3,3,3,3,3,3,3,3,3,3,4),(-79.4430884231335,
-79.1118122157528,-78.6142536483581,-78.1166950809635,-77.6191365135688,
-77.1215779461741,-76.6240193787795,-76.1264608113848,-75.6289022439901,
-75.1313436765954,-74.6337851092008,-74.1362265418061,-73.6386679744114,
-73.1599031159539),.UNSPECIFIED.);
#707=B_SPLINE_CURVE_WITH_KNOTS('',3,(#64134,#64135,#64136,#64137,#64138,
#64139,#64140,#64141,#64142,#64143,#64144,#64145,#64146,#64147,#64148,#64149,
#64150,#64151,#64152,#64153,#64154,#64155,#64156,#64157,#64158,#64159,#64160,
#64161,#64162,#64163,#64164,#64165,#64166,#64167,#64168,#64169,#64170,#64171,
#64172,#64173),.UNSPECIFIED.,.F.,.F.,(4,3,3,3,3,3,3,3,3,3,3,3,3,4),(70.2250835898869,
70.6533165700434,71.1508751374381,71.6484337048327,72.1459922722274,72.6435508396221,
73.1411094070168,73.6386679744114,74.1362265418061,74.6337851092008,75.1313436765954,
75.6289022439901,76.1264608113848,76.5082688970665),.UNSPECIFIED.);
#708=B_SPLINE_CURVE_WITH_KNOTS('',3,(#64178,#64179,#64180,#64181,#64182,
#64183,#64184,#64185,#64186,#64187,#64188,#64189,#64190,#64191,#64192,#64193,
#64194,#64195,#64196,#64197,#64198,#64199,#64200,#64201,#64202,#64203,#64204,
#64205,#64206,#64207,#64208,#64209,#64210,#64211,#64212,#64213,#64214,#64215,
#64216,#64217,#64218,#64219,#64220),.UNSPECIFIED.,.F.,.F.,(4,3,3,3,3,3,
3,3,3,3,3,3,3,3,4),(-85.7262737303131,-85.5800735918835,-85.0825150244889,
-84.5849564570942,-84.0873978896995,-83.5898393223049,-83.0922807549102,
-82.5947221875155,-82.0971636201208,-81.5996050527262,-81.1020464853315,
-80.6044879179368,-80.1069293505422,-79.6093707831475,-79.4430884231335),
 .UNSPECIFIED.);
#709=B_SPLINE_CURVE_WITH_KNOTS('',3,(#64221,#64222,#64223,#64224,#64225,
#64226,#64227,#64228,#64229,#64230,#64231,#64232,#64233,#64234,#64235,#64236,
#64237,#64238,#64239,#64240,#64241,#64242,#64243,#64244,#64245,#64246,#64247,
#64248,#64249,#64250,#64251,#64252,#64253,#64254,#64255,#64256,#64257,#64258,
#64259,#64260,#64261,#64262,#64263),.UNSPECIFIED.,.F.,.F.,(4,3,3,3,3,3,
3,3,3,3,3,3,3,3,4),(76.5082688970665,76.6240193787795,77.1215779461741,
77.6191365135688,78.1166950809635,78.6142536483582,79.1118122157528,79.6093707831475,
80.1069293505422,80.6044879179368,81.1020464853315,81.5996050527262,82.0971636201209,
82.5947221875155,82.7914542042461),.UNSPECIFIED.);
#710=B_SPLINE_CURVE_WITH_KNOTS('',3,(#64268,#64269,#64270,#64271,#64272,
#64273,#64274,#64275,#64276,#64277,#64278,#64279,#64280,#64281,#64282,#64283,
#64284,#64285,#64286,#64287,#64288,#64289,#64290,#64291,#64292,#64293,#64294,
#64295,#64296,#64297,#64298,#64299,#64300,#64301,#64302,#64303,#64304,#64305,
#64306,#64307),.UNSPECIFIED.,.F.,.F.,(4,3,3,3,3,3,3,3,3,3,3,3,3,4),(-92.0094590374927,
-91.5507764006196,-91.0532178332249,-90.5556592658303,-90.0581006984356,
-89.5605421310409,-89.0629835636462,-88.5654249962516,-88.0678664288569,
-87.5703078614622,-87.0727492940676,-86.5751907266729,-86.0776321592782,
-85.7262737303131),.UNSPECIFIED.);
#711=B_SPLINE_CURVE_WITH_KNOTS('',3,(#64308,#64309,#64310,#64311,#64312,
#64313,#64314,#64315,#64316,#64317,#64318,#64319,#64320,#64321,#64322,#64323,
#64324,#64325,#64326,#64327,#64328,#64329,#64330,#64331,#64332,#64333,#64334,
#64335,#64336,#64337,#64338,#64339,#64340,#64341,#64342,#64343,#64344,#64345,
#64346,#64347,#64348,#64349,#64350),.UNSPECIFIED.,.F.,.F.,(4,3,3,3,3,3,
3,3,3,3,3,3,3,3,4),(82.7914542042461,83.0922807549102,83.5898393223049,
84.0873978896996,84.5849564570942,85.0825150244889,85.5800735918836,86.0776321592782,
86.5751907266729,87.0727492940676,87.5703078614623,88.0678664288569,88.5654249962516,
89.0629835636463,89.0746395114257),.UNSPECIFIED.);
#712=B_SPLINE_CURVE_WITH_KNOTS('',3,(#64355,#64356,#64357,#64358,#64359,
#64360,#64361,#64362,#64363,#64364,#64365,#64366,#64367,#64368,#64369,#64370,
#64371,#64372,#64373,#64374,#64375,#64376,#64377,#64378,#64379,#64380,#64381,
#64382,#64383,#64384,#64385,#64386,#64387,#64388,#64389,#64390,#64391,#64392,
#64393,#64394,#64395,#64396,#64397),.UNSPECIFIED.,.F.,.F.,(4,3,3,3,3,3,
3,3,3,3,3,3,3,3,4),(-98.2926443446723,-98.0190377767503,-97.5214792093557,
-97.023920641961,-96.5263620745663,-96.0288035071717,-95.531244939777,-95.0336863723823,
-94.5361278049876,-94.038569237593,-93.5410106701983,-93.0434521028036,
-92.5458935354089,-92.0483349680143,-92.0094590374927),.UNSPECIFIED.);
#713=B_SPLINE_CURVE_WITH_KNOTS('',3,(#64398,#64399,#64400,#64401,#64402,
#64403,#64404,#64405,#64406,#64407,#64408,#64409,#64410,#64411,#64412,#64413,
#64414,#64415,#64416,#64417,#64418,#64419,#64420,#64421,#64422,#64423,#64424,
#64425,#64426,#64427,#64428,#64429,#64430,#64431,#64432,#64433,#64434,#64435,
#64436,#64437),.UNSPECIFIED.,.F.,.F.,(4,3,3,3,3,3,3,3,3,3,3,3,3,4),(89.0746395114257,
89.5605421310409,90.0581006984356,90.5556592658303,91.0532178332249,91.5507764006196,
92.0483349680143,92.545893535409,93.0434521028036,93.5410106701983,94.038569237593,
94.5361278049877,95.0336863723823,95.3578248186053),.UNSPECIFIED.);
#714=B_SPLINE_CURVE_WITH_KNOTS('',3,(#64442,#64443,#64444,#64445,#64446,
#64447,#64448,#64449,#64450,#64451,#64452,#64453,#64454,#64455,#64456,#64457,
#64458,#64459,#64460,#64461,#64462,#64463,#64464,#64465,#64466,#64467,#64468,
#64469,#64470,#64471,#64472,#64473,#64474,#64475,#64476,#64477,#64478,#64479,
#64480,#64481,#64482,#64483,#64484),.UNSPECIFIED.,.F.,.F.,(4,3,3,3,3,3,
3,3,3,3,3,3,3,3,4),(-104.575829651852,-104.487299152881,-103.989740585486,
-103.492182018092,-102.994623450697,-102.497064883302,-101.999506315908,
-101.501947748513,-101.004389181118,-100.506830613724,-100.009272046329,
-99.5117134789344,-99.0141549115397,-98.516596344145,-98.2926443446723),
 .UNSPECIFIED.);
#715=B_SPLINE_CURVE_WITH_KNOTS('',3,(#64485,#64486,#64487,#64488,#64489,
#64490,#64491,#64492,#64493,#64494,#64495,#64496,#64497,#64498,#64499,#64500,
#64501,#64502,#64503,#64504,#64505,#64506,#64507,#64508,#64509,#64510,#64511,
#64512,#64513,#64514,#64515,#64516,#64517,#64518,#64519,#64520,#64521,#64522,
#64523,#64524,#64525,#64526,#64527),.UNSPECIFIED.,.F.,.F.,(4,3,3,3,3,3,
3,3,3,3,3,3,3,3,4),(95.3578248186053,95.531244939777,96.0288035071717,96.5263620745663,
97.023920641961,97.5214792093557,98.0190377767504,98.516596344145,99.0141549115397,
99.5117134789344,100.009272046329,100.506830613724,101.004389181118,101.501947748513,
101.641010125785),.UNSPECIFIED.);
#716=B_SPLINE_CURVE_WITH_KNOTS('',3,(#64532,#64533,#64534,#64535,#64536,
#64537,#64538,#64539,#64540,#64541,#64542,#64543,#64544,#64545,#64546,#64547,
#64548,#64549,#64550,#64551,#64552,#64553,#64554,#64555,#64556,#64557,#64558,
#64559,#64560,#64561,#64562,#64563,#64564,#64565,#64566,#64567,#64568,#64569,
#64570,#64571),.UNSPECIFIED.,.F.,.F.,(4,3,3,3,3,3,3,3,3,3,3,3,3,4),(-110.859014959031,
-110.458001961617,-109.960443394222,-109.462884826828,-108.965326259433,
-108.467767692038,-107.970209124644,-107.472650557249,-106.975091989854,
-106.47753342246,-105.979974855065,-105.48241628767,-104.984857720276,-104.575829651852),
 .UNSPECIFIED.);
#717=B_SPLINE_CURVE_WITH_KNOTS('',3,(#64572,#64573,#64574,#64575,#64576,
#64577,#64578,#64579,#64580,#64581,#64582,#64583,#64584,#64585,#64586,#64587,
#64588,#64589,#64590,#64591,#64592,#64593,#64594,#64595,#64596,#64597,#64598,
#64599,#64600,#64601,#64602,#64603,#64604,#64605,#64606,#64607,#64608,#64609,
#64610,#64611),.UNSPECIFIED.,.F.,.F.,(4,3,3,3,3,3,3,3,3,3,3,3,3,4),(101.641010125785,
101.999506315908,102.497064883302,102.994623450697,103.492182018092,103.989740585486,
104.487299152881,104.984857720276,105.48241628767,105.979974855065,106.47753342246,
106.975091989854,107.472650557249,107.924195432964),.UNSPECIFIED.);
#718=B_SPLINE_CURVE_WITH_KNOTS('',3,(#64616,#64617,#64618,#64619,#64620,
#64621,#64622,#64623,#64624,#64625,#64626,#64627,#64628,#64629,#64630,#64631,
#64632,#64633,#64634,#64635,#64636,#64637,#64638,#64639,#64640,#64641,#64642,
#64643,#64644,#64645,#64646,#64647,#64648,#64649,#64650,#64651,#64652,#64653,
#64654,#64655,#64656,#64657,#64658),.UNSPECIFIED.,.F.,.F.,(4,3,3,3,3,3,
3,3,3,3,3,3,3,3,4),(-117.142200266211,-116.926263337748,-116.428704770353,
-115.931146202959,-115.433587635564,-114.936029068169,-114.438470500775,
-113.94091193338,-113.443353365985,-112.94579479859,-112.448236231196,-111.950677663801,
-111.453119096406,-110.955560529012,-110.859014959031),.UNSPECIFIED.);
#719=B_SPLINE_CURVE_WITH_KNOTS('',3,(#64659,#64660,#64661,#64662,#64663,
#64664,#64665,#64666,#64667,#64668,#64669,#64670,#64671,#64672,#64673,#64674,
#64675,#64676,#64677,#64678,#64679,#64680,#64681,#64682,#64683,#64684,#64685,
#64686,#64687,#64688,#64689,#64690,#64691,#64692,#64693,#64694,#64695,#64696,
#64697,#64698,#64699,#64700,#64701),.UNSPECIFIED.,.F.,.F.,(4,3,3,3,3,3,
3,3,3,3,3,3,3,3,4),(107.924195432964,107.970209124644,108.467767692038,
108.965326259433,109.462884826828,109.960443394222,110.458001961617,110.955560529012,
111.453119096406,111.950677663801,112.448236231196,112.945794798591,113.443353365985,
113.94091193338,114.207380740144),.UNSPECIFIED.);
#720=B_SPLINE_CURVE_WITH_KNOTS('',3,(#64706,#64707,#64708,#64709,#64710,
#64711,#64712,#64713,#64714,#64715,#64716,#64717,#64718,#64719,#64720,#64721,
#64722,#64723,#64724,#64725,#64726,#64727,#64728,#64729,#64730,#64731,#64732,
#64733,#64734,#64735,#64736,#64737,#64738,#64739,#64740,#64741,#64742,#64743,
#64744,#64745,#64746,#64747,#64748),.UNSPECIFIED.,.F.,.F.,(4,3,3,3,3,3,
3,3,3,3,3,3,3,3,4),(-123.425385573391,-123.394524713879,-122.896966146484,
-122.399407579089,-121.901849011695,-121.4042904443,-120.906731876905,-120.409173309511,
-119.911614742116,-119.414056174721,-118.916497607327,-118.418939039932,
-117.921380472537,-117.423821905143,-117.142200266211),.UNSPECIFIED.);
#721=B_SPLINE_CURVE_WITH_KNOTS('',3,(#64749,#64750,#64751,#64752,#64753,
#64754,#64755,#64756,#64757,#64758,#64759,#64760,#64761,#64762,#64763,#64764,
#64765,#64766,#64767,#64768,#64769,#64770,#64771,#64772,#64773,#64774,#64775,
#64776,#64777,#64778,#64779,#64780,#64781,#64782,#64783,#64784,#64785,#64786,
#64787,#64788,#64789,#64790,#64791),.UNSPECIFIED.,.F.,.F.,(4,3,3,3,3,3,
3,3,3,3,3,3,3,3,4),(114.207380740144,114.438470500775,114.936029068169,
115.433587635564,115.931146202959,116.428704770353,116.926263337748,117.423821905143,
117.921380472537,118.418939039932,118.916497607327,119.414056174721,119.911614742116,
120.409173309511,120.490566047324),.UNSPECIFIED.);
#722=B_SPLINE_CURVE_WITH_KNOTS('',3,(#64796,#64797,#64798,#64799,#64800,
#64801,#64802,#64803,#64804,#64805,#64806,#64807,#64808,#64809,#64810,#64811,
#64812,#64813,#64814,#64815,#64816,#64817,#64818,#64819,#64820,#64821,#64822,
#64823,#64824,#64825,#64826,#64827,#64828,#64829,#64830,#64831,#64832,#64833,
#64834,#64835),.UNSPECIFIED.,.F.,.F.,(4,3,3,3,3,3,3,3,3,3,3,3,3,4),(-129.70857088057,
-129.365227522615,-128.86766895522,-128.370110387825,-127.872551820431,
-127.374993253036,-126.877434685641,-126.379876118247,-125.882317550852,
-125.384758983457,-124.887200416063,-124.389641848668,-123.892083281273,
-123.425385573391),.UNSPECIFIED.);
#723=B_SPLINE_CURVE_WITH_KNOTS('',3,(#64836,#64837,#64838,#64839,#64840,
#64841,#64842,#64843,#64844,#64845,#64846,#64847,#64848,#64849,#64850,#64851,
#64852,#64853,#64854,#64855,#64856,#64857,#64858,#64859,#64860,#64861,#64862,
#64863,#64864,#64865,#64866,#64867,#64868,#64869,#64870,#64871,#64872,#64873,
#64874,#64875),.UNSPECIFIED.,.F.,.F.,(4,3,3,3,3,3,3,3,3,3,3,3,3,4),(120.490566047324,
120.906731876905,121.4042904443,121.901849011695,122.399407579089,122.896966146484,
123.394524713879,123.892083281273,124.389641848668,124.887200416063,125.384758983457,
125.882317550852,126.379876118247,126.773751354503),.UNSPECIFIED.);
#724=B_SPLINE_CURVE_WITH_KNOTS('',3,(#64880,#64881,#64882,#64883,#64884,
#64885,#64886,#64887,#64888,#64889,#64890,#64891,#64892,#64893,#64894,#64895,
#64896,#64897,#64898,#64899,#64900,#64901,#64902,#64903,#64904,#64905,#64906,
#64907,#64908,#64909,#64910,#64911,#64912,#64913,#64914,#64915,#64916,#64917,
#64918,#64919,#64920,#64921,#64922),.UNSPECIFIED.,.F.,.F.,(4,3,3,3,3,3,
3,3,3,3,3,3,3,3,4),(-135.99175618775,-135.833488898745,-135.335930331351,
-134.838371763956,-134.340813196561,-133.843254629167,-133.345696061772,
-132.848137494377,-132.350578926983,-131.853020359588,-131.355461792193,
-130.857903224799,-130.360344657404,-129.862786090009,-129.70857088057),
 .UNSPECIFIED.);
#725=B_SPLINE_CURVE_WITH_KNOTS('',3,(#64923,#64924,#64925,#64926,#64927,
#64928,#64929,#64930,#64931,#64932,#64933,#64934,#64935,#64936,#64937,#64938,
#64939,#64940,#64941,#64942,#64943,#64944,#64945,#64946,#64947,#64948,#64949,
#64950,#64951,#64952,#64953,#64954,#64955,#64956,#64957,#64958,#64959,#64960,
#64961,#64962,#64963,#64964,#64965),.UNSPECIFIED.,.F.,.F.,(4,3,3,3,3,3,
3,3,3,3,3,3,3,3,4),(126.773751354503,126.877434685641,127.374993253036,
127.872551820431,128.370110387825,128.86766895522,129.365227522615,129.862786090009,
130.360344657404,130.857903224799,131.355461792193,131.853020359588,132.350578926983,
132.848137494377,133.056936661683),.UNSPECIFIED.);
#726=B_SPLINE_CURVE_WITH_KNOTS('',3,(#64970,#64971,#64972,#64973,#64974,
#64975,#64976,#64977,#64978,#64979,#64980,#64981,#64982,#64983,#64984,#64985,
#64986,#64987,#64988,#64989,#64990,#64991,#64992,#64993,#64994,#64995,#64996,
#64997,#64998,#64999,#65000,#65001,#65002,#65003,#65004,#65005,#65006,#65007,
#65008,#65009),.UNSPECIFIED.,.F.,.F.,(4,3,3,3,3,3,3,3,3,3,3,3,3,4),(-142.274941494929,
-141.804191707481,-141.306633140087,-140.809074572692,-140.311516005297,
-139.813957437903,-139.316398870508,-138.818840303113,-138.321281735719,
-137.823723168324,-137.326164600929,-136.828606033535,-136.33104746614,
-135.99175618775),.UNSPECIFIED.);
#727=B_SPLINE_CURVE_WITH_KNOTS('',3,(#65010,#65011,#65012,#65013,#65014,
#65015,#65016,#65017,#65018,#65019,#65020,#65021,#65022,#65023,#65024,#65025,
#65026,#65027,#65028,#65029,#65030,#65031,#65032,#65033,#65034,#65035,#65036,
#65037,#65038,#65039,#65040,#65041,#65042,#65043,#65044,#65045,#65046,#65047,
#65048,#65049,#65050,#65051,#65052),.UNSPECIFIED.,.F.,.F.,(4,3,3,3,3,3,
3,3,3,3,3,3,3,3,4),(133.056936661683,133.345696061772,133.843254629167,
134.340813196561,134.838371763956,135.335930331351,135.833488898745,136.33104746614,
136.828606033535,137.326164600929,137.823723168324,138.321281735719,138.818840303113,
139.316398870508,139.340121968862),.UNSPECIFIED.);
#728=B_SPLINE_CURVE_WITH_KNOTS('',3,(#65057,#65058,#65059,#65060,#65061,
#65062,#65063,#65064,#65065,#65066,#65067,#65068,#65069,#65070,#65071,#65072,
#65073,#65074,#65075,#65076,#65077,#65078,#65079,#65080,#65081,#65082,#65083,
#65084,#65085,#65086,#65087,#65088,#65089,#65090,#65091,#65092,#65093,#65094,
#65095,#65096,#65097,#65098,#65099),.UNSPECIFIED.,.F.,.F.,(4,3,3,3,3,3,
3,3,3,3,3,3,3,3,4),(-148.558126802109,-148.272453083612,-147.774894516218,
-147.277335948823,-146.779777381428,-146.282218814033,-145.784660246639,
-145.287101679244,-144.789543111849,-144.291984544455,-143.79442597706,
-143.296867409665,-142.799308842271,-142.301750274876,-142.274941494929),
 .UNSPECIFIED.);
#729=B_SPLINE_CURVE_WITH_KNOTS('',3,(#65100,#65101,#65102,#65103,#65104,
#65105,#65106,#65107,#65108,#65109,#65110,#65111,#65112,#65113,#65114,#65115,
#65116,#65117,#65118,#65119,#65120,#65121,#65122,#65123,#65124,#65125,#65126,
#65127,#65128,#65129,#65130,#65131,#65132,#65133,#65134,#65135,#65136,#65137,
#65138,#65139),.UNSPECIFIED.,.F.,.F.,(4,3,3,3,3,3,3,3,3,3,3,3,3,4),(139.340121968862,
139.813957437903,140.311516005297,140.809074572692,141.306633140087,141.804191707481,
142.301750274876,142.799308842271,143.296867409665,143.79442597706,144.291984544455,
144.789543111849,145.287101679244,145.623307276042),.UNSPECIFIED.);
#730=B_SPLINE_CURVE_WITH_KNOTS('',3,(#65144,#65145,#65146,#65147,#65148,
#65149,#65150,#65151,#65152,#65153,#65154,#65155,#65156,#65157,#65158,#65159,
#65160,#65161,#65162,#65163,#65164,#65165,#65166,#65167,#65168,#65169,#65170,
#65171,#65172,#65173,#65174,#65175,#65176,#65177,#65178,#65179,#65180,#65181,
#65182,#65183,#65184,#65185,#65186),.UNSPECIFIED.,.F.,.F.,(4,3,3,3,3,3,
3,3,3,3,3,3,3,3,4),(-154.841312109289,-154.740714459743,-154.243155892348,
-153.745597324954,-153.248038757559,-152.750480190164,-152.25292162277,
-151.755363055375,-151.25780448798,-150.760245920586,-150.262687353191,
-149.765128785796,-149.267570218402,-148.770011651007,-148.558126802109),
 .UNSPECIFIED.);
#731=B_SPLINE_CURVE_WITH_KNOTS('',3,(#65187,#65188,#65189,#65190,#65191,
#65192,#65193,#65194,#65195,#65196,#65197,#65198,#65199,#65200,#65201,#65202,
#65203,#65204,#65205,#65206,#65207,#65208,#65209,#65210,#65211,#65212,#65213,
#65214,#65215,#65216,#65217,#65218,#65219,#65220,#65221,#65222,#65223,#65224,
#65225,#65226,#65227,#65228,#65229),.UNSPECIFIED.,.F.,.F.,(4,3,3,3,3,3,
3,3,3,3,3,3,3,3,4),(145.623307276042,145.784660246639,146.282218814034,
146.779777381428,147.277335948823,147.774894516218,148.272453083612,148.770011651007,
149.267570218402,149.765128785796,150.262687353191,150.760245920586,151.25780448798,
151.755363055375,151.906492583222),.UNSPECIFIED.);
#732=B_SPLINE_CURVE_WITH_KNOTS('',3,(#65234,#65235,#65236,#65237,#65238,
#65239,#65240,#65241,#65242,#65243,#65244,#65245,#65246,#65247,#65248,#65249,
#65250,#65251,#65252,#65253,#65254,#65255,#65256,#65257,#65258,#65259,#65260,
#65261,#65262,#65263,#65264,#65265,#65266,#65267,#65268,#65269,#65270,#65271,
#65272,#65273),.UNSPECIFIED.,.F.,.F.,(4,3,3,3,3,3,3,3,3,3,3,3,3,4),(-161.124497416468,
-160.711417268479,-160.213858701084,-159.71630013369,-159.218741566295,
-158.7211829989,-158.223624431506,-157.726065864111,-157.228507296716,-156.730948729322,
-156.233390161927,-155.735831594532,-155.238273027138,-154.841312109289),
 .UNSPECIFIED.);
#733=B_SPLINE_CURVE_WITH_KNOTS('',3,(#65274,#65275,#65276,#65277,#65278,
#65279,#65280,#65281,#65282,#65283,#65284,#65285,#65286,#65287,#65288,#65289,
#65290,#65291,#65292,#65293,#65294,#65295,#65296,#65297,#65298,#65299,#65300,
#65301,#65302,#65303,#65304,#65305,#65306,#65307,#65308,#65309,#65310,#65311,
#65312,#65313),.UNSPECIFIED.,.F.,.F.,(4,3,3,3,3,3,3,3,3,3,3,3,3,4),(151.906492583222,
152.25292162277,152.750480190164,153.248038757559,153.745597324954,154.243155892348,
154.740714459743,155.238273027138,155.735831594532,156.233390161927,156.730948729322,
157.228507296716,157.726065864111,158.189677890401),.UNSPECIFIED.);
#734=B_SPLINE_CURVE_WITH_KNOTS('',3,(#65318,#65319,#65320,#65321,#65322,
#65323,#65324,#65325,#65326,#65327,#65328,#65329,#65330,#65331,#65332,#65333,
#65334,#65335,#65336,#65337,#65338,#65339,#65340,#65341,#65342,#65343,#65344,
#65345,#65346,#65347,#65348,#65349,#65350,#65351,#65352,#65353,#65354,#65355,
#65356,#65357,#65358,#65359,#65360),.UNSPECIFIED.,.F.,.F.,(4,3,3,3,3,3,
3,3,3,3,3,3,3,3,4),(-167.407682723648,-167.17967864461,-166.682120077215,
-166.18456150982,-165.687002942426,-165.189444375031,-164.691885807636,
-164.194327240242,-163.696768672847,-163.199210105452,-162.701651538058,
-162.204092970663,-161.706534403268,-161.208975835874,-161.124497416468),
 .UNSPECIFIED.);
#735=B_SPLINE_CURVE_WITH_KNOTS('',3,(#65361,#65362,#65363,#65364,#65365,
#65366,#65367,#65368,#65369,#65370,#65371,#65372,#65373,#65374,#65375,#65376,
#65377,#65378,#65379,#65380,#65381,#65382,#65383,#65384,#65385,#65386,#65387,
#65388,#65389,#65390,#65391,#65392,#65393,#65394,#65395,#65396,#65397,#65398,
#65399,#65400,#65401,#65402,#65403),.UNSPECIFIED.,.F.,.F.,(4,3,3,3,3,3,
3,3,3,3,3,3,3,3,4),(158.189677890401,158.223624431506,158.7211829989,159.218741566295,
159.71630013369,160.213858701084,160.711417268479,161.208975835874,161.706534403268,
162.204092970663,162.701651538058,163.199210105452,163.696768672847,164.194327240242,
164.472863197581),.UNSPECIFIED.);
#736=B_SPLINE_CURVE_WITH_KNOTS('',3,(#65408,#65409,#65410,#65411,#65412,
#65413,#65414,#65415,#65416,#65417,#65418,#65419,#65420,#65421,#65422,#65423,
#65424,#65425,#65426,#65427,#65428,#65429,#65430,#65431,#65432,#65433,#65434,
#65435,#65436,#65437,#65438,#65439,#65440,#65441,#65442,#65443,#65444,#65445,
#65446,#65447,#65448,#65449,#65450),.UNSPECIFIED.,.F.,.F.,(4,3,3,3,3,3,
3,3,3,3,3,3,3,3,4),(-173.690868030827,-173.64794002074,-173.150381453346,
-172.652822885951,-172.155264318556,-171.657705751162,-171.160147183767,
-170.662588616372,-170.165030048978,-169.667471481583,-169.169912914188,
-168.672354346794,-168.174795779399,-167.677237212004,-167.407682723648),
 .UNSPECIFIED.);
#737=B_SPLINE_CURVE_WITH_KNOTS('',3,(#65451,#65452,#65453,#65454,#65455,
#65456,#65457,#65458,#65459,#65460,#65461,#65462,#65463,#65464,#65465,#65466,
#65467,#65468,#65469,#65470,#65471,#65472,#65473,#65474,#65475,#65476,#65477,
#65478,#65479,#65480,#65481,#65482,#65483,#65484,#65485,#65486,#65487,#65488,
#65489,#65490,#65491,#65492,#65493),.UNSPECIFIED.,.F.,.F.,(4,3,3,3,3,3,
3,3,3,3,3,3,3,3,4),(164.472863197581,164.691885807636,165.189444375031,
165.687002942426,166.18456150982,166.682120077215,167.17967864461,167.677237212004,
168.174795779399,168.672354346794,169.169912914188,169.667471481583,170.165030048978,
170.662588616372,170.75604850476),.UNSPECIFIED.);
#738=B_SPLINE_CURVE_WITH_KNOTS('',3,(#65498,#65499,#65500,#65501,#65502,
#65503,#65504,#65505,#65506,#65507,#65508,#65509,#65510,#65511,#65512,#65513,
#65514,#65515,#65516,#65517,#65518,#65519,#65520,#65521,#65522,#65523,#65524,
#65525,#65526,#65527,#65528,#65529,#65530,#65531,#65532,#65533,#65534,#65535,
#65536,#65537),.UNSPECIFIED.,.F.,.F.,(4,3,3,3,3,3,3,3,3,3,3,3,3,4),(-179.974053338007,
-179.618642829476,-179.121084262082,-178.623525694687,-178.125967127293,
-177.628408559898,-177.130849992503,-176.633291425108,-176.135732857714,
-175.638174290319,-175.140615722924,-174.64305715553,-174.145498588135,
-173.690868030827),.UNSPECIFIED.);
#739=B_SPLINE_CURVE_WITH_KNOTS('',3,(#65538,#65539,#65540,#65541,#65542,
#65543,#65544,#65545,#65546,#65547,#65548,#65549,#65550,#65551,#65552,#65553,
#65554,#65555,#65556,#65557,#65558,#65559,#65560,#65561,#65562,#65563,#65564,
#65565,#65566,#65567,#65568,#65569,#65570,#65571,#65572,#65573,#65574,#65575,
#65576,#65577),.UNSPECIFIED.,.F.,.F.,(4,3,3,3,3,3,3,3,3,3,3,3,3,4),(170.75604850476,
171.160147183767,171.657705751162,172.155264318556,172.652822885951,173.150381453346,
173.64794002074,174.145498588135,174.64305715553,175.140615722925,175.638174290319,
176.135732857714,176.633291425109,177.03923381194),.UNSPECIFIED.);
#740=B_SPLINE_CURVE_WITH_KNOTS('',3,(#65583,#65584,#65585,#65586),
 .UNSPECIFIED.,.F.,.F.,(4,4),(191.637151868977,191.75621690312),
 .UNSPECIFIED.);
#741=B_SPLINE_CURVE_WITH_KNOTS('',3,(#65592,#65593,#65594,#65595,#65596,
#65597,#65598,#65599,#65600,#65601,#65602,#65603,#65604,#65605,#65606,#65607),
 .UNSPECIFIED.,.F.,.F.,(4,1,1,1,1,1,1,1,1,1,1,1,1,4),(185.353966561798,
185.808597119106,186.3061556865,186.803714253895,187.30127282129,187.798831388684,
188.296389956079,188.793948523474,189.291507090868,189.789065658263,190.286624225658,
190.784182793052,191.281741360447,191.637151868977),.UNSPECIFIED.);
#742=B_SPLINE_CURVE_WITH_KNOTS('',3,(#65610,#65611,#65612,#65613,#65614,
#65615,#65616,#65617,#65618,#65619,#65620,#65621,#65622,#65623),
 .UNSPECIFIED.,.F.,.F.,(4,1,1,1,1,1,1,1,1,1,1,4),(185.353966561798,185.445582742361,
185.943141309756,186.440699877151,186.938258444545,187.43581701194,187.933375579335,
188.430934146729,188.928492714124,189.426051281519,189.923609848913,190.421168416308),
 .UNSPECIFIED.);
#743=B_SPLINE_CURVE_WITH_KNOTS('',3,(#65628,#65629,#65630,#65631,#65632,
#65633,#65634,#65635,#65636,#65637,#65638,#65639,#65640,#65641,#65642,#65643,
#65644),.UNSPECIFIED.,.F.,.F.,(4,1,1,1,1,1,1,1,1,1,1,1,1,1,4),(179.070781254618,
179.340335742975,179.83789431037,180.335452877764,180.833011445159,181.330570012554,
181.828128579948,182.325687147343,182.823245714738,183.320804282132,183.818362849527,
184.315921416922,184.813479984316,185.311038551711,185.353966561798),
 .UNSPECIFIED.);
#744=B_SPLINE_CURVE_WITH_KNOTS('',3,(#65645,#65646,#65647,#65648,#65649,
#65650,#65651,#65652,#65653,#65654,#65655,#65656,#65657,#65658,#65659,#65660),
 .UNSPECIFIED.,.F.,.F.,(4,1,1,1,1,1,1,1,1,1,1,1,1,4),(179.070781254618,
179.474879933625,179.97243850102,180.469997068415,180.967555635809,181.465114203204,
181.962672770599,182.460231337993,182.957789905388,183.455348472783,183.952907040177,
184.450465607572,184.948024174967,185.353966561798),.UNSPECIFIED.);
#745=B_SPLINE_CURVE_WITH_KNOTS('',3,(#65665,#65666,#65667,#65668,#65669,
#65670,#65671,#65672,#65673,#65674,#65675,#65676,#65677,#65678,#65679,#65680,
#65681),.UNSPECIFIED.,.F.,.F.,(4,1,1,1,1,1,1,1,1,1,1,1,1,1,4),(172.787595947439,
172.872074366844,173.369632934239,173.867191501634,174.364750069028,174.862308636423,
175.359867203818,175.857425771212,176.354984338607,176.852542906002,177.350101473396,
177.847660040791,178.345218608186,178.84277717558,179.070781254618),
 .UNSPECIFIED.);
#746=B_SPLINE_CURVE_WITH_KNOTS('',3,(#65682,#65683,#65684,#65685,#65686,
#65687,#65688,#65689,#65690,#65691,#65692,#65693,#65694,#65695,#65696,#65697,
#65698),.UNSPECIFIED.,.F.,.F.,(4,1,1,1,1,1,1,1,1,1,1,1,1,1,4),(172.787595947439,
173.006618557495,173.504177124889,174.001735692284,174.499294259679,174.996852827073,
175.494411394468,175.991969961863,176.489528529257,176.987087096652,177.484645664047,
177.982204231441,178.479762798836,178.977321366231,179.070781254618),
 .UNSPECIFIED.);
#747=B_SPLINE_CURVE_WITH_KNOTS('',3,(#65703,#65704,#65705,#65706,#65707,
#65708,#65709,#65710,#65711,#65712,#65713,#65714,#65715,#65716,#65717,#65718),
 .UNSPECIFIED.,.F.,.F.,(4,1,1,1,1,1,1,1,1,1,1,1,1,4),(166.504410640259,
166.901371558108,167.398930125503,167.896488692898,168.394047260292,168.891605827687,
169.389164395082,169.886722962476,170.384281529871,170.881840097266,171.37939866466,
171.876957232055,172.37451579945,172.787595947439),.UNSPECIFIED.);
#748=B_SPLINE_CURVE_WITH_KNOTS('',3,(#65719,#65720,#65721,#65722,#65723,
#65724,#65725,#65726,#65727,#65728,#65729,#65730,#65731,#65732,#65733,#65734,
#65735),.UNSPECIFIED.,.F.,.F.,(4,1,1,1,1,1,1,1,1,1,1,1,1,1,4),(166.504410640259,
166.538357181364,167.035915748758,167.533474316153,168.031032883548,168.528591450942,
169.026150018337,169.523708585732,170.021267153126,170.518825720521,171.016384287916,
171.51394285531,172.011501422705,172.5090599901,172.787595947439),
 .UNSPECIFIED.);
#749=B_SPLINE_CURVE_WITH_KNOTS('',3,(#65740,#65741,#65742,#65743,#65744,
#65745,#65746,#65747,#65748,#65749,#65750,#65751,#65752,#65753,#65754,#65755,
#65756),.UNSPECIFIED.,.F.,.F.,(4,1,1,1,1,1,1,1,1,1,1,1,1,1,4),(160.22122533308,
160.433110181977,160.930668749372,161.428227316767,161.925785884161,162.423344451556,
162.920903018951,163.418461586346,163.91602015374,164.413578721135,164.91113728853,
165.408695855924,165.906254423319,166.403812990714,166.504410640259),
 .UNSPECIFIED.);
#750=B_SPLINE_CURVE_WITH_KNOTS('',3,(#65757,#65758,#65759,#65760,#65761,
#65762,#65763,#65764,#65765,#65766,#65767,#65768,#65769,#65770,#65771,#65772),
 .UNSPECIFIED.,.F.,.F.,(4,1,1,1,1,1,1,1,1,1,1,1,1,4),(160.22122533308,160.567654372628,
161.065212940022,161.562771507417,162.060330074812,162.557888642206,163.055447209601,
163.553005776996,164.05056434439,164.548122911785,165.04568147918,165.543240046574,
166.040798613969,166.504410640259),.UNSPECIFIED.);
#751=B_SPLINE_CURVE_WITH_KNOTS('',3,(#65777,#65778,#65779,#65780,#65781,
#65782,#65783,#65784,#65785,#65786,#65787,#65788,#65789,#65790,#65791,#65792,
#65793),.UNSPECIFIED.,.F.,.F.,(4,1,1,1,1,1,1,1,1,1,1,1,1,1,4),(153.9380400259,
153.964848805847,154.462407373241,154.959965940636,155.457524508031,155.955083075425,
156.45264164282,156.950200210215,157.447758777609,157.945317345004,158.442875912399,
158.940434479793,159.437993047188,159.935551614583,160.22122533308),
 .UNSPECIFIED.);
#752=B_SPLINE_CURVE_WITH_KNOTS('',3,(#65794,#65795,#65796,#65797,#65798,
#65799,#65800,#65801,#65802,#65803,#65804,#65805,#65806,#65807,#65808,#65809,
#65810),.UNSPECIFIED.,.F.,.F.,(4,1,1,1,1,1,1,1,1,1,1,1,1,1,4),(153.9380400259,
154.099392996497,154.596951563892,155.094510131286,155.592068698681,156.089627266076,
156.58718583347,157.084744400865,157.58230296826,158.079861535654,158.577420103049,
159.074978670444,159.572537237838,160.070095805233,160.22122533308),
 .UNSPECIFIED.);
#753=B_SPLINE_CURVE_WITH_KNOTS('',3,(#65815,#65816,#65817,#65818,#65819,
#65820,#65821,#65822,#65823,#65824,#65825,#65826,#65827,#65828,#65829,#65830),
 .UNSPECIFIED.,.F.,.F.,(4,1,1,1,1,1,1,1,1,1,1,1,1,4),(147.65485471872,147.994145997111,
148.491704564505,148.9892631319,149.486821699295,149.984380266689,150.481938834084,
150.979497401479,151.477055968873,151.974614536268,152.472173103663,152.969731671057,
153.467290238452,153.9380400259),.UNSPECIFIED.);
#754=B_SPLINE_CURVE_WITH_KNOTS('',3,(#65831,#65832,#65833,#65834,#65835,
#65836,#65837,#65838,#65839,#65840,#65841,#65842,#65843,#65844,#65845,#65846),
 .UNSPECIFIED.,.F.,.F.,(4,1,1,1,1,1,1,1,1,1,1,1,1,4),(147.65485471872,148.128690187761,
148.626248755156,149.12380732255,149.621365889945,150.11892445734,150.616483024734,
151.114041592129,151.611600159524,152.109158726918,152.606717294313,153.104275861708,
153.601834429102,153.9380400259),.UNSPECIFIED.);
#755=B_SPLINE_CURVE_WITH_KNOTS('',3,(#65851,#65852,#65853,#65854,#65855,
#65856,#65857,#65858,#65859,#65860,#65861,#65862,#65863,#65864,#65865,#65866,
#65867),.UNSPECIFIED.,.F.,.F.,(4,1,1,1,1,1,1,1,1,1,1,1,1,1,4),(141.371669411541,
141.52588462098,142.023443188375,142.521001755769,143.018560323164,143.516118890559,
144.013677457953,144.511236025348,145.008794592743,145.506353160137,146.003911727532,
146.501470294927,146.999028862321,147.496587429716,147.65485471872),
 .UNSPECIFIED.);
#756=B_SPLINE_CURVE_WITH_KNOTS('',3,(#65868,#65869,#65870,#65871,#65872,
#65873,#65874,#65875,#65876,#65877,#65878,#65879,#65880,#65881,#65882,#65883,
#65884),.UNSPECIFIED.,.F.,.F.,(4,1,1,1,1,1,1,1,1,1,1,1,1,1,4),(141.371669411541,
141.66042881163,142.157987379025,142.65554594642,143.153104513814,143.650663081209,
144.148221648604,144.645780215998,145.143338783393,145.640897350788,146.138455918182,
146.636014485577,147.133573052972,147.631131620366,147.65485471872),
 .UNSPECIFIED.);
#757=B_SPLINE_CURVE_WITH_KNOTS('',3,(#65889,#65890,#65891,#65892,#65893,
#65894,#65895,#65896,#65897,#65898,#65899,#65900,#65901,#65902,#65903,#65904),
 .UNSPECIFIED.,.F.,.F.,(4,1,1,1,1,1,1,1,1,1,1,1,1,4),(135.088484104361,
135.555181812244,136.052740379639,136.550298947033,137.047857514428,137.545416081823,
138.042974649217,138.540533216612,139.038091784007,139.535650351401,140.033208918796,
140.530767486191,141.028326053585,141.371669411541),.UNSPECIFIED.);
#758=B_SPLINE_CURVE_WITH_KNOTS('',3,(#65905,#65906,#65907,#65908,#65909,
#65910,#65911,#65912,#65913,#65914,#65915,#65916,#65917,#65918,#65919,#65920,
#65921),.UNSPECIFIED.,.F.,.F.,(4,1,1,1,1,1,1,1,1,1,1,1,1,1,4),(135.088484104361,
135.192167435499,135.689726002894,136.187284570289,136.684843137683,137.182401705078,
137.679960272473,138.177518839867,138.675077407262,139.172635974657,139.670194542051,
140.167753109446,140.665311676841,141.162870244235,141.371669411541),
 .UNSPECIFIED.);
#759=B_SPLINE_CURVE_WITH_KNOTS('',3,(#65926,#65927,#65928,#65929,#65930,
#65931,#65932,#65933,#65934,#65935,#65936,#65937,#65938,#65939,#65940,#65941,
#65942),.UNSPECIFIED.,.F.,.F.,(4,1,1,1,1,1,1,1,1,1,1,1,1,1,4),(128.805298797182,
129.086920436113,129.584479003508,130.082037570902,130.579596138297,131.077154705692,
131.574713273087,132.072271840481,132.569830407876,133.067388975271,133.564947542665,
134.06250611006,134.560064677455,135.057623244849,135.088484104361),
 .UNSPECIFIED.);
#760=B_SPLINE_CURVE_WITH_KNOTS('',3,(#65943,#65944,#65945,#65946,#65947,
#65948,#65949,#65950,#65951,#65952,#65953,#65954,#65955,#65956,#65957,#65958),
 .UNSPECIFIED.,.F.,.F.,(4,1,1,1,1,1,1,1,1,1,1,1,1,4),(128.805298797182,
129.221464626763,129.719023194158,130.216581761553,130.714140328947,131.211698896342,
131.709257463737,132.206816031131,132.704374598526,133.201933165921,133.699491733315,
134.19705030071,134.694608868105,135.088484104361),.UNSPECIFIED.);
#761=B_SPLINE_CURVE_WITH_KNOTS('',3,(#65963,#65964,#65965,#65966,#65967,
#65968,#65969,#65970,#65971,#65972,#65973,#65974,#65975,#65976,#65977,#65978,
#65979),.UNSPECIFIED.,.F.,.F.,(4,1,1,1,1,1,1,1,1,1,1,1,1,1,4),(122.522113490002,
122.618659059982,123.116217627377,123.613776194772,124.111334762166,124.608893329561,
125.106451896956,125.60401046435,126.101569031745,126.59912759914,127.096686166534,
127.594244733929,128.091803301324,128.589361868718,128.805298797182),
 .UNSPECIFIED.);
#762=B_SPLINE_CURVE_WITH_KNOTS('',3,(#65980,#65981,#65982,#65983,#65984,
#65985,#65986,#65987,#65988,#65989,#65990,#65991,#65992,#65993,#65994,#65995,
#65996),.UNSPECIFIED.,.F.,.F.,(4,1,1,1,1,1,1,1,1,1,1,1,1,1,4),(122.522113490002,
122.753203250633,123.250761818027,123.748320385422,124.245878952817,124.743437520211,
125.240996087606,125.738554655001,126.236113222395,126.73367178979,127.231230357185,
127.728788924579,128.226347491974,128.723906059369,128.805298797182),
 .UNSPECIFIED.);
#763=B_SPLINE_CURVE_WITH_KNOTS('',3,(#66001,#66002,#66003,#66004,#66005,
#66006,#66007,#66008,#66009,#66010,#66011,#66012,#66013,#66014,#66015,#66016),
 .UNSPECIFIED.,.F.,.F.,(4,1,1,1,1,1,1,1,1,1,1,1,1,4),(116.238928182823,
116.647956251246,117.145514818641,117.643073386036,118.14063195343,118.638190520825,
119.13574908822,119.633307655614,120.130866223009,120.628424790404,121.125983357798,
121.623541925193,122.121100492588,122.522113490002),.UNSPECIFIED.);
#764=B_SPLINE_CURVE_WITH_KNOTS('',3,(#66017,#66018,#66019,#66020,#66021,
#66022,#66023,#66024,#66025,#66026,#66027,#66028,#66029,#66030,#66031,#66032,
#66033),.UNSPECIFIED.,.F.,.F.,(4,1,1,1,1,1,1,1,1,1,1,1,1,1,4),(116.238928182823,
116.284941874502,116.782500441897,117.280059009291,117.777617576686,118.275176144081,
118.772734711475,119.27029327887,119.767851846265,120.265410413659,120.762968981054,
121.260527548449,121.758086115843,122.255644683238,122.522113490002),
 .UNSPECIFIED.);
#765=B_SPLINE_CURVE_WITH_KNOTS('',3,(#66038,#66039,#66040,#66041,#66042,
#66043,#66044,#66045,#66046,#66047,#66048,#66049,#66050,#66051,#66052,#66053,
#66054),.UNSPECIFIED.,.F.,.F.,(4,1,1,1,1,1,1,1,1,1,1,1,1,1,4),(109.955742875643,
110.179694875116,110.67725344251,111.174812009905,111.6723705773,112.169929144694,
112.667487712089,113.165046279484,113.662604846878,114.160163414273,114.657721981668,
115.155280549062,115.652839116457,116.150397683852,116.238928182823),
 .UNSPECIFIED.);
#766=B_SPLINE_CURVE_WITH_KNOTS('',3,(#66055,#66056,#66057,#66058,#66059,
#66060,#66061,#66062,#66063,#66064,#66065,#66066,#66067,#66068,#66069,#66070),
 .UNSPECIFIED.,.F.,.F.,(4,1,1,1,1,1,1,1,1,1,1,1,1,4),(109.955742875643,
110.314239065766,110.811797633161,111.309356200555,111.80691476795,112.304473335345,
112.802031902739,113.299590470134,113.797149037529,114.294707604923,114.792266172318,
115.289824739713,115.787383307107,116.238928182823),.UNSPECIFIED.);
#767=B_SPLINE_CURVE_WITH_KNOTS('',3,(#66075,#66076,#66077,#66078,#66079,
#66080,#66081,#66082,#66083,#66084,#66085,#66086,#66087,#66088,#66089,#66090,
#66091),.UNSPECIFIED.,.F.,.F.,(4,1,1,1,1,1,1,1,1,1,1,1,1,1,4),(103.672557568463,
103.711433498985,104.20899206638,104.706550633774,105.204109201169,105.701667768564,
106.199226335958,106.696784903353,107.194343470748,107.691902038142,108.189460605537,
108.687019172932,109.184577740326,109.682136307721,109.955742875643),
 .UNSPECIFIED.);
#768=B_SPLINE_CURVE_WITH_KNOTS('',3,(#66092,#66093,#66094,#66095,#66096,
#66097,#66098,#66099,#66100,#66101,#66102,#66103,#66104,#66105,#66106,#66107,
#66108),.UNSPECIFIED.,.F.,.F.,(4,1,1,1,1,1,1,1,1,1,1,1,1,1,4),(103.672557568463,
103.845977689635,104.34353625703,104.841094824424,105.338653391819,105.836211959214,
106.333770526608,106.831329094003,107.328887661398,107.826446228792,108.324004796187,
108.821563363582,109.319121930977,109.816680498371,109.955742875643),
 .UNSPECIFIED.);
#769=B_SPLINE_CURVE_WITH_KNOTS('',3,(#66113,#66114,#66115,#66116,#66117,
#66118,#66119,#66120,#66121,#66122,#66123,#66124,#66125,#66126,#66127,#66128),
 .UNSPECIFIED.,.F.,.F.,(4,1,1,1,1,1,1,1,1,1,1,1,1,4),(97.3893722612838,
97.7407306902488,98.2382892576435,98.7358478250382,99.2334063924328,99.7309649598275,
100.228523527222,100.726082094617,101.223640662012,101.721199229406,102.218757796801,
102.716316364196,103.21387493159,103.672557568463),.UNSPECIFIED.);
#770=B_SPLINE_CURVE_WITH_KNOTS('',3,(#66129,#66130,#66131,#66132,#66133,
#66134,#66135,#66136,#66137,#66138,#66139,#66140,#66141,#66142,#66143,#66144),
 .UNSPECIFIED.,.F.,.F.,(4,1,1,1,1,1,1,1,1,1,1,1,1,4),(97.3893722612838,
97.875274880899,98.3728334482937,98.8703920156884,99.3679505830831,99.8655091504777,
100.363067717872,100.860626285267,101.358184852662,101.855743420056,102.353301987451,
102.850860554846,103.34841912224,103.672557568463),.UNSPECIFIED.);
#771=B_SPLINE_CURVE_WITH_KNOTS('',3,(#66149,#66150,#66151,#66152,#66153,
#66154,#66155,#66156,#66157,#66158,#66159,#66160,#66161,#66162,#66163,#66164,
#66165),.UNSPECIFIED.,.F.,.F.,(4,1,1,1,1,1,1,1,1,1,1,1,1,1,4),(91.1061869541042,
91.2724693141181,91.7700278815128,92.2675864489074,92.7651450163021,93.2627035836968,
93.7602621510915,94.2578207184861,94.7553792858808,95.2529378532755,95.7504964206701,
96.2480549880648,96.7456135554595,97.2431721228542,97.3893722612838),
 .UNSPECIFIED.);
#772=B_SPLINE_CURVE_WITH_KNOTS('',3,(#66166,#66167,#66168,#66169,#66170,
#66171,#66172,#66173,#66174,#66175,#66176,#66177,#66178,#66179,#66180,#66181,
#66182),.UNSPECIFIED.,.F.,.F.,(4,1,1,1,1,1,1,1,1,1,1,1,1,1,4),(91.1061869541041,
91.4070135047683,91.904572072163,92.4021306395577,92.8996892069523,93.397247774347,
93.8948063417417,94.3923649091363,94.889923476531,95.3874820439257,95.8850406113204,
96.382599178715,96.8801577461097,97.3777163135044,97.3893722612838),
 .UNSPECIFIED.);
#773=B_SPLINE_CURVE_WITH_KNOTS('',3,(#66187,#66188,#66189,#66190,#66191,
#66192,#66193,#66194,#66195,#66196,#66197,#66198,#66199,#66200,#66201,#66202),
 .UNSPECIFIED.,.F.,.F.,(4,1,1,1,1,1,1,1,1,1,1,1,1,4),(84.8230016469246,
85.301766505382,85.7993250727767,86.2968836401714,86.794442207566,87.2920007749607,
87.7895593423554,88.2871179097501,88.7846764771447,89.2822350445394,89.7797936119341,
90.2773521793287,90.7749107467234,91.1061869541042),.UNSPECIFIED.);
#774=B_SPLINE_CURVE_WITH_KNOTS('',3,(#66203,#66204,#66205,#66206,#66207,
#66208,#66209,#66210,#66211,#66212,#66213,#66214,#66215,#66216,#66217,#66218,
#66219),.UNSPECIFIED.,.F.,.F.,(4,1,1,1,1,1,1,1,1,1,1,1,1,1,4),(84.8230016469245,
84.9387521286376,85.4363106960323,85.9338692634269,86.4314278308216,86.9289863982163,
87.4265449656109,87.9241035330056,88.4216621004003,88.9192206677949,89.4167792351896,
89.9143378025843,90.411896369979,90.9094549373736,91.1061869541041),
 .UNSPECIFIED.);
#775=B_SPLINE_CURVE_WITH_KNOTS('',3,(#66224,#66225,#66226,#66227,#66228,
#66229,#66230,#66231,#66232,#66233,#66234,#66235,#66236,#66237,#66238,#66239,
#66240),.UNSPECIFIED.,.F.,.F.,(4,1,1,1,1,1,1,1,1,1,1,1,1,1,4),(78.539816339745,
78.8335051292513,79.331063696646,79.8286222640406,80.3261808314353,80.82373939883,
81.3212979662247,81.8188565336193,82.316415101014,82.8139736684087,83.3115322358033,
83.809090803198,84.3066493705927,84.8042079379874,84.8230016469246),
 .UNSPECIFIED.);
#776=B_SPLINE_CURVE_WITH_KNOTS('',3,(#66241,#66242,#66243,#66244,#66245,
#66246,#66247,#66248,#66249,#66250,#66251,#66252,#66253,#66254,#66255,#66256),
 .UNSPECIFIED.,.F.,.F.,(4,1,1,1,1,1,1,1,1,1,1,1,1,4),(78.539816339745,78.9680493199015,
79.4656078872962,79.9631664546908,80.4607250220855,80.9582835894802,81.4558421568749,
81.9534007242695,82.4509592916642,82.9485178590589,83.4460764264536,83.9436349938482,
84.4411935612429,84.8230016469245),.UNSPECIFIED.);
#777=B_SPLINE_CURVE_WITH_KNOTS('',3,(#66261,#66262,#66263,#66264,#66265,
#66266,#66267,#66268,#66269,#66270,#66271,#66272,#66273,#66274,#66275,#66276,
#66277),.UNSPECIFIED.,.F.,.F.,(4,1,1,1,1,1,1,1,1,1,1,1,1,1,4),(72.2566310325654,
72.3652437531206,72.8628023205152,73.3603608879099,73.8579194553046,74.3554780226992,
74.8530365900939,75.3505951574886,75.8481537248833,76.3457122922779,76.8432708596726,
77.3408294270673,77.838387994462,78.3359465618566,78.539816339745),
 .UNSPECIFIED.);
#778=B_SPLINE_CURVE_WITH_KNOTS('',3,(#66278,#66279,#66280,#66281,#66282,
#66283,#66284,#66285,#66286,#66287,#66288,#66289,#66290,#66291,#66292,#66293,
#66294),.UNSPECIFIED.,.F.,.F.,(4,1,1,1,1,1,1,1,1,1,1,1,1,1,4),(72.2566310325654,
72.4997879437708,72.9973465111654,73.4949050785601,73.9924636459548,74.4900222133495,
74.9875807807441,75.4851393481388,75.9826979155335,76.4802564829282,76.9778150503228,
77.4753736177175,77.9729321851122,78.4704907525068,78.539816339745),
 .UNSPECIFIED.);
#779=B_SPLINE_CURVE_WITH_KNOTS('',3,(#66299,#66300,#66301,#66302,#66303,
#66304,#66305,#66306,#66307,#66308,#66309,#66310,#66311,#66312,#66313,#66314),
 .UNSPECIFIED.,.F.,.F.,(4,1,1,1,1,1,1,1,1,1,1,1,1,4),(65.9734457253858,
66.3945409443845,66.8920995117792,67.3896580791738,67.8872166465685,68.3847752139632,
68.8823337813579,69.3798923487525,69.8774509161472,70.3750094835419,70.8725680509366,
71.3701266183312,71.8676851857259,72.2566310325654),.UNSPECIFIED.);
#780=B_SPLINE_CURVE_WITH_KNOTS('',3,(#66315,#66316,#66317,#66318,#66319,
#66320,#66321,#66322,#66323,#66324,#66325,#66326,#66327,#66328,#66329,#66330,
#66331),.UNSPECIFIED.,.F.,.F.,(4,1,1,1,1,1,1,1,1,1,1,1,1,1,4),(65.9734457253858,
66.03152656764,66.5290851350347,67.0266437024294,67.5242022698241,68.0217608372187,
68.5193194046134,69.0168779720081,69.5144365394028,70.0119951067974,70.5095536741921,
71.0071122415868,71.5046708089814,72.0022293763761,72.2566310325654),
 .UNSPECIFIED.);
#781=B_SPLINE_CURVE_WITH_KNOTS('',3,(#66336,#66337,#66338,#66339,#66340,
#66341,#66342,#66343,#66344,#66345,#66346,#66347,#66348,#66349,#66350,#66351,
#66352),.UNSPECIFIED.,.F.,.F.,(4,1,1,1,1,1,1,1,1,1,1,1,1,1,4),(59.6902604182062,
59.9262795682538,60.4238381356484,60.9213967030431,61.4189552704378,61.9165138378325,
62.4140724052271,62.9116309726218,63.4091895400165,63.9067481074111,64.4043066748058,
64.9018652422005,65.3994238095952,65.8969823769898,65.9734457253858),
 .UNSPECIFIED.);
#782=B_SPLINE_CURVE_WITH_KNOTS('',3,(#66353,#66354,#66355,#66356,#66357,
#66358,#66359,#66360,#66361,#66362,#66363,#66364,#66365,#66366,#66367,#66368),
 .UNSPECIFIED.,.F.,.F.,(4,1,1,1,1,1,1,1,1,1,1,1,1,4),(59.6902604182062,
60.060823758904,60.5583823262987,61.0559408936933,61.553499461088,62.0510580284827,
62.5486165958773,63.046175163272,63.5437337306667,64.0412922980614,64.538850865456,
65.0364094328507,65.5339680002454,65.9734457253858),.UNSPECIFIED.);
#783=B_SPLINE_CURVE_WITH_KNOTS('',3,(#66373,#66374,#66375,#66376,#66377,
#66378,#66379,#66380,#66381,#66382,#66383,#66384,#66385,#66386,#66387,#66388,
#66389),.UNSPECIFIED.,.F.,.F.,(4,1,1,1,1,1,1,1,1,1,1,1,1,1,4),(53.4070751110266,
53.458018192123,53.9555767595177,54.4531353269124,54.9506938943071,55.4482524617017,
55.9458110290964,56.4433695964911,56.9409281638857,57.4384867312804,57.9360452986751,
58.4336038660698,58.9311624334644,59.4287210008591,59.6902604182062),
 .UNSPECIFIED.);
#784=B_SPLINE_CURVE_WITH_KNOTS('',3,(#66390,#66391,#66392,#66393,#66394,
#66395,#66396,#66397,#66398,#66399,#66400,#66401,#66402,#66403,#66404,#66405,
#66406),.UNSPECIFIED.,.F.,.F.,(4,1,1,1,1,1,1,1,1,1,1,1,1,1,4),(53.4070751110266,
53.5925623827733,54.0901209501679,54.5876795175626,55.0852380849573,55.5827966523519,
56.0803552197466,56.5779137871413,57.075472354536,57.5730309219306,58.0705894893253,
58.56814805672,59.0657066241146,59.5632651915093,59.6902604182062),
 .UNSPECIFIED.);
#785=B_SPLINE_CURVE_WITH_KNOTS('',3,(#66411,#66412,#66413,#66414,#66415,
#66416,#66417,#66418,#66419,#66420,#66421,#66422,#66423,#66424,#66425,#66426),
 .UNSPECIFIED.,.F.,.F.,(4,1,1,1,1,1,1,1,1,1,1,1,1,4),(47.123889803847,47.487315383387,
47.9848739507816,48.4824325181763,48.979991085571,49.4775496529657,49.9751082203603,
50.472666787755,50.9702253551497,51.4677839225444,51.965342489939,52.4629010573337,
52.9604596247284,53.4070751110266),.UNSPECIFIED.);
#786=B_SPLINE_CURVE_WITH_KNOTS('',3,(#66427,#66428,#66429,#66430,#66431,
#66432,#66433,#66434,#66435,#66436,#66437,#66438,#66439,#66440,#66441,#66442,
#66443),.UNSPECIFIED.,.F.,.F.,(4,1,1,1,1,1,1,1,1,1,1,1,1,1,4),(47.123889803847,
47.1243010066425,47.6218595740372,48.1194181414319,48.6169767088265,49.1145352762212,
49.6120938436159,50.1096524110105,50.6072109784052,51.1047695457999,51.6023281131946,
52.0998866805892,52.5974452479839,53.0950038153786,53.4070751110266),
 .UNSPECIFIED.);
#787=B_SPLINE_CURVE_WITH_KNOTS('',3,(#66448,#66449,#66450,#66451,#66452,
#66453,#66454,#66455,#66456,#66457,#66458,#66459,#66460,#66461,#66462,#66463,
#66464),.UNSPECIFIED.,.F.,.F.,(4,1,1,1,1,1,1,1,1,1,1,1,1,1,4),(40.8407044966674,
41.0190540072562,41.5166125746509,42.0141711420456,42.5117297094403,43.0092882768349,
43.5068468442296,44.0044054116243,44.501963979019,44.9995225464136,45.4970811138083,
45.994639681203,46.4921982485976,46.9897568159923,47.123889803847),
 .UNSPECIFIED.);
#788=B_SPLINE_CURVE_WITH_KNOTS('',3,(#66465,#66466,#66467,#66468,#66469,
#66470,#66471,#66472,#66473,#66474,#66475,#66476,#66477,#66478,#66479,#66480),
 .UNSPECIFIED.,.F.,.F.,(4,1,1,1,1,1,1,1,1,1,1,1,1,4),(40.8407044966674,
41.1535981979065,41.6511567653011,42.1487153326958,42.6462739000905,43.1438324674851,
43.6413910348798,44.1389496022745,44.6365081696692,45.1340667370638,45.6316253044585,
46.1291838718532,46.6267424392478,47.123889803847),.UNSPECIFIED.);
#789=B_SPLINE_CURVE_WITH_KNOTS('',3,(#66485,#66486,#66487,#66488,#66489,
#66490,#66491,#66492,#66493,#66494,#66495,#66496,#66497,#66498,#66499,#66500),
 .UNSPECIFIED.,.F.,.F.,(4,1,1,1,1,1,1,1,1,1,1,1,1,4),(34.5575191894878,
35.0483511985202,35.5459097659149,36.0434683333095,36.5410269007042,37.0385854680989,
37.5361440354935,38.0337026028882,38.5312611702829,39.0288197376776,39.5263783050722,
40.0239368724669,40.5214954398616,40.8407044966674),.UNSPECIFIED.);
#790=B_SPLINE_CURVE_WITH_KNOTS('',3,(#66501,#66502,#66503,#66504,#66505,
#66506,#66507,#66508,#66509,#66510,#66511,#66512,#66513,#66514,#66515,#66516,
#66517),.UNSPECIFIED.,.F.,.F.,(4,1,1,1,1,1,1,1,1,1,1,1,1,1,4),(34.5575191894878,
34.6853368217757,35.1828953891704,35.6804539565651,36.1780125239597,36.6755710913544,
37.1731296587491,37.6706882261438,38.1682467935384,38.6658053609331,39.1633639283278,
39.6609224957224,40.1584810631171,40.6560396305118,40.8407044966674),
 .UNSPECIFIED.);
#791=B_SPLINE_CURVE_WITH_KNOTS('',3,(#66522,#66523,#66524,#66525,#66526,
#66527,#66528,#66529,#66530,#66531,#66532,#66533,#66534,#66535,#66536,#66537,
#66538),.UNSPECIFIED.,.F.,.F.,(4,1,1,1,1,1,1,1,1,1,1,1,1,1,4),(28.2743338823083,
28.5800898223895,29.0776483897841,29.5752069571788,30.0727655245735,30.5703240919681,
31.0678826593628,31.5654412267575,32.0629997941522,32.5605583615468,33.0581169289415,
33.5556754963362,34.0532340637308,34.5507926311255,34.5575191894878),
 .UNSPECIFIED.);
#792=B_SPLINE_CURVE_WITH_KNOTS('',3,(#66539,#66540,#66541,#66542,#66543,
#66544,#66545,#66546,#66547,#66548,#66549,#66550,#66551,#66552,#66553,#66554),
 .UNSPECIFIED.,.F.,.F.,(4,1,1,1,1,1,1,1,1,1,1,1,1,4),(28.2743338823082,
28.7146340130397,29.2121925804343,29.709751147829,30.2073097152237,30.7048682826183,
31.202426850013,31.6999854174077,32.1975439848024,32.695102552197,33.1926611195917,
33.6902196869864,34.187778254381,34.5575191894878),.UNSPECIFIED.);
#793=B_SPLINE_CURVE_WITH_KNOTS('',3,(#66559,#66560,#66561,#66562,#66563,
#66564,#66565,#66566,#66567,#66568,#66569,#66570,#66571,#66572,#66573,#66574,
#66575),.UNSPECIFIED.,.F.,.F.,(4,1,1,1,1,1,1,1,1,1,1,1,1,1,4),(21.9911485751287,
22.1118284462587,22.6093870136534,23.1069455810481,23.6045041484427,24.1020627158374,
24.5996212832321,25.0971798506268,25.5947384180214,26.0922969854161,26.5898555528108,
27.0874141202054,27.5849726876001,28.0825312549948,28.2743338823083),
 .UNSPECIFIED.);
#794=B_SPLINE_CURVE_WITH_KNOTS('',3,(#66576,#66577,#66578,#66579,#66580,
#66581,#66582,#66583,#66584,#66585,#66586,#66587,#66588,#66589,#66590,#66591,
#66592),.UNSPECIFIED.,.F.,.F.,(4,1,1,1,1,1,1,1,1,1,1,1,1,1,4),(21.9911485751286,
22.2463726369089,22.7439312043036,23.2414897716983,23.7390483390929,24.2366069064876,
24.7341654738823,25.231724041277,25.7292826086716,26.2268411760663,26.724399743461,
27.2219583108556,27.7195168782503,28.217075445645,28.2743338823082),
 .UNSPECIFIED.);
#795=B_SPLINE_CURVE_WITH_KNOTS('',3,(#66597,#66598,#66599,#66600,#66601,
#66602,#66603,#66604,#66605,#66606,#66607,#66608,#66609,#66610,#66611,#66612),
 .UNSPECIFIED.,.F.,.F.,(4,1,1,1,1,1,1,1,1,1,1,1,1,4),(15.7079632679491,
16.1411256375227,16.6386842049173,17.136242772312,17.6338013397067,18.1313599071013,
18.628918474496,19.1264770418907,19.6240356092854,20.12159417668,20.6191527440747,
21.1167113114694,21.6142698788641,21.9911485751287),.UNSPECIFIED.);
#796=B_SPLINE_CURVE_WITH_KNOTS('',3,(#66613,#66614,#66615,#66616,#66617,
#66618,#66619,#66620,#66621,#66622,#66623,#66624,#66625,#66626,#66627,#66628,
#66629),.UNSPECIFIED.,.F.,.F.,(4,1,1,1,1,1,1,1,1,1,1,1,1,1,4),(15.707963267949,
15.7781112607782,16.2756698281729,16.7732283955675,17.2707869629622,17.7683455303569,
18.2659040977515,18.7634626651462,19.2610212325409,19.7585797999356,20.2561383673302,
20.7536969347249,21.2512555021196,21.7488140695142,21.9911485751286),
 .UNSPECIFIED.);
#797=B_SPLINE_CURVE_WITH_KNOTS('',3,(#66716,#66717,#66718,#66719,#66720,
#66721,#66722,#66723,#66724,#66725,#66726,#66727,#66728,#66729,#66730,#66731,
#66732,#66733,#66734,#66735,#66736,#66737,#66738,#66739,#66740,#66741,#66742,
#66743,#66744,#66745,#66746,#66747,#66748,#66749,#66750,#66751,#66752,#66753,
#66754,#66755,#66756,#66757,#66758,#66759,#66760,#66761,#66762,#66763,#66764,
#66765,#66766,#66767,#66768,#66769,#66770,#66771,#66772,#66773,#66774,#66775,
#66776,#66777,#66778,#66779,#66780,#66781,#66782,#66783,#66784,#66785,#66786,
#66787,#66788,#66789,#66790,#66791,#66792,#66793,#66794,#66795,#66796,#66797,
#66798,#66799,#66800,#66801,#66802,#66803,#66804,#66805,#66806,#66807,#66808,
#66809,#66810,#66811,#66812,#66813,#66814,#66815,#66816,#66817,#66818,#66819,
#66820,#66821,#66822,#66823,#66824),.UNSPECIFIED.,.F.,.F.,(4,3,3,3,3,3,
3,3,3,3,3,3,3,3,3,3,3,3,3,3,3,3,3,3,3,3,3,3,3,3,3,3,3,3,3,3,4),(-1.20073064134858,
-1.18778889510928,-1.1398809107738,-1.09143646705355,-1.07167907036071,
-1.06368126609984,-1.01465795392427,-0.965525826915534,-0.949331916808721,
-0.939879021382713,-0.9328302901472,-0.904080313500865,-0.855201229579345,
-0.805662558038644,-0.75704812329517,-0.720587297237565,-0.712370775609727,
-0.705760795802535,-0.65517935802383,-0.611204819064748,-0.560866233442363,
-0.510236856742273,-0.485178941357645,-0.478744674077057,-0.427679530002635,
-0.376207397355228,-0.324773909996537,-0.309773533665251,-0.271051841957094,
-0.254111101834776,-0.243588941900348,-0.237182702864077,-0.18584215881788,
-0.133559100291154,-0.0811710356345407,-0.0293189969567095,0.),
 .UNSPECIFIED.);
#798=B_SPLINE_CURVE_WITH_KNOTS('',3,(#66825,#66826,#66827,#66828,#66829,
#66830,#66831,#66832,#66833,#66834,#66835,#66836,#66837,#66838,#66839,#66840,
#66841,#66842,#66843,#66844,#66845,#66846,#66847,#66848,#66849,#66850,#66851,
#66852,#66853,#66854,#66855,#66856,#66857,#66858,#66859,#66860,#66861,#66862,
#66863,#66864,#66865,#66866,#66867,#66868,#66869,#66870,#66871,#66872,#66873,
#66874,#66875,#66876,#66877,#66878,#66879,#66880,#66881,#66882,#66883,#66884,
#66885,#66886,#66887,#66888,#66889,#66890,#66891,#66892,#66893,#66894,#66895,
#66896,#66897,#66898,#66899,#66900,#66901,#66902,#66903,#66904,#66905,#66906,
#66907,#66908,#66909,#66910,#66911,#66912,#66913,#66914,#66915,#66916,#66917,
#66918,#66919,#66920,#66921,#66922,#66923,#66924,#66925,#66926,#66927,#66928,
#66929,#66930,#66931,#66932,#66933,#66934,#66935,#66936),.UNSPECIFIED.,
 .F.,.F.,(4,3,3,3,3,3,3,3,3,3,3,3,3,3,3,3,3,3,3,3,3,3,3,3,3,3,3,3,3,3,3,
3,3,3,3,3,3,4),(-1.19772932745414,-1.18324084153904,-1.13092606054596,-1.07854075486302,
-1.06423152128911,-1.05378540339643,-1.0457165976122,-0.993876688902704,
-0.942396624118497,-0.92423148604273,-0.913627519080255,-0.906671232415686,
-0.875156121752095,-0.824147097148111,-0.772884353583531,-0.723395591317534,
-0.686279019618035,-0.677622815735757,-0.671424748299867,-0.621152038487914,
-0.57492930451954,-0.524525823920772,-0.474360645599062,-0.450422408151564,
-0.444347114400611,-0.394859071579653,-0.345423983708049,-0.29661796726323,
-0.283145695127838,-0.247752483236858,-0.232267953034554,-0.222024799734449,
-0.215891342040097,-0.167475083764442,-0.1188340990637,-0.0705281081382581,
-0.0231956473791646,0.),.UNSPECIFIED.);
#799=B_SPLINE_CURVE_WITH_KNOTS('',3,(#68413,#68414,#68415,#68416,#68417,
#68418,#68419,#68420,#68421,#68422,#68423,#68424,#68425,#68426,#68427,#68428,
#68429,#68430,#68431,#68432,#68433,#68434),.UNSPECIFIED.,.F.,.F.,(4,3,3,
3,3,3,3,4),(177.03923381194,177.130849992503,177.628408559898,178.125967127293,
178.623525694687,179.121084262082,179.618642829477,180.09311837215),
 .UNSPECIFIED.);
#800=B_SPLINE_CURVE_WITH_KNOTS('',3,(#68436,#68437,#68438,#68439,#68440,
#68441,#68442,#68443,#68444,#68445,#68446,#68447,#68448,#68449,#68450,#68451,
#68452,#68453,#68454,#68455,#68456,#68457,#68458,#68459,#68460,#68461,#68462,
#68463,#68464,#68465,#68466,#68467,#68468,#68469,#68470,#68471,#68472,#68473,
#68474,#68475,#68476,#68477,#68478,#68479,#68480,#68481,#68482,#68483,#68484,
#68485,#68486,#68487,#68488,#68489,#68490,#68491,#68492,#68493,#68494,#68495,
#68496,#68497,#68498,#68499,#68500,#68501,#68502,#68503,#68504,#68505,#68506,
#68507,#68508,#68509,#68510,#68511,#68512,#68513,#68514,#68515,#68516,#68517,
#68518,#68519,#68520,#68521,#68522,#68523,#68524,#68525,#68526,#68527,#68528,
#68529,#68530,#68531,#68532,#68533,#68534,#68535,#68536,#68537,#68538,#68539,
#68540,#68541,#68542,#68543,#68544),.UNSPECIFIED.,.F.,.F.,(4,3,3,3,3,3,
3,3,3,3,3,3,3,3,3,3,3,3,3,3,3,3,3,3,3,3,3,3,3,3,3,3,3,3,3,3,4),(-1.2007306413486,
-1.18778889510928,-1.13988090885874,-1.09143646452528,-1.0716790710066,
-1.06368126691445,-1.01465795435031,-0.965525827699372,-0.949331916721051,
-0.939879020937942,-0.932830289337633,-0.904080313500891,-0.855201231210953,
-0.805662560079378,-0.75704812482572,-0.720587298385477,-0.712370780336783,
-0.705760796757552,-0.655179359089079,-0.611204819064748,-0.560866235739618,
-0.510236859441321,-0.485178943719314,-0.478744677456852,-0.42767953585913,
-0.376207404286961,-0.324773913556237,-0.309773533665262,-0.271051841957104,
-0.254111101834785,-0.243588942121311,-0.23718270326285,-0.185842150821897,
-0.133559088665273,-0.0811710250067116,-0.0293189950592701,0.),
 .UNSPECIFIED.);
#801=B_SPLINE_CURVE_WITH_KNOTS('',3,(#68545,#68546,#68547,#68548,#68549,
#68550,#68551,#68552,#68553,#68554,#68555,#68556,#68557,#68558),
 .UNSPECIFIED.,.F.,.F.,(4,1,1,1,1,1,1,1,1,1,1,4),(10.3280500441581,10.8025255868315,
11.3000841542261,11.7976427216208,12.2952012890155,12.7927598564102,13.2903184238048,
13.7878769911995,14.2854355585942,14.7829941259888,15.2805526933835,15.707963267949),
 .UNSPECIFIED.);
#802=B_SPLINE_CURVE_WITH_KNOTS('',3,(#68564,#68565,#68566,#68567,#68568,
#68569,#68570,#68571,#68572,#68573,#68574,#68575,#68576,#68577,#68578,#68579,
#68580,#68581,#68582,#68583,#68584,#68585,#68586,#68587,#68588,#68589,#68590,
#68591,#68592,#68593,#68594,#68595,#68596,#68597,#68598,#68599,#68600,#68601,
#68602,#68603,#68604,#68605,#68606,#68607,#68608,#68609,#68610,#68611,#68612,
#68613,#68614,#68615,#68616,#68617,#68618,#68619,#68620,#68621,#68622,#68623,
#68624,#68625,#68626,#68627,#68628,#68629,#68630,#68631,#68632,#68633,#68634,
#68635,#68636,#68637,#68638,#68639,#68640,#68641,#68642,#68643,#68644,#68645,
#68646,#68647,#68648,#68649,#68650,#68651,#68652,#68653,#68654,#68655,#68656,
#68657,#68658,#68659,#68660,#68661,#68662,#68663,#68664,#68665,#68666,#68667,
#68668,#68669,#68670,#68671,#68672,#68673,#68674,#68675),.UNSPECIFIED.,
 .F.,.F.,(4,3,3,3,3,3,3,3,3,3,3,3,3,3,3,3,3,3,3,3,3,3,3,3,3,3,3,3,3,3,3,
3,3,3,3,3,3,4),(-1.19772932745415,-1.18324084153908,-1.13092606079167,-1.07854075497836,
-1.06423152144802,-1.05378540334809,-1.04571659768592,-0.993876688885037,
-0.942396624390617,-0.92423148651965,-0.91362752205776,-0.90667123366724,
-0.875156121752115,-0.824147097414577,-0.772884353235954,-0.723395591056853,
-0.686279019422527,-0.677622814824214,-0.671424747566094,-0.621152035937331,
-0.574929304519549,-0.524525824283539,-0.474360650973971,-0.450422418698554,
-0.444347128932818,-0.394859086211904,-0.345424002104565,-0.296617994979428,
-0.283145695127844,-0.247752483236863,-0.23226795303456,-0.222024799667534,
-0.215891341869747,-0.167475088741914,-0.118834100956772,-0.0705281023105065,
-0.0231956289141124,0.),.UNSPECIFIED.);
#803=B_SPLINE_CURVE_WITH_KNOTS('',3,(#68678,#68679,#68680,#68681,#68682,
#68683,#68684,#68685,#68686,#68687,#68688,#68689),.UNSPECIFIED.,.F.,.F.,
(4,1,1,1,1,1,1,1,1,4),(11.6630985309706,12.1606570983653,12.65821566576,
13.1557742331546,13.6533328005493,14.150891367944,14.6484499353386,15.1460085027333,
15.643567070128,15.7079632679491),.UNSPECIFIED.);
#804=B_SPLINE_CURVE_WITH_KNOTS('',3,(#70166,#70167,#70168,#70169,#70170,
#70171,#70172,#70173,#70174,#70175,#70176,#70177,#70178,#70179,#70180,#70181),
 .UNSPECIFIED.,.F.,.F.,(4,3,3,3,3,4),(-182.10643566645,-181.608877099055,
-181.111318531661,-180.613759964266,-180.116201396871,-179.974053338007),
 .UNSPECIFIED.);
#1296=FACE_BOUND('',#7286,.T.);
#1297=FACE_BOUND('',#7446,.T.);
#1298=FACE_BOUND('',#7447,.T.);
#1299=FACE_BOUND('',#7448,.T.);
#1300=FACE_BOUND('',#7449,.T.);
#1301=FACE_BOUND('',#7450,.T.);
#1302=FACE_BOUND('',#7451,.T.);
#1303=FACE_BOUND('',#7452,.T.);
#1304=FACE_BOUND('',#7453,.T.);
#1305=FACE_BOUND('',#7454,.T.);
#1306=FACE_BOUND('',#7455,.T.);
#1307=FACE_BOUND('',#7456,.T.);
#1308=FACE_BOUND('',#7457,.T.);
#1309=FACE_BOUND('',#7458,.T.);
#1310=FACE_BOUND('',#7459,.T.);
#1311=FACE_BOUND('',#7460,.T.);
#1312=FACE_BOUND('',#7461,.T.);
#1313=FACE_BOUND('',#7462,.T.);
#1314=FACE_BOUND('',#7463,.T.);
#1315=FACE_BOUND('',#7464,.T.);
#1316=FACE_BOUND('',#7465,.T.);
#1317=FACE_BOUND('',#7466,.T.);
#1318=FACE_BOUND('',#7467,.T.);
#1319=FACE_BOUND('',#7468,.T.);
#1320=FACE_BOUND('',#7469,.T.);
#1321=FACE_BOUND('',#7470,.T.);
#1322=FACE_BOUND('',#7471,.T.);
#1323=FACE_BOUND('',#7472,.T.);
#1324=FACE_BOUND('',#7473,.T.);
#1325=FACE_BOUND('',#7474,.T.);
#1326=FACE_BOUND('',#7475,.T.);
#1327=FACE_BOUND('',#7476,.T.);
#1328=FACE_BOUND('',#7477,.T.);
#1329=FACE_BOUND('',#7478,.T.);
#1330=FACE_BOUND('',#7479,.T.);
#1331=FACE_BOUND('',#7480,.T.);
#2805=PLANE('',#37339);
#2806=PLANE('',#37340);
#2807=PLANE('',#37341);
#2808=PLANE('',#37344);
#2809=PLANE('',#37350);
#2810=PLANE('',#37351);
#2811=PLANE('',#37352);
#2812=PLANE('',#37353);
#2813=PLANE('',#37355);
#2814=PLANE('',#37356);
#2815=PLANE('',#37362);
#2816=PLANE('',#37363);
#2817=PLANE('',#37365);
#2818=PLANE('',#37366);
#2819=PLANE('',#37368);
#2820=PLANE('',#37369);
#2821=PLANE('',#37371);
#2822=PLANE('',#37372);
#2823=PLANE('',#37374);
#2824=PLANE('',#37375);
#2825=PLANE('',#37377);
#2826=PLANE('',#37378);
#2827=PLANE('',#37380);
#2828=PLANE('',#37381);
#2829=PLANE('',#37383);
#2830=PLANE('',#37384);
#2831=PLANE('',#37386);
#2832=PLANE('',#37387);
#2833=PLANE('',#37389);
#2834=PLANE('',#37390);
#2835=PLANE('',#37392);
#2836=PLANE('',#37393);
#2837=PLANE('',#37395);
#2838=PLANE('',#37396);
#2839=PLANE('',#37398);
#2840=PLANE('',#37399);
#2841=PLANE('',#37401);
#2842=PLANE('',#37402);
#2843=PLANE('',#37404);
#2844=PLANE('',#37405);
#2845=PLANE('',#37407);
#2846=PLANE('',#37408);
#2847=PLANE('',#37410);
#2848=PLANE('',#37411);
#2849=PLANE('',#37413);
#2850=PLANE('',#37414);
#2851=PLANE('',#37416);
#2852=PLANE('',#37417);
#2853=PLANE('',#37419);
#2854=PLANE('',#37420);
#2855=PLANE('',#37422);
#2856=PLANE('',#37423);
#2857=PLANE('',#37425);
#2858=PLANE('',#37426);
#2859=PLANE('',#37428);
#2860=PLANE('',#37429);
#2861=PLANE('',#37431);
#2862=PLANE('',#37432);
#2863=PLANE('',#37434);
#2864=PLANE('',#37435);
#2865=PLANE('',#37437);
#2866=PLANE('',#37438);
#2867=PLANE('',#37440);
#2868=PLANE('',#37441);
#2869=PLANE('',#37443);
#2870=PLANE('',#37444);
#2871=PLANE('',#37446);
#2872=PLANE('',#37447);
#2873=PLANE('',#37449);
#2874=PLANE('',#37450);
#2875=PLANE('',#37452);
#2876=PLANE('',#37453);
#2877=PLANE('',#37455);
#2878=PLANE('',#37456);
#2879=PLANE('',#37458);
#2880=PLANE('',#37459);
#2881=PLANE('',#37461);
#2882=PLANE('',#37462);
#2883=PLANE('',#37464);
#2884=PLANE('',#37465);
#2885=PLANE('',#37468);
#2886=PLANE('',#37469);
#2887=PLANE('',#37472);
#2888=PLANE('',#37473);
#2889=PLANE('',#37475);
#2890=PLANE('',#37476);
#2891=PLANE('',#37478);
#2892=PLANE('',#37479);
#2893=PLANE('',#37481);
#2894=PLANE('',#37482);
#2895=PLANE('',#37484);
#2896=PLANE('',#37485);
#2897=PLANE('',#37487);
#2898=PLANE('',#37488);
#2899=PLANE('',#37490);
#2900=PLANE('',#37491);
#2901=PLANE('',#37493);
#2902=PLANE('',#37494);
#2903=PLANE('',#37496);
#2904=PLANE('',#37497);
#2905=PLANE('',#37499);
#2906=PLANE('',#37500);
#2907=PLANE('',#37502);
#2908=PLANE('',#37503);
#2909=PLANE('',#37505);
#2910=PLANE('',#37506);
#2911=PLANE('',#37508);
#2912=PLANE('',#37509);
#2913=PLANE('',#37511);
#2914=PLANE('',#37512);
#2915=PLANE('',#37514);
#2916=PLANE('',#37515);
#2917=PLANE('',#37517);
#2918=PLANE('',#37518);
#2919=PLANE('',#37520);
#2920=PLANE('',#37521);
#2921=PLANE('',#37523);
#2922=PLANE('',#37524);
#2923=PLANE('',#37526);
#2924=PLANE('',#37527);
#2925=PLANE('',#37529);
#2926=PLANE('',#37530);
#2927=PLANE('',#37532);
#2928=PLANE('',#37533);
#2929=PLANE('',#37535);
#2930=PLANE('',#37536);
#2931=PLANE('',#37538);
#2932=PLANE('',#37539);
#2933=PLANE('',#37541);
#2934=PLANE('',#37542);
#2935=PLANE('',#37544);
#2936=PLANE('',#37545);
#2937=PLANE('',#37547);
#2938=PLANE('',#37548);
#2939=PLANE('',#37550);
#2940=PLANE('',#37551);
#2941=PLANE('',#37553);
#2942=PLANE('',#37554);
#2943=PLANE('',#37556);
#2944=PLANE('',#37557);
#2945=PLANE('',#37559);
#2946=PLANE('',#37560);
#2947=PLANE('',#37562);
#2948=PLANE('',#37563);
#2949=PLANE('',#37565);
#2950=PLANE('',#37566);
#2951=PLANE('',#37568);
#2952=PLANE('',#37569);
#2953=PLANE('',#37571);
#2954=PLANE('',#37572);
#2955=PLANE('',#37574);
#2956=PLANE('',#37575);
#2957=PLANE('',#37577);
#2958=PLANE('',#37578);
#3076=CYLINDRICAL_SURFACE('',#37270,6.28269);
#3077=CYLINDRICAL_SURFACE('',#37272,6.28269);
#3078=CYLINDRICAL_SURFACE('',#37273,6.28269);
#3079=CYLINDRICAL_SURFACE('',#37274,6.28269);
#3080=CYLINDRICAL_SURFACE('',#37275,6.28269);
#3081=CYLINDRICAL_SURFACE('',#37276,6.28269);
#3082=CYLINDRICAL_SURFACE('',#37277,6.28269);
#3083=CYLINDRICAL_SURFACE('',#37278,6.28269);
#3084=CYLINDRICAL_SURFACE('',#37279,6.28269);
#3085=CYLINDRICAL_SURFACE('',#37280,6.28269);
#3086=CYLINDRICAL_SURFACE('',#37281,6.28269);
#3087=CYLINDRICAL_SURFACE('',#37282,6.28269);
#3088=CYLINDRICAL_SURFACE('',#37283,6.28269);
#3089=CYLINDRICAL_SURFACE('',#37284,6.28269);
#3090=CYLINDRICAL_SURFACE('',#37285,6.28269);
#3091=CYLINDRICAL_SURFACE('',#37286,6.28269);
#3092=CYLINDRICAL_SURFACE('',#37287,6.28269);
#3093=CYLINDRICAL_SURFACE('',#37288,6.28269);
#3094=CYLINDRICAL_SURFACE('',#37289,6.28269);
#3095=CYLINDRICAL_SURFACE('',#37290,6.28269);
#3096=CYLINDRICAL_SURFACE('',#37291,6.28269);
#3097=CYLINDRICAL_SURFACE('',#37292,6.28269);
#3098=CYLINDRICAL_SURFACE('',#37293,6.28269);
#3099=CYLINDRICAL_SURFACE('',#37294,6.28269);
#3100=CYLINDRICAL_SURFACE('',#37295,6.28269);
#3101=CYLINDRICAL_SURFACE('',#37296,6.28269);
#3102=CYLINDRICAL_SURFACE('',#37297,6.28269);
#3103=CYLINDRICAL_SURFACE('',#37298,6.28269);
#3104=CYLINDRICAL_SURFACE('',#37299,6.28269);
#3105=CYLINDRICAL_SURFACE('',#37300,5.57784);
#3106=CYLINDRICAL_SURFACE('',#37302,5.57784);
#3107=CYLINDRICAL_SURFACE('',#37304,5.57784);
#3108=CYLINDRICAL_SURFACE('',#37305,5.57784);
#3109=CYLINDRICAL_SURFACE('',#37306,5.57784);
#3110=CYLINDRICAL_SURFACE('',#37307,5.57784);
#3111=CYLINDRICAL_SURFACE('',#37308,5.57784);
#3112=CYLINDRICAL_SURFACE('',#37309,5.57784);
#3113=CYLINDRICAL_SURFACE('',#37310,5.57784);
#3114=CYLINDRICAL_SURFACE('',#37311,5.57784);
#3115=CYLINDRICAL_SURFACE('',#37312,5.57784);
#3116=CYLINDRICAL_SURFACE('',#37313,5.57784);
#3117=CYLINDRICAL_SURFACE('',#37314,5.57784);
#3118=CYLINDRICAL_SURFACE('',#37315,5.57784);
#3119=CYLINDRICAL_SURFACE('',#37316,5.57784);
#3120=CYLINDRICAL_SURFACE('',#37317,5.57784);
#3121=CYLINDRICAL_SURFACE('',#37318,5.57784);
#3122=CYLINDRICAL_SURFACE('',#37319,5.57784);
#3123=CYLINDRICAL_SURFACE('',#37320,5.57784);
#3124=CYLINDRICAL_SURFACE('',#37321,5.57784);
#3125=CYLINDRICAL_SURFACE('',#37322,5.57784);
#3126=CYLINDRICAL_SURFACE('',#37323,5.57784);
#3127=CYLINDRICAL_SURFACE('',#37324,5.57784);
#3128=CYLINDRICAL_SURFACE('',#37325,5.57784);
#3129=CYLINDRICAL_SURFACE('',#37326,5.57784);
#3130=CYLINDRICAL_SURFACE('',#37327,5.57784);
#3131=CYLINDRICAL_SURFACE('',#37328,5.57784);
#3132=CYLINDRICAL_SURFACE('',#37329,5.57784);
#3133=CYLINDRICAL_SURFACE('',#37330,5.57784);
#3134=CYLINDRICAL_SURFACE('',#37345,11.);
#3135=CYLINDRICAL_SURFACE('',#37360,5.57784);
#3136=CYLINDRICAL_SURFACE('',#37361,6.28269);
#3137=CYLINDRICAL_SURFACE('',#37580,7.17);
#4962=FACE_OUTER_BOUND('',#7223,.T.);
#4963=FACE_OUTER_BOUND('',#7224,.T.);
#4964=FACE_OUTER_BOUND('',#7225,.T.);
#4965=FACE_OUTER_BOUND('',#7226,.T.);
#4966=FACE_OUTER_BOUND('',#7227,.T.);
#4967=FACE_OUTER_BOUND('',#7228,.T.);
#4968=FACE_OUTER_BOUND('',#7229,.T.);
#4969=FACE_OUTER_BOUND('',#7230,.T.);
#4970=FACE_OUTER_BOUND('',#7231,.T.);
#4971=FACE_OUTER_BOUND('',#7232,.T.);
#4972=FACE_OUTER_BOUND('',#7233,.T.);
#4973=FACE_OUTER_BOUND('',#7234,.T.);
#4974=FACE_OUTER_BOUND('',#7235,.T.);
#4975=FACE_OUTER_BOUND('',#7236,.T.);
#4976=FACE_OUTER_BOUND('',#7237,.T.);
#4977=FACE_OUTER_BOUND('',#7238,.T.);
#4978=FACE_OUTER_BOUND('',#7239,.T.);
#4979=FACE_OUTER_BOUND('',#7240,.T.);
#4980=FACE_OUTER_BOUND('',#7241,.T.);
#4981=FACE_OUTER_BOUND('',#7242,.T.);
#4982=FACE_OUTER_BOUND('',#7243,.T.);
#4983=FACE_OUTER_BOUND('',#7244,.T.);
#4984=FACE_OUTER_BOUND('',#7245,.T.);
#4985=FACE_OUTER_BOUND('',#7246,.T.);
#4986=FACE_OUTER_BOUND('',#7247,.T.);
#4987=FACE_OUTER_BOUND('',#7248,.T.);
#4988=FACE_OUTER_BOUND('',#7249,.T.);
#4989=FACE_OUTER_BOUND('',#7250,.T.);
#4990=FACE_OUTER_BOUND('',#7251,.T.);
#4991=FACE_OUTER_BOUND('',#7252,.T.);
#4992=FACE_OUTER_BOUND('',#7253,.T.);
#4993=FACE_OUTER_BOUND('',#7254,.T.);
#4994=FACE_OUTER_BOUND('',#7255,.T.);
#4995=FACE_OUTER_BOUND('',#7256,.T.);
#4996=FACE_OUTER_BOUND('',#7257,.T.);
#4997=FACE_OUTER_BOUND('',#7258,.T.);
#4998=FACE_OUTER_BOUND('',#7259,.T.);
#4999=FACE_OUTER_BOUND('',#7260,.T.);
#5000=FACE_OUTER_BOUND('',#7261,.T.);
#5001=FACE_OUTER_BOUND('',#7262,.T.);
#5002=FACE_OUTER_BOUND('',#7263,.T.);
#5003=FACE_OUTER_BOUND('',#7264,.T.);
#5004=FACE_OUTER_BOUND('',#7265,.T.);
#5005=FACE_OUTER_BOUND('',#7266,.T.);
#5006=FACE_OUTER_BOUND('',#7267,.T.);
#5007=FACE_OUTER_BOUND('',#7268,.T.);
#5008=FACE_OUTER_BOUND('',#7269,.T.);
#5009=FACE_OUTER_BOUND('',#7270,.T.);
#5010=FACE_OUTER_BOUND('',#7271,.T.);
#5011=FACE_OUTER_BOUND('',#7272,.T.);
#5012=FACE_OUTER_BOUND('',#7273,.T.);
#5013=FACE_OUTER_BOUND('',#7274,.T.);
#5014=FACE_OUTER_BOUND('',#7275,.T.);
#5015=FACE_OUTER_BOUND('',#7276,.T.);
#5016=FACE_OUTER_BOUND('',#7277,.T.);
#5017=FACE_OUTER_BOUND('',#7278,.T.);
#5018=FACE_OUTER_BOUND('',#7279,.T.);
#5019=FACE_OUTER_BOUND('',#7280,.T.);
#5020=FACE_OUTER_BOUND('',#7281,.T.);
#5021=FACE_OUTER_BOUND('',#7282,.T.);
#5022=FACE_OUTER_BOUND('',#7283,.T.);
#5023=FACE_OUTER_BOUND('',#7284,.T.);
#5024=FACE_OUTER_BOUND('',#7285,.T.);
#5025=FACE_OUTER_BOUND('',#7287,.T.);
#5026=FACE_OUTER_BOUND('',#7288,.T.);
#5027=FACE_OUTER_BOUND('',#7289,.T.);
#5028=FACE_OUTER_BOUND('',#7290,.T.);
#5029=FACE_OUTER_BOUND('',#7291,.T.);
#5030=FACE_OUTER_BOUND('',#7292,.T.);
#5031=FACE_OUTER_BOUND('',#7293,.T.);
#5032=FACE_OUTER_BOUND('',#7294,.T.);
#5033=FACE_OUTER_BOUND('',#7295,.T.);
#5034=FACE_OUTER_BOUND('',#7296,.T.);
#5035=FACE_OUTER_BOUND('',#7297,.T.);
#5036=FACE_OUTER_BOUND('',#7298,.T.);
#5037=FACE_OUTER_BOUND('',#7299,.T.);
#5038=FACE_OUTER_BOUND('',#7300,.T.);
#5039=FACE_OUTER_BOUND('',#7301,.T.);
#5040=FACE_OUTER_BOUND('',#7302,.T.);
#5041=FACE_OUTER_BOUND('',#7303,.T.);
#5042=FACE_OUTER_BOUND('',#7304,.T.);
#5043=FACE_OUTER_BOUND('',#7305,.T.);
#5044=FACE_OUTER_BOUND('',#7306,.T.);
#5045=FACE_OUTER_BOUND('',#7307,.T.);
#5046=FACE_OUTER_BOUND('',#7308,.T.);
#5047=FACE_OUTER_BOUND('',#7309,.T.);
#5048=FACE_OUTER_BOUND('',#7310,.T.);
#5049=FACE_OUTER_BOUND('',#7311,.T.);
#5050=FACE_OUTER_BOUND('',#7312,.T.);
#5051=FACE_OUTER_BOUND('',#7313,.T.);
#5052=FACE_OUTER_BOUND('',#7314,.T.);
#5053=FACE_OUTER_BOUND('',#7315,.T.);
#5054=FACE_OUTER_BOUND('',#7316,.T.);
#5055=FACE_OUTER_BOUND('',#7317,.T.);
#5056=FACE_OUTER_BOUND('',#7318,.T.);
#5057=FACE_OUTER_BOUND('',#7319,.T.);
#5058=FACE_OUTER_BOUND('',#7320,.T.);
#5059=FACE_OUTER_BOUND('',#7321,.T.);
#5060=FACE_OUTER_BOUND('',#7322,.T.);
#5061=FACE_OUTER_BOUND('',#7323,.T.);
#5062=FACE_OUTER_BOUND('',#7324,.T.);
#5063=FACE_OUTER_BOUND('',#7325,.T.);
#5064=FACE_OUTER_BOUND('',#7326,.T.);
#5065=FACE_OUTER_BOUND('',#7327,.T.);
#5066=FACE_OUTER_BOUND('',#7328,.T.);
#5067=FACE_OUTER_BOUND('',#7329,.T.);
#5068=FACE_OUTER_BOUND('',#7330,.T.);
#5069=FACE_OUTER_BOUND('',#7331,.T.);
#5070=FACE_OUTER_BOUND('',#7332,.T.);
#5071=FACE_OUTER_BOUND('',#7333,.T.);
#5072=FACE_OUTER_BOUND('',#7334,.T.);
#5073=FACE_OUTER_BOUND('',#7335,.T.);
#5074=FACE_OUTER_BOUND('',#7336,.T.);
#5075=FACE_OUTER_BOUND('',#7337,.T.);
#5076=FACE_OUTER_BOUND('',#7338,.T.);
#5077=FACE_OUTER_BOUND('',#7339,.T.);
#5078=FACE_OUTER_BOUND('',#7340,.T.);
#5079=FACE_OUTER_BOUND('',#7341,.T.);
#5080=FACE_OUTER_BOUND('',#7342,.T.);
#5081=FACE_OUTER_BOUND('',#7343,.T.);
#5082=FACE_OUTER_BOUND('',#7344,.T.);
#5083=FACE_OUTER_BOUND('',#7345,.T.);
#5084=FACE_OUTER_BOUND('',#7346,.T.);
#5085=FACE_OUTER_BOUND('',#7347,.T.);
#5086=FACE_OUTER_BOUND('',#7348,.T.);
#5087=FACE_OUTER_BOUND('',#7349,.T.);
#5088=FACE_OUTER_BOUND('',#7350,.T.);
#5089=FACE_OUTER_BOUND('',#7351,.T.);
#5090=FACE_OUTER_BOUND('',#7352,.T.);
#5091=FACE_OUTER_BOUND('',#7353,.T.);
#5092=FACE_OUTER_BOUND('',#7354,.T.);
#5093=FACE_OUTER_BOUND('',#7355,.T.);
#5094=FACE_OUTER_BOUND('',#7356,.T.);
#5095=FACE_OUTER_BOUND('',#7357,.T.);
#5096=FACE_OUTER_BOUND('',#7358,.T.);
#5097=FACE_OUTER_BOUND('',#7359,.T.);
#5098=FACE_OUTER_BOUND('',#7360,.T.);
#5099=FACE_OUTER_BOUND('',#7361,.T.);
#5100=FACE_OUTER_BOUND('',#7362,.T.);
#5101=FACE_OUTER_BOUND('',#7363,.T.);
#5102=FACE_OUTER_BOUND('',#7364,.T.);
#5103=FACE_OUTER_BOUND('',#7365,.T.);
#5104=FACE_OUTER_BOUND('',#7366,.T.);
#5105=FACE_OUTER_BOUND('',#7367,.T.);
#5106=FACE_OUTER_BOUND('',#7368,.T.);
#5107=FACE_OUTER_BOUND('',#7369,.T.);
#5108=FACE_OUTER_BOUND('',#7370,.T.);
#5109=FACE_OUTER_BOUND('',#7371,.T.);
#5110=FACE_OUTER_BOUND('',#7372,.T.);
#5111=FACE_OUTER_BOUND('',#7373,.T.);
#5112=FACE_OUTER_BOUND('',#7374,.T.);
#5113=FACE_OUTER_BOUND('',#7375,.T.);
#5114=FACE_OUTER_BOUND('',#7376,.T.);
#5115=FACE_OUTER_BOUND('',#7377,.T.);
#5116=FACE_OUTER_BOUND('',#7378,.T.);
#5117=FACE_OUTER_BOUND('',#7379,.T.);
#5118=FACE_OUTER_BOUND('',#7380,.T.);
#5119=FACE_OUTER_BOUND('',#7381,.T.);
#5120=FACE_OUTER_BOUND('',#7382,.T.);
#5121=FACE_OUTER_BOUND('',#7383,.T.);
#5122=FACE_OUTER_BOUND('',#7384,.T.);
#5123=FACE_OUTER_BOUND('',#7385,.T.);
#5124=FACE_OUTER_BOUND('',#7386,.T.);
#5125=FACE_OUTER_BOUND('',#7387,.T.);
#5126=FACE_OUTER_BOUND('',#7388,.T.);
#5127=FACE_OUTER_BOUND('',#7389,.T.);
#5128=FACE_OUTER_BOUND('',#7390,.T.);
#5129=FACE_OUTER_BOUND('',#7391,.T.);
#5130=FACE_OUTER_BOUND('',#7392,.T.);
#5131=FACE_OUTER_BOUND('',#7393,.T.);
#5132=FACE_OUTER_BOUND('',#7394,.T.);
#5133=FACE_OUTER_BOUND('',#7395,.T.);
#5134=FACE_OUTER_BOUND('',#7396,.T.);
#5135=FACE_OUTER_BOUND('',#7397,.T.);
#5136=FACE_OUTER_BOUND('',#7398,.T.);
#5137=FACE_OUTER_BOUND('',#7399,.T.);
#5138=FACE_OUTER_BOUND('',#7400,.T.);
#5139=FACE_OUTER_BOUND('',#7401,.T.);
#5140=FACE_OUTER_BOUND('',#7402,.T.);
#5141=FACE_OUTER_BOUND('',#7403,.T.);
#5142=FACE_OUTER_BOUND('',#7404,.T.);
#5143=FACE_OUTER_BOUND('',#7405,.T.);
#5144=FACE_OUTER_BOUND('',#7406,.T.);
#5145=FACE_OUTER_BOUND('',#7407,.T.);
#5146=FACE_OUTER_BOUND('',#7408,.T.);
#5147=FACE_OUTER_BOUND('',#7409,.T.);
#5148=FACE_OUTER_BOUND('',#7410,.T.);
#5149=FACE_OUTER_BOUND('',#7411,.T.);
#5150=FACE_OUTER_BOUND('',#7412,.T.);
#5151=FACE_OUTER_BOUND('',#7413,.T.);
#5152=FACE_OUTER_BOUND('',#7414,.T.);
#5153=FACE_OUTER_BOUND('',#7415,.T.);
#5154=FACE_OUTER_BOUND('',#7416,.T.);
#5155=FACE_OUTER_BOUND('',#7417,.T.);
#5156=FACE_OUTER_BOUND('',#7418,.T.);
#5157=FACE_OUTER_BOUND('',#7419,.T.);
#5158=FACE_OUTER_BOUND('',#7420,.T.);
#5159=FACE_OUTER_BOUND('',#7421,.T.);
#5160=FACE_OUTER_BOUND('',#7422,.T.);
#5161=FACE_OUTER_BOUND('',#7423,.T.);
#5162=FACE_OUTER_BOUND('',#7424,.T.);
#5163=FACE_OUTER_BOUND('',#7425,.T.);
#5164=FACE_OUTER_BOUND('',#7426,.T.);
#5165=FACE_OUTER_BOUND('',#7427,.T.);
#5166=FACE_OUTER_BOUND('',#7428,.T.);
#5167=FACE_OUTER_BOUND('',#7429,.T.);
#5168=FACE_OUTER_BOUND('',#7430,.T.);
#5169=FACE_OUTER_BOUND('',#7431,.T.);
#5170=FACE_OUTER_BOUND('',#7432,.T.);
#5171=FACE_OUTER_BOUND('',#7433,.T.);
#5172=FACE_OUTER_BOUND('',#7434,.T.);
#5173=FACE_OUTER_BOUND('',#7435,.T.);
#5174=FACE_OUTER_BOUND('',#7436,.T.);
#5175=FACE_OUTER_BOUND('',#7437,.T.);
#5176=FACE_OUTER_BOUND('',#7438,.T.);
#5177=FACE_OUTER_BOUND('',#7439,.T.);
#5178=FACE_OUTER_BOUND('',#7440,.T.);
#5179=FACE_OUTER_BOUND('',#7441,.T.);
#5180=FACE_OUTER_BOUND('',#7442,.T.);
#5181=FACE_OUTER_BOUND('',#7443,.T.);
#5182=FACE_OUTER_BOUND('',#7444,.T.);
#5183=FACE_OUTER_BOUND('',#7445,.T.);
#5184=FACE_OUTER_BOUND('',#7481,.T.);
#7223=EDGE_LOOP('',(#30624,#30625,#30626,#30627));
#7224=EDGE_LOOP('',(#30628,#30629,#30630,#30631));
#7225=EDGE_LOOP('',(#30632,#30633,#30634,#30635));
#7226=EDGE_LOOP('',(#30636,#30637,#30638,#30639));
#7227=EDGE_LOOP('',(#30640,#30641,#30642,#30643));
#7228=EDGE_LOOP('',(#30644,#30645,#30646,#30647));
#7229=EDGE_LOOP('',(#30648,#30649,#30650,#30651));
#7230=EDGE_LOOP('',(#30652,#30653,#30654,#30655));
#7231=EDGE_LOOP('',(#30656,#30657,#30658,#30659));
#7232=EDGE_LOOP('',(#30660,#30661,#30662,#30663));
#7233=EDGE_LOOP('',(#30664,#30665,#30666,#30667));
#7234=EDGE_LOOP('',(#30668,#30669,#30670,#30671));
#7235=EDGE_LOOP('',(#30672,#30673,#30674,#30675));
#7236=EDGE_LOOP('',(#30676,#30677,#30678,#30679));
#7237=EDGE_LOOP('',(#30680,#30681,#30682,#30683));
#7238=EDGE_LOOP('',(#30684,#30685,#30686,#30687));
#7239=EDGE_LOOP('',(#30688,#30689,#30690,#30691));
#7240=EDGE_LOOP('',(#30692,#30693,#30694,#30695));
#7241=EDGE_LOOP('',(#30696,#30697,#30698,#30699));
#7242=EDGE_LOOP('',(#30700,#30701,#30702,#30703));
#7243=EDGE_LOOP('',(#30704,#30705,#30706,#30707));
#7244=EDGE_LOOP('',(#30708,#30709,#30710,#30711));
#7245=EDGE_LOOP('',(#30712,#30713,#30714,#30715));
#7246=EDGE_LOOP('',(#30716,#30717,#30718,#30719));
#7247=EDGE_LOOP('',(#30720,#30721,#30722,#30723));
#7248=EDGE_LOOP('',(#30724,#30725,#30726,#30727));
#7249=EDGE_LOOP('',(#30728,#30729,#30730,#30731));
#7250=EDGE_LOOP('',(#30732,#30733,#30734,#30735));
#7251=EDGE_LOOP('',(#30736,#30737,#30738,#30739));
#7252=EDGE_LOOP('',(#30740,#30741,#30742));
#7253=EDGE_LOOP('',(#30743,#30744,#30745,#30746,#30747));
#7254=EDGE_LOOP('',(#30748,#30749,#30750,#30751));
#7255=EDGE_LOOP('',(#30752,#30753,#30754,#30755));
#7256=EDGE_LOOP('',(#30756,#30757,#30758,#30759));
#7257=EDGE_LOOP('',(#30760,#30761,#30762,#30763));
#7258=EDGE_LOOP('',(#30764,#30765,#30766,#30767));
#7259=EDGE_LOOP('',(#30768,#30769,#30770,#30771));
#7260=EDGE_LOOP('',(#30772,#30773,#30774,#30775));
#7261=EDGE_LOOP('',(#30776,#30777,#30778,#30779));
#7262=EDGE_LOOP('',(#30780,#30781,#30782,#30783));
#7263=EDGE_LOOP('',(#30784,#30785,#30786,#30787));
#7264=EDGE_LOOP('',(#30788,#30789,#30790,#30791));
#7265=EDGE_LOOP('',(#30792,#30793,#30794,#30795));
#7266=EDGE_LOOP('',(#30796,#30797,#30798,#30799));
#7267=EDGE_LOOP('',(#30800,#30801,#30802,#30803));
#7268=EDGE_LOOP('',(#30804,#30805,#30806,#30807));
#7269=EDGE_LOOP('',(#30808,#30809,#30810,#30811));
#7270=EDGE_LOOP('',(#30812,#30813,#30814,#30815));
#7271=EDGE_LOOP('',(#30816,#30817,#30818,#30819));
#7272=EDGE_LOOP('',(#30820,#30821,#30822,#30823));
#7273=EDGE_LOOP('',(#30824,#30825,#30826,#30827));
#7274=EDGE_LOOP('',(#30828,#30829,#30830,#30831));
#7275=EDGE_LOOP('',(#30832,#30833,#30834,#30835));
#7276=EDGE_LOOP('',(#30836,#30837,#30838,#30839));
#7277=EDGE_LOOP('',(#30840,#30841,#30842,#30843));
#7278=EDGE_LOOP('',(#30844,#30845,#30846,#30847));
#7279=EDGE_LOOP('',(#30848,#30849,#30850,#30851));
#7280=EDGE_LOOP('',(#30852,#30853,#30854,#30855));
#7281=EDGE_LOOP('',(#30856,#30857,#30858,#30859,#30860));
#7282=EDGE_LOOP('',(#30861,#30862,#30863,#30864,#30865,#30866,#30867));
#7283=EDGE_LOOP('',(#30868));
#7284=EDGE_LOOP('',(#30869,#30870,#30871,#30872,#30873,#30874));
#7285=EDGE_LOOP('',(#30875,#30876));
#7286=EDGE_LOOP('',(#30877));
#7287=EDGE_LOOP('',(#30878,#30879,#30880,#30881,#30882,#30883));
#7288=EDGE_LOOP('',(#30884,#30885,#30886,#30887));
#7289=EDGE_LOOP('',(#30888,#30889,#30890,#30891,#30892,#30893));
#7290=EDGE_LOOP('',(#30894,#30895,#30896,#30897,#30898,#30899));
#7291=EDGE_LOOP('',(#30900,#30901,#30902,#30903));
#7292=EDGE_LOOP('',(#30904,#30905));
#7293=EDGE_LOOP('',(#30906,#30907,#30908,#30909,#30910,#30911));
#7294=EDGE_LOOP('',(#30912,#30913,#30914,#30915,#30916,#30917));
#7295=EDGE_LOOP('',(#30918,#30919,#30920,#30921,#30922,#30923));
#7296=EDGE_LOOP('',(#30924,#30925,#30926,#30927,#30928,#30929,#30930,#30931,
#30932,#30933,#30934,#30935,#30936,#30937,#30938,#30939,#30940,#30941,#30942,
#30943,#30944,#30945,#30946,#30947,#30948,#30949,#30950,#30951,#30952,#30953,
#30954,#30955,#30956,#30957,#30958,#30959,#30960,#30961,#30962,#30963,#30964,
#30965,#30966,#30967,#30968,#30969,#30970,#30971,#30972,#30973,#30974,#30975,
#30976,#30977,#30978,#30979,#30980,#30981,#30982,#30983,#30984));
#7297=EDGE_LOOP('',(#30985,#30986,#30987,#30988,#30989));
#7298=EDGE_LOOP('',(#30990,#30991,#30992,#30993));
#7299=EDGE_LOOP('',(#30994,#30995,#30996,#30997,#30998,#30999,#31000,#31001,
#31002,#31003,#31004,#31005,#31006,#31007,#31008,#31009,#31010,#31011,#31012,
#31013,#31014,#31015,#31016,#31017,#31018,#31019,#31020,#31021,#31022,#31023,
#31024,#31025,#31026,#31027,#31028,#31029,#31030,#31031,#31032,#31033,#31034,
#31035,#31036,#31037,#31038,#31039,#31040,#31041,#31042,#31043,#31044,#31045,
#31046,#31047,#31048,#31049,#31050,#31051,#31052,#31053,#31054,#31055));
#7300=EDGE_LOOP('',(#31056,#31057,#31058,#31059));
#7301=EDGE_LOOP('',(#31060,#31061,#31062,#31063));
#7302=EDGE_LOOP('',(#31064,#31065,#31066));
#7303=EDGE_LOOP('',(#31067,#31068,#31069,#31070));
#7304=EDGE_LOOP('',(#31071,#31072,#31073));
#7305=EDGE_LOOP('',(#31074,#31075,#31076,#31077));
#7306=EDGE_LOOP('',(#31078,#31079,#31080));
#7307=EDGE_LOOP('',(#31081,#31082,#31083,#31084));
#7308=EDGE_LOOP('',(#31085,#31086,#31087));
#7309=EDGE_LOOP('',(#31088,#31089,#31090,#31091));
#7310=EDGE_LOOP('',(#31092,#31093,#31094));
#7311=EDGE_LOOP('',(#31095,#31096,#31097,#31098));
#7312=EDGE_LOOP('',(#31099,#31100,#31101));
#7313=EDGE_LOOP('',(#31102,#31103,#31104,#31105));
#7314=EDGE_LOOP('',(#31106,#31107,#31108));
#7315=EDGE_LOOP('',(#31109,#31110,#31111,#31112));
#7316=EDGE_LOOP('',(#31113,#31114,#31115));
#7317=EDGE_LOOP('',(#31116,#31117,#31118,#31119));
#7318=EDGE_LOOP('',(#31120,#31121,#31122));
#7319=EDGE_LOOP('',(#31123,#31124,#31125,#31126));
#7320=EDGE_LOOP('',(#31127,#31128,#31129));
#7321=EDGE_LOOP('',(#31130,#31131,#31132,#31133));
#7322=EDGE_LOOP('',(#31134,#31135,#31136));
#7323=EDGE_LOOP('',(#31137,#31138,#31139,#31140));
#7324=EDGE_LOOP('',(#31141,#31142,#31143));
#7325=EDGE_LOOP('',(#31144,#31145,#31146,#31147));
#7326=EDGE_LOOP('',(#31148,#31149,#31150));
#7327=EDGE_LOOP('',(#31151,#31152,#31153,#31154));
#7328=EDGE_LOOP('',(#31155,#31156,#31157));
#7329=EDGE_LOOP('',(#31158,#31159,#31160,#31161));
#7330=EDGE_LOOP('',(#31162,#31163,#31164));
#7331=EDGE_LOOP('',(#31165,#31166,#31167,#31168));
#7332=EDGE_LOOP('',(#31169,#31170,#31171));
#7333=EDGE_LOOP('',(#31172,#31173,#31174,#31175));
#7334=EDGE_LOOP('',(#31176,#31177,#31178));
#7335=EDGE_LOOP('',(#31179,#31180,#31181,#31182));
#7336=EDGE_LOOP('',(#31183,#31184,#31185));
#7337=EDGE_LOOP('',(#31186,#31187,#31188,#31189));
#7338=EDGE_LOOP('',(#31190,#31191,#31192));
#7339=EDGE_LOOP('',(#31193,#31194,#31195,#31196));
#7340=EDGE_LOOP('',(#31197,#31198,#31199));
#7341=EDGE_LOOP('',(#31200,#31201,#31202,#31203));
#7342=EDGE_LOOP('',(#31204,#31205,#31206));
#7343=EDGE_LOOP('',(#31207,#31208,#31209,#31210));
#7344=EDGE_LOOP('',(#31211,#31212,#31213));
#7345=EDGE_LOOP('',(#31214,#31215,#31216,#31217));
#7346=EDGE_LOOP('',(#31218,#31219,#31220));
#7347=EDGE_LOOP('',(#31221,#31222,#31223,#31224));
#7348=EDGE_LOOP('',(#31225,#31226,#31227));
#7349=EDGE_LOOP('',(#31228,#31229,#31230,#31231));
#7350=EDGE_LOOP('',(#31232,#31233,#31234));
#7351=EDGE_LOOP('',(#31235,#31236,#31237,#31238));
#7352=EDGE_LOOP('',(#31239,#31240,#31241));
#7353=EDGE_LOOP('',(#31242,#31243,#31244,#31245));
#7354=EDGE_LOOP('',(#31246,#31247,#31248));
#7355=EDGE_LOOP('',(#31249,#31250,#31251,#31252));
#7356=EDGE_LOOP('',(#31253,#31254,#31255));
#7357=EDGE_LOOP('',(#31256,#31257,#31258,#31259));
#7358=EDGE_LOOP('',(#31260,#31261,#31262));
#7359=EDGE_LOOP('',(#31263,#31264,#31265,#31266));
#7360=EDGE_LOOP('',(#31267,#31268,#31269));
#7361=EDGE_LOOP('',(#31270,#31271,#31272,#31273));
#7362=EDGE_LOOP('',(#31274,#31275,#31276));
#7363=EDGE_LOOP('',(#31277,#31278,#31279,#31280));
#7364=EDGE_LOOP('',(#31281,#31282,#31283));
#7365=EDGE_LOOP('',(#31284,#31285,#31286,#31287));
#7366=EDGE_LOOP('',(#31288,#31289,#31290));
#7367=EDGE_LOOP('',(#31291,#31292,#31293,#31294));
#7368=EDGE_LOOP('',(#31295,#31296,#31297));
#7369=EDGE_LOOP('',(#31298,#31299,#31300,#31301));
#7370=EDGE_LOOP('',(#31302,#31303,#31304,#31305));
#7371=EDGE_LOOP('',(#31306,#31307,#31308,#31309));
#7372=EDGE_LOOP('',(#31310,#31311,#31312,#31313));
#7373=EDGE_LOOP('',(#31314,#31315,#31316,#31317));
#7374=EDGE_LOOP('',(#31318,#31319,#31320));
#7375=EDGE_LOOP('',(#31321,#31322,#31323,#31324));
#7376=EDGE_LOOP('',(#31325,#31326,#31327));
#7377=EDGE_LOOP('',(#31328,#31329,#31330,#31331));
#7378=EDGE_LOOP('',(#31332,#31333,#31334));
#7379=EDGE_LOOP('',(#31335,#31336,#31337,#31338));
#7380=EDGE_LOOP('',(#31339,#31340,#31341));
#7381=EDGE_LOOP('',(#31342,#31343,#31344,#31345));
#7382=EDGE_LOOP('',(#31346,#31347,#31348));
#7383=EDGE_LOOP('',(#31349,#31350,#31351,#31352));
#7384=EDGE_LOOP('',(#31353,#31354,#31355));
#7385=EDGE_LOOP('',(#31356,#31357,#31358,#31359));
#7386=EDGE_LOOP('',(#31360,#31361,#31362));
#7387=EDGE_LOOP('',(#31363,#31364,#31365,#31366));
#7388=EDGE_LOOP('',(#31367,#31368,#31369));
#7389=EDGE_LOOP('',(#31370,#31371,#31372,#31373));
#7390=EDGE_LOOP('',(#31374,#31375,#31376));
#7391=EDGE_LOOP('',(#31377,#31378,#31379,#31380));
#7392=EDGE_LOOP('',(#31381,#31382,#31383));
#7393=EDGE_LOOP('',(#31384,#31385,#31386,#31387));
#7394=EDGE_LOOP('',(#31388,#31389,#31390));
#7395=EDGE_LOOP('',(#31391,#31392,#31393,#31394));
#7396=EDGE_LOOP('',(#31395,#31396,#31397));
#7397=EDGE_LOOP('',(#31398,#31399,#31400,#31401));
#7398=EDGE_LOOP('',(#31402,#31403,#31404));
#7399=EDGE_LOOP('',(#31405,#31406,#31407,#31408));
#7400=EDGE_LOOP('',(#31409,#31410,#31411));
#7401=EDGE_LOOP('',(#31412,#31413,#31414,#31415));
#7402=EDGE_LOOP('',(#31416,#31417,#31418));
#7403=EDGE_LOOP('',(#31419,#31420,#31421,#31422));
#7404=EDGE_LOOP('',(#31423,#31424,#31425));
#7405=EDGE_LOOP('',(#31426,#31427,#31428,#31429));
#7406=EDGE_LOOP('',(#31430,#31431,#31432));
#7407=EDGE_LOOP('',(#31433,#31434,#31435,#31436));
#7408=EDGE_LOOP('',(#31437,#31438,#31439));
#7409=EDGE_LOOP('',(#31440,#31441,#31442,#31443));
#7410=EDGE_LOOP('',(#31444,#31445,#31446));
#7411=EDGE_LOOP('',(#31447,#31448,#31449,#31450));
#7412=EDGE_LOOP('',(#31451,#31452,#31453));
#7413=EDGE_LOOP('',(#31454,#31455,#31456,#31457));
#7414=EDGE_LOOP('',(#31458,#31459,#31460));
#7415=EDGE_LOOP('',(#31461,#31462,#31463,#31464));
#7416=EDGE_LOOP('',(#31465,#31466,#31467));
#7417=EDGE_LOOP('',(#31468,#31469,#31470,#31471));
#7418=EDGE_LOOP('',(#31472,#31473,#31474));
#7419=EDGE_LOOP('',(#31475,#31476,#31477,#31478));
#7420=EDGE_LOOP('',(#31479,#31480,#31481));
#7421=EDGE_LOOP('',(#31482,#31483,#31484,#31485));
#7422=EDGE_LOOP('',(#31486,#31487,#31488));
#7423=EDGE_LOOP('',(#31489,#31490,#31491,#31492));
#7424=EDGE_LOOP('',(#31493,#31494,#31495));
#7425=EDGE_LOOP('',(#31496,#31497,#31498,#31499));
#7426=EDGE_LOOP('',(#31500,#31501,#31502));
#7427=EDGE_LOOP('',(#31503,#31504,#31505,#31506));
#7428=EDGE_LOOP('',(#31507,#31508,#31509));
#7429=EDGE_LOOP('',(#31510,#31511,#31512,#31513));
#7430=EDGE_LOOP('',(#31514,#31515,#31516));
#7431=EDGE_LOOP('',(#31517,#31518,#31519,#31520));
#7432=EDGE_LOOP('',(#31521,#31522,#31523));
#7433=EDGE_LOOP('',(#31524,#31525,#31526,#31527));
#7434=EDGE_LOOP('',(#31528,#31529,#31530));
#7435=EDGE_LOOP('',(#31531,#31532,#31533,#31534));
#7436=EDGE_LOOP('',(#31535,#31536,#31537));
#7437=EDGE_LOOP('',(#31538,#31539,#31540,#31541));
#7438=EDGE_LOOP('',(#31542,#31543,#31544));
#7439=EDGE_LOOP('',(#31545,#31546,#31547,#31548));
#7440=EDGE_LOOP('',(#31549,#31550,#31551));
#7441=EDGE_LOOP('',(#31552,#31553,#31554,#31555));
#7442=EDGE_LOOP('',(#31556,#31557,#31558));
#7443=EDGE_LOOP('',(#31559,#31560,#31561,#31562));
#7444=EDGE_LOOP('',(#31563,#31564,#31565));
#7445=EDGE_LOOP('',(#31566,#31567,#31568,#31569,#31570,#31571,#31572,#31573,
#31574,#31575,#31576,#31577));
#7446=EDGE_LOOP('',(#31578,#31579,#31580,#31581));
#7447=EDGE_LOOP('',(#31582,#31583,#31584,#31585));
#7448=EDGE_LOOP('',(#31586,#31587,#31588,#31589));
#7449=EDGE_LOOP('',(#31590,#31591,#31592,#31593));
#7450=EDGE_LOOP('',(#31594,#31595,#31596,#31597));
#7451=EDGE_LOOP('',(#31598,#31599,#31600,#31601));
#7452=EDGE_LOOP('',(#31602,#31603,#31604,#31605));
#7453=EDGE_LOOP('',(#31606,#31607,#31608,#31609));
#7454=EDGE_LOOP('',(#31610,#31611,#31612,#31613));
#7455=EDGE_LOOP('',(#31614,#31615,#31616,#31617));
#7456=EDGE_LOOP('',(#31618,#31619,#31620,#31621));
#7457=EDGE_LOOP('',(#31622,#31623,#31624,#31625));
#7458=EDGE_LOOP('',(#31626,#31627,#31628,#31629));
#7459=EDGE_LOOP('',(#31630,#31631,#31632,#31633));
#7460=EDGE_LOOP('',(#31634,#31635,#31636,#31637));
#7461=EDGE_LOOP('',(#31638,#31639,#31640,#31641));
#7462=EDGE_LOOP('',(#31642,#31643,#31644,#31645));
#7463=EDGE_LOOP('',(#31646,#31647,#31648,#31649));
#7464=EDGE_LOOP('',(#31650,#31651,#31652,#31653));
#7465=EDGE_LOOP('',(#31654,#31655,#31656,#31657));
#7466=EDGE_LOOP('',(#31658,#31659,#31660,#31661));
#7467=EDGE_LOOP('',(#31662,#31663,#31664,#31665));
#7468=EDGE_LOOP('',(#31666,#31667,#31668,#31669));
#7469=EDGE_LOOP('',(#31670,#31671,#31672,#31673));
#7470=EDGE_LOOP('',(#31674,#31675,#31676,#31677));
#7471=EDGE_LOOP('',(#31678,#31679,#31680,#31681));
#7472=EDGE_LOOP('',(#31682,#31683,#31684,#31685));
#7473=EDGE_LOOP('',(#31686,#31687,#31688,#31689));
#7474=EDGE_LOOP('',(#31690,#31691,#31692,#31693));
#7475=EDGE_LOOP('',(#31694,#31695,#31696,#31697));
#7476=EDGE_LOOP('',(#31698,#31699,#31700,#31701));
#7477=EDGE_LOOP('',(#31702,#31703,#31704,#31705));
#7478=EDGE_LOOP('',(#31706,#31707,#31708,#31709));
#7479=EDGE_LOOP('',(#31710,#31711,#31712,#31713));
#7480=EDGE_LOOP('',(#31714,#31715,#31716,#31717));
#7481=EDGE_LOOP('',(#31718,#31719,#31720,#31721,#31722,#31723));
#10205=LINE('',#63097,#13255);
#10206=LINE('',#63130,#13256);
#10207=LINE('',#63214,#13257);
#10208=LINE('',#63304,#13258);
#10209=LINE('',#63394,#13259);
#10210=LINE('',#63478,#13260);
#10211=LINE('',#63568,#13261);
#10212=LINE('',#63652,#13262);
#10213=LINE('',#63739,#13263);
#10214=LINE('',#63829,#13264);
#10215=LINE('',#63913,#13265);
#10216=LINE('',#64003,#13266);
#10217=LINE('',#64093,#13267);
#10218=LINE('',#64177,#13268);
#10219=LINE('',#64267,#13269);
#10220=LINE('',#64354,#13270);
#10221=LINE('',#64441,#13271);
#10222=LINE('',#64531,#13272);
#10223=LINE('',#64615,#13273);
#10224=LINE('',#64705,#13274);
#10225=LINE('',#64795,#13275);
#10226=LINE('',#64879,#13276);
#10227=LINE('',#64969,#13277);
#10228=LINE('',#65056,#13278);
#10229=LINE('',#65143,#13279);
#10230=LINE('',#65233,#13280);
#10231=LINE('',#65317,#13281);
#10232=LINE('',#65407,#13282);
#10233=LINE('',#65497,#13283);
#10234=LINE('',#65581,#13284);
#10235=LINE('',#65591,#13285);
#10236=LINE('',#65627,#13286);
#10237=LINE('',#65664,#13287);
#10238=LINE('',#65702,#13288);
#10239=LINE('',#65739,#13289);
#10240=LINE('',#65776,#13290);
#10241=LINE('',#65814,#13291);
#10242=LINE('',#65850,#13292);
#10243=LINE('',#65888,#13293);
#10244=LINE('',#65925,#13294);
#10245=LINE('',#65962,#13295);
#10246=LINE('',#66000,#13296);
#10247=LINE('',#66037,#13297);
#10248=LINE('',#66074,#13298);
#10249=LINE('',#66112,#13299);
#10250=LINE('',#66148,#13300);
#10251=LINE('',#66186,#13301);
#10252=LINE('',#66223,#13302);
#10253=LINE('',#66260,#13303);
#10254=LINE('',#66298,#13304);
#10255=LINE('',#66335,#13305);
#10256=LINE('',#66372,#13306);
#10257=LINE('',#66410,#13307);
#10258=LINE('',#66447,#13308);
#10259=LINE('',#66484,#13309);
#10260=LINE('',#66521,#13310);
#10261=LINE('',#66558,#13311);
#10262=LINE('',#66596,#13312);
#10263=LINE('',#66634,#13313);
#10264=LINE('',#66640,#13314);
#10265=LINE('',#66654,#13315);
#10266=LINE('',#66660,#13316);
#10267=LINE('',#66662,#13317);
#10268=LINE('',#66663,#13318);
#10269=LINE('',#66670,#13319);
#10270=LINE('',#66672,#13320);
#10271=LINE('',#66678,#13321);
#10272=LINE('',#66686,#13322);
#10273=LINE('',#66704,#13323);
#10274=LINE('',#66705,#13324);
#10275=LINE('',#66706,#13325);
#10276=LINE('',#66708,#13326);
#10277=LINE('',#70186,#13327);
#10278=LINE('',#70188,#13328);
#10279=LINE('',#70190,#13329);
#10280=LINE('',#70191,#13330);
#10281=LINE('',#70195,#13331);
#10282=LINE('',#70198,#13332);
#10283=LINE('',#70199,#13333);
#10284=LINE('',#70205,#13334);
#10285=LINE('',#70207,#13335);
#10286=LINE('',#70209,#13336);
#10287=LINE('',#70210,#13337);
#10288=LINE('',#70214,#13338);
#10289=LINE('',#70217,#13339);
#10290=LINE('',#70218,#13340);
#10291=LINE('',#70224,#13341);
#10292=LINE('',#70226,#13342);
#10293=LINE('',#70228,#13343);
#10294=LINE('',#70229,#13344);
#10295=LINE('',#70233,#13345);
#10296=LINE('',#70236,#13346);
#10297=LINE('',#70237,#13347);
#10298=LINE('',#70243,#13348);
#10299=LINE('',#70245,#13349);
#10300=LINE('',#70247,#13350);
#10301=LINE('',#70248,#13351);
#10302=LINE('',#70252,#13352);
#10303=LINE('',#70255,#13353);
#10304=LINE('',#70256,#13354);
#10305=LINE('',#70262,#13355);
#10306=LINE('',#70264,#13356);
#10307=LINE('',#70266,#13357);
#10308=LINE('',#70267,#13358);
#10309=LINE('',#70271,#13359);
#10310=LINE('',#70274,#13360);
#10311=LINE('',#70275,#13361);
#10312=LINE('',#70281,#13362);
#10313=LINE('',#70283,#13363);
#10314=LINE('',#70285,#13364);
#10315=LINE('',#70286,#13365);
#10316=LINE('',#70290,#13366);
#10317=LINE('',#70293,#13367);
#10318=LINE('',#70294,#13368);
#10319=LINE('',#70300,#13369);
#10320=LINE('',#70302,#13370);
#10321=LINE('',#70304,#13371);
#10322=LINE('',#70305,#13372);
#10323=LINE('',#70309,#13373);
#10324=LINE('',#70312,#13374);
#10325=LINE('',#70313,#13375);
#10326=LINE('',#70319,#13376);
#10327=LINE('',#70321,#13377);
#10328=LINE('',#70323,#13378);
#10329=LINE('',#70324,#13379);
#10330=LINE('',#70328,#13380);
#10331=LINE('',#70331,#13381);
#10332=LINE('',#70332,#13382);
#10333=LINE('',#70338,#13383);
#10334=LINE('',#70340,#13384);
#10335=LINE('',#70342,#13385);
#10336=LINE('',#70343,#13386);
#10337=LINE('',#70347,#13387);
#10338=LINE('',#70350,#13388);
#10339=LINE('',#70351,#13389);
#10340=LINE('',#70357,#13390);
#10341=LINE('',#70359,#13391);
#10342=LINE('',#70361,#13392);
#10343=LINE('',#70362,#13393);
#10344=LINE('',#70366,#13394);
#10345=LINE('',#70369,#13395);
#10346=LINE('',#70370,#13396);
#10347=LINE('',#70376,#13397);
#10348=LINE('',#70378,#13398);
#10349=LINE('',#70380,#13399);
#10350=LINE('',#70381,#13400);
#10351=LINE('',#70385,#13401);
#10352=LINE('',#70388,#13402);
#10353=LINE('',#70389,#13403);
#10354=LINE('',#70395,#13404);
#10355=LINE('',#70397,#13405);
#10356=LINE('',#70399,#13406);
#10357=LINE('',#70400,#13407);
#10358=LINE('',#70404,#13408);
#10359=LINE('',#70407,#13409);
#10360=LINE('',#70408,#13410);
#10361=LINE('',#70414,#13411);
#10362=LINE('',#70416,#13412);
#10363=LINE('',#70418,#13413);
#10364=LINE('',#70419,#13414);
#10365=LINE('',#70423,#13415);
#10366=LINE('',#70426,#13416);
#10367=LINE('',#70427,#13417);
#10368=LINE('',#70433,#13418);
#10369=LINE('',#70435,#13419);
#10370=LINE('',#70437,#13420);
#10371=LINE('',#70438,#13421);
#10372=LINE('',#70442,#13422);
#10373=LINE('',#70445,#13423);
#10374=LINE('',#70446,#13424);
#10375=LINE('',#70452,#13425);
#10376=LINE('',#70454,#13426);
#10377=LINE('',#70456,#13427);
#10378=LINE('',#70457,#13428);
#10379=LINE('',#70461,#13429);
#10380=LINE('',#70464,#13430);
#10381=LINE('',#70465,#13431);
#10382=LINE('',#70471,#13432);
#10383=LINE('',#70473,#13433);
#10384=LINE('',#70475,#13434);
#10385=LINE('',#70476,#13435);
#10386=LINE('',#70480,#13436);
#10387=LINE('',#70483,#13437);
#10388=LINE('',#70484,#13438);
#10389=LINE('',#70490,#13439);
#10390=LINE('',#70492,#13440);
#10391=LINE('',#70494,#13441);
#10392=LINE('',#70495,#13442);
#10393=LINE('',#70499,#13443);
#10394=LINE('',#70502,#13444);
#10395=LINE('',#70503,#13445);
#10396=LINE('',#70509,#13446);
#10397=LINE('',#70511,#13447);
#10398=LINE('',#70513,#13448);
#10399=LINE('',#70514,#13449);
#10400=LINE('',#70519,#13450);
#10401=LINE('',#70523,#13451);
#10402=LINE('',#70524,#13452);
#10403=LINE('',#70532,#13453);
#10404=LINE('',#70534,#13454);
#10405=LINE('',#70536,#13455);
#10406=LINE('',#70537,#13456);
#10407=LINE('',#70541,#13457);
#10408=LINE('',#70544,#13458);
#10409=LINE('',#70545,#13459);
#10410=LINE('',#70551,#13460);
#10411=LINE('',#70553,#13461);
#10412=LINE('',#70555,#13462);
#10413=LINE('',#70556,#13463);
#10414=LINE('',#70560,#13464);
#10415=LINE('',#70563,#13465);
#10416=LINE('',#70564,#13466);
#10417=LINE('',#70570,#13467);
#10418=LINE('',#70572,#13468);
#10419=LINE('',#70574,#13469);
#10420=LINE('',#70575,#13470);
#10421=LINE('',#70579,#13471);
#10422=LINE('',#70582,#13472);
#10423=LINE('',#70583,#13473);
#10424=LINE('',#70589,#13474);
#10425=LINE('',#70591,#13475);
#10426=LINE('',#70593,#13476);
#10427=LINE('',#70594,#13477);
#10428=LINE('',#70598,#13478);
#10429=LINE('',#70601,#13479);
#10430=LINE('',#70602,#13480);
#10431=LINE('',#70608,#13481);
#10432=LINE('',#70610,#13482);
#10433=LINE('',#70612,#13483);
#10434=LINE('',#70613,#13484);
#10435=LINE('',#70617,#13485);
#10436=LINE('',#70620,#13486);
#10437=LINE('',#70621,#13487);
#10438=LINE('',#70627,#13488);
#10439=LINE('',#70629,#13489);
#10440=LINE('',#70631,#13490);
#10441=LINE('',#70632,#13491);
#10442=LINE('',#70636,#13492);
#10443=LINE('',#70639,#13493);
#10444=LINE('',#70640,#13494);
#10445=LINE('',#70646,#13495);
#10446=LINE('',#70648,#13496);
#10447=LINE('',#70650,#13497);
#10448=LINE('',#70651,#13498);
#10449=LINE('',#70655,#13499);
#10450=LINE('',#70658,#13500);
#10451=LINE('',#70659,#13501);
#10452=LINE('',#70665,#13502);
#10453=LINE('',#70667,#13503);
#10454=LINE('',#70669,#13504);
#10455=LINE('',#70670,#13505);
#10456=LINE('',#70674,#13506);
#10457=LINE('',#70677,#13507);
#10458=LINE('',#70678,#13508);
#10459=LINE('',#70684,#13509);
#10460=LINE('',#70686,#13510);
#10461=LINE('',#70688,#13511);
#10462=LINE('',#70689,#13512);
#10463=LINE('',#70693,#13513);
#10464=LINE('',#70696,#13514);
#10465=LINE('',#70697,#13515);
#10466=LINE('',#70703,#13516);
#10467=LINE('',#70705,#13517);
#10468=LINE('',#70707,#13518);
#10469=LINE('',#70708,#13519);
#10470=LINE('',#70712,#13520);
#10471=LINE('',#70715,#13521);
#10472=LINE('',#70716,#13522);
#10473=LINE('',#70722,#13523);
#10474=LINE('',#70724,#13524);
#10475=LINE('',#70726,#13525);
#10476=LINE('',#70727,#13526);
#10477=LINE('',#70731,#13527);
#10478=LINE('',#70734,#13528);
#10479=LINE('',#70735,#13529);
#10480=LINE('',#70741,#13530);
#10481=LINE('',#70743,#13531);
#10482=LINE('',#70745,#13532);
#10483=LINE('',#70746,#13533);
#10484=LINE('',#70750,#13534);
#10485=LINE('',#70753,#13535);
#10486=LINE('',#70754,#13536);
#10487=LINE('',#70760,#13537);
#10488=LINE('',#70762,#13538);
#10489=LINE('',#70764,#13539);
#10490=LINE('',#70765,#13540);
#10491=LINE('',#70769,#13541);
#10492=LINE('',#70772,#13542);
#10493=LINE('',#70773,#13543);
#10494=LINE('',#70779,#13544);
#10495=LINE('',#70781,#13545);
#10496=LINE('',#70783,#13546);
#10497=LINE('',#70784,#13547);
#10498=LINE('',#70788,#13548);
#10499=LINE('',#70791,#13549);
#10500=LINE('',#70792,#13550);
#10501=LINE('',#70798,#13551);
#10502=LINE('',#70800,#13552);
#10503=LINE('',#70802,#13553);
#10504=LINE('',#70803,#13554);
#10505=LINE('',#70807,#13555);
#10506=LINE('',#70810,#13556);
#10507=LINE('',#70811,#13557);
#10508=LINE('',#70817,#13558);
#10509=LINE('',#70819,#13559);
#10510=LINE('',#70821,#13560);
#10511=LINE('',#70822,#13561);
#10512=LINE('',#70826,#13562);
#10513=LINE('',#70829,#13563);
#10514=LINE('',#70830,#13564);
#10515=LINE('',#70836,#13565);
#10516=LINE('',#70838,#13566);
#10517=LINE('',#70840,#13567);
#10518=LINE('',#70841,#13568);
#10519=LINE('',#70845,#13569);
#10520=LINE('',#70848,#13570);
#10521=LINE('',#70849,#13571);
#10522=LINE('',#70855,#13572);
#10523=LINE('',#70857,#13573);
#10524=LINE('',#70859,#13574);
#10525=LINE('',#70860,#13575);
#10526=LINE('',#70864,#13576);
#10527=LINE('',#70867,#13577);
#10528=LINE('',#70868,#13578);
#10529=LINE('',#70874,#13579);
#10530=LINE('',#70875,#13580);
#10531=LINE('',#70877,#13581);
#13255=VECTOR('',#46144,6.35);
#13256=VECTOR('',#46149,6.35);
#13257=VECTOR('',#46152,6.35);
#13258=VECTOR('',#46155,6.35);
#13259=VECTOR('',#46158,6.35);
#13260=VECTOR('',#46161,6.35);
#13261=VECTOR('',#46164,6.35);
#13262=VECTOR('',#46167,6.35);
#13263=VECTOR('',#46170,6.35);
#13264=VECTOR('',#46173,6.35);
#13265=VECTOR('',#46176,6.35);
#13266=VECTOR('',#46179,6.35);
#13267=VECTOR('',#46182,6.35);
#13268=VECTOR('',#46185,6.35);
#13269=VECTOR('',#46188,6.35);
#13270=VECTOR('',#46191,6.35);
#13271=VECTOR('',#46194,6.35);
#13272=VECTOR('',#46197,6.35);
#13273=VECTOR('',#46200,6.35);
#13274=VECTOR('',#46203,6.35);
#13275=VECTOR('',#46206,6.35);
#13276=VECTOR('',#46209,6.35);
#13277=VECTOR('',#46212,6.35);
#13278=VECTOR('',#46215,6.35);
#13279=VECTOR('',#46218,6.35);
#13280=VECTOR('',#46221,6.35);
#13281=VECTOR('',#46224,6.35);
#13282=VECTOR('',#46227,6.35);
#13283=VECTOR('',#46230,6.35);
#13284=VECTOR('',#46233,5.57784);
#13285=VECTOR('',#46238,5.57784);
#13286=VECTOR('',#46243,5.57784);
#13287=VECTOR('',#46246,5.57784);
#13288=VECTOR('',#46249,5.57784);
#13289=VECTOR('',#46252,5.57784);
#13290=VECTOR('',#46255,5.57784);
#13291=VECTOR('',#46258,5.57784);
#13292=VECTOR('',#46261,5.57784);
#13293=VECTOR('',#46264,5.57784);
#13294=VECTOR('',#46267,5.57784);
#13295=VECTOR('',#46270,5.57784);
#13296=VECTOR('',#46273,5.57784);
#13297=VECTOR('',#46276,5.57784);
#13298=VECTOR('',#46279,5.57784);
#13299=VECTOR('',#46282,5.57784);
#13300=VECTOR('',#46285,5.57784);
#13301=VECTOR('',#46288,5.57784);
#13302=VECTOR('',#46291,5.57784);
#13303=VECTOR('',#46294,5.57784);
#13304=VECTOR('',#46297,5.57784);
#13305=VECTOR('',#46300,5.57784);
#13306=VECTOR('',#46303,5.57784);
#13307=VECTOR('',#46306,5.57784);
#13308=VECTOR('',#46309,5.57784);
#13309=VECTOR('',#46312,5.57784);
#13310=VECTOR('',#46315,5.57784);
#13311=VECTOR('',#46318,5.57784);
#13312=VECTOR('',#46321,5.57784);
#13313=VECTOR('',#46326,5.47677669529664);
#13314=VECTOR('',#46333,5.95);
#13315=VECTOR('',#46344,10.);
#13316=VECTOR('',#46345,10.);
#13317=VECTOR('',#46346,10.);
#13318=VECTOR('',#46347,10.);
#13319=VECTOR('',#46356,10.);
#13320=VECTOR('',#46357,10.);
#13321=VECTOR('',#46358,10.);
#13322=VECTOR('',#46363,10.);
#13323=VECTOR('',#46372,10.);
#13324=VECTOR('',#46373,10.);
#13325=VECTOR('',#46374,10.);
#13326=VECTOR('',#46377,10.);
#13327=VECTOR('',#46400,10.);
#13328=VECTOR('',#46401,10.);
#13329=VECTOR('',#46402,10.);
#13330=VECTOR('',#46403,10.);
#13331=VECTOR('',#46408,10.);
#13332=VECTOR('',#46411,10.);
#13333=VECTOR('',#46412,10.);
#13334=VECTOR('',#46419,10.);
#13335=VECTOR('',#46420,10.);
#13336=VECTOR('',#46421,10.);
#13337=VECTOR('',#46422,10.);
#13338=VECTOR('',#46427,10.);
#13339=VECTOR('',#46430,10.);
#13340=VECTOR('',#46431,10.);
#13341=VECTOR('',#46438,10.);
#13342=VECTOR('',#46439,10.);
#13343=VECTOR('',#46440,10.);
#13344=VECTOR('',#46441,10.);
#13345=VECTOR('',#46446,10.);
#13346=VECTOR('',#46449,10.);
#13347=VECTOR('',#46450,10.);
#13348=VECTOR('',#46457,10.);
#13349=VECTOR('',#46458,10.);
#13350=VECTOR('',#46459,10.);
#13351=VECTOR('',#46460,10.);
#13352=VECTOR('',#46465,10.);
#13353=VECTOR('',#46468,10.);
#13354=VECTOR('',#46469,10.);
#13355=VECTOR('',#46476,10.);
#13356=VECTOR('',#46477,10.);
#13357=VECTOR('',#46478,10.);
#13358=VECTOR('',#46479,10.);
#13359=VECTOR('',#46484,10.);
#13360=VECTOR('',#46487,10.);
#13361=VECTOR('',#46488,10.);
#13362=VECTOR('',#46495,10.);
#13363=VECTOR('',#46496,10.);
#13364=VECTOR('',#46497,10.);
#13365=VECTOR('',#46498,10.);
#13366=VECTOR('',#46503,10.);
#13367=VECTOR('',#46506,10.);
#13368=VECTOR('',#46507,10.);
#13369=VECTOR('',#46514,10.);
#13370=VECTOR('',#46515,10.);
#13371=VECTOR('',#46516,10.);
#13372=VECTOR('',#46517,10.);
#13373=VECTOR('',#46522,10.);
#13374=VECTOR('',#46525,10.);
#13375=VECTOR('',#46526,10.);
#13376=VECTOR('',#46533,10.);
#13377=VECTOR('',#46534,10.);
#13378=VECTOR('',#46535,10.);
#13379=VECTOR('',#46536,10.);
#13380=VECTOR('',#46541,10.);
#13381=VECTOR('',#46544,10.);
#13382=VECTOR('',#46545,10.);
#13383=VECTOR('',#46552,10.);
#13384=VECTOR('',#46553,10.);
#13385=VECTOR('',#46554,10.);
#13386=VECTOR('',#46555,10.);
#13387=VECTOR('',#46560,10.);
#13388=VECTOR('',#46563,10.);
#13389=VECTOR('',#46564,10.);
#13390=VECTOR('',#46571,10.);
#13391=VECTOR('',#46572,10.);
#13392=VECTOR('',#46573,10.);
#13393=VECTOR('',#46574,10.);
#13394=VECTOR('',#46579,10.);
#13395=VECTOR('',#46582,10.);
#13396=VECTOR('',#46583,10.);
#13397=VECTOR('',#46590,10.);
#13398=VECTOR('',#46591,10.);
#13399=VECTOR('',#46592,10.);
#13400=VECTOR('',#46593,10.);
#13401=VECTOR('',#46598,10.);
#13402=VECTOR('',#46601,10.);
#13403=VECTOR('',#46602,10.);
#13404=VECTOR('',#46609,10.);
#13405=VECTOR('',#46610,10.);
#13406=VECTOR('',#46611,10.);
#13407=VECTOR('',#46612,10.);
#13408=VECTOR('',#46617,10.);
#13409=VECTOR('',#46620,10.);
#13410=VECTOR('',#46621,10.);
#13411=VECTOR('',#46628,10.);
#13412=VECTOR('',#46629,10.);
#13413=VECTOR('',#46630,10.);
#13414=VECTOR('',#46631,10.);
#13415=VECTOR('',#46636,10.);
#13416=VECTOR('',#46639,10.);
#13417=VECTOR('',#46640,10.);
#13418=VECTOR('',#46647,10.);
#13419=VECTOR('',#46648,10.);
#13420=VECTOR('',#46649,10.);
#13421=VECTOR('',#46650,10.);
#13422=VECTOR('',#46655,10.);
#13423=VECTOR('',#46658,10.);
#13424=VECTOR('',#46659,10.);
#13425=VECTOR('',#46666,10.);
#13426=VECTOR('',#46667,10.);
#13427=VECTOR('',#46668,10.);
#13428=VECTOR('',#46669,10.);
#13429=VECTOR('',#46674,10.);
#13430=VECTOR('',#46677,10.);
#13431=VECTOR('',#46678,10.);
#13432=VECTOR('',#46685,10.);
#13433=VECTOR('',#46686,10.);
#13434=VECTOR('',#46687,10.);
#13435=VECTOR('',#46688,10.);
#13436=VECTOR('',#46693,10.);
#13437=VECTOR('',#46696,10.);
#13438=VECTOR('',#46697,10.);
#13439=VECTOR('',#46704,10.);
#13440=VECTOR('',#46705,10.);
#13441=VECTOR('',#46706,10.);
#13442=VECTOR('',#46707,10.);
#13443=VECTOR('',#46712,10.);
#13444=VECTOR('',#46715,10.);
#13445=VECTOR('',#46716,10.);
#13446=VECTOR('',#46723,10.);
#13447=VECTOR('',#46724,10.);
#13448=VECTOR('',#46725,10.);
#13449=VECTOR('',#46726,10.);
#13450=VECTOR('',#46731,10.);
#13451=VECTOR('',#46736,10.);
#13452=VECTOR('',#46737,10.);
#13453=VECTOR('',#46746,10.);
#13454=VECTOR('',#46747,10.);
#13455=VECTOR('',#46748,10.);
#13456=VECTOR('',#46749,10.);
#13457=VECTOR('',#46754,10.);
#13458=VECTOR('',#46757,10.);
#13459=VECTOR('',#46758,10.);
#13460=VECTOR('',#46765,10.);
#13461=VECTOR('',#46766,10.);
#13462=VECTOR('',#46767,10.);
#13463=VECTOR('',#46768,10.);
#13464=VECTOR('',#46773,10.);
#13465=VECTOR('',#46776,10.);
#13466=VECTOR('',#46777,10.);
#13467=VECTOR('',#46784,10.);
#13468=VECTOR('',#46785,10.);
#13469=VECTOR('',#46786,10.);
#13470=VECTOR('',#46787,10.);
#13471=VECTOR('',#46792,10.);
#13472=VECTOR('',#46795,10.);
#13473=VECTOR('',#46796,10.);
#13474=VECTOR('',#46803,10.);
#13475=VECTOR('',#46804,10.);
#13476=VECTOR('',#46805,10.);
#13477=VECTOR('',#46806,10.);
#13478=VECTOR('',#46811,10.);
#13479=VECTOR('',#46814,10.);
#13480=VECTOR('',#46815,10.);
#13481=VECTOR('',#46822,10.);
#13482=VECTOR('',#46823,10.);
#13483=VECTOR('',#46824,10.);
#13484=VECTOR('',#46825,10.);
#13485=VECTOR('',#46830,10.);
#13486=VECTOR('',#46833,10.);
#13487=VECTOR('',#46834,10.);
#13488=VECTOR('',#46841,10.);
#13489=VECTOR('',#46842,10.);
#13490=VECTOR('',#46843,10.);
#13491=VECTOR('',#46844,10.);
#13492=VECTOR('',#46849,10.);
#13493=VECTOR('',#46852,10.);
#13494=VECTOR('',#46853,10.);
#13495=VECTOR('',#46860,10.);
#13496=VECTOR('',#46861,10.);
#13497=VECTOR('',#46862,10.);
#13498=VECTOR('',#46863,10.);
#13499=VECTOR('',#46868,10.);
#13500=VECTOR('',#46871,10.);
#13501=VECTOR('',#46872,10.);
#13502=VECTOR('',#46879,10.);
#13503=VECTOR('',#46880,10.);
#13504=VECTOR('',#46881,10.);
#13505=VECTOR('',#46882,10.);
#13506=VECTOR('',#46887,10.);
#13507=VECTOR('',#46890,10.);
#13508=VECTOR('',#46891,10.);
#13509=VECTOR('',#46898,10.);
#13510=VECTOR('',#46899,10.);
#13511=VECTOR('',#46900,10.);
#13512=VECTOR('',#46901,10.);
#13513=VECTOR('',#46906,10.);
#13514=VECTOR('',#46909,10.);
#13515=VECTOR('',#46910,10.);
#13516=VECTOR('',#46917,10.);
#13517=VECTOR('',#46918,10.);
#13518=VECTOR('',#46919,10.);
#13519=VECTOR('',#46920,10.);
#13520=VECTOR('',#46925,10.);
#13521=VECTOR('',#46928,10.);
#13522=VECTOR('',#46929,10.);
#13523=VECTOR('',#46936,10.);
#13524=VECTOR('',#46937,10.);
#13525=VECTOR('',#46938,10.);
#13526=VECTOR('',#46939,10.);
#13527=VECTOR('',#46944,10.);
#13528=VECTOR('',#46947,10.);
#13529=VECTOR('',#46948,10.);
#13530=VECTOR('',#46955,10.);
#13531=VECTOR('',#46956,10.);
#13532=VECTOR('',#46957,10.);
#13533=VECTOR('',#46958,10.);
#13534=VECTOR('',#46963,10.);
#13535=VECTOR('',#46966,10.);
#13536=VECTOR('',#46967,10.);
#13537=VECTOR('',#46974,10.);
#13538=VECTOR('',#46975,10.);
#13539=VECTOR('',#46976,10.);
#13540=VECTOR('',#46977,10.);
#13541=VECTOR('',#46982,10.);
#13542=VECTOR('',#46985,10.);
#13543=VECTOR('',#46986,10.);
#13544=VECTOR('',#46993,10.);
#13545=VECTOR('',#46994,10.);
#13546=VECTOR('',#46995,10.);
#13547=VECTOR('',#46996,10.);
#13548=VECTOR('',#47001,10.);
#13549=VECTOR('',#47004,10.);
#13550=VECTOR('',#47005,10.);
#13551=VECTOR('',#47012,10.);
#13552=VECTOR('',#47013,10.);
#13553=VECTOR('',#47014,10.);
#13554=VECTOR('',#47015,10.);
#13555=VECTOR('',#47020,10.);
#13556=VECTOR('',#47023,10.);
#13557=VECTOR('',#47024,10.);
#13558=VECTOR('',#47031,10.);
#13559=VECTOR('',#47032,10.);
#13560=VECTOR('',#47033,10.);
#13561=VECTOR('',#47034,10.);
#13562=VECTOR('',#47039,10.);
#13563=VECTOR('',#47042,10.);
#13564=VECTOR('',#47043,10.);
#13565=VECTOR('',#47050,10.);
#13566=VECTOR('',#47051,10.);
#13567=VECTOR('',#47052,10.);
#13568=VECTOR('',#47053,10.);
#13569=VECTOR('',#47058,10.);
#13570=VECTOR('',#47061,10.);
#13571=VECTOR('',#47062,10.);
#13572=VECTOR('',#47069,10.);
#13573=VECTOR('',#47070,10.);
#13574=VECTOR('',#47071,10.);
#13575=VECTOR('',#47072,10.);
#13576=VECTOR('',#47077,10.);
#13577=VECTOR('',#47080,10.);
#13578=VECTOR('',#47081,10.);
#13579=VECTOR('',#47090,7.17);
#13580=VECTOR('',#47091,7.17);
#13581=VECTOR('',#47094,6.76);
#14427=CIRCLE('',#37271,6.28269);
#14428=CIRCLE('',#37301,5.57784);
#14429=CIRCLE('',#37303,5.57784);
#14430=CIRCLE('',#37332,5.05);
#14431=CIRCLE('',#37333,5.90355339059328);
#14432=CIRCLE('',#37334,5.90355339059328);
#14433=CIRCLE('',#37336,6.28269);
#14434=CIRCLE('',#37337,6.28269);
#14435=CIRCLE('',#37338,6.28269);
#14436=CIRCLE('',#37342,10.4);
#14437=CIRCLE('',#37343,7.17);
#14438=CIRCLE('',#37346,11.);
#14439=CIRCLE('',#37347,11.);
#14440=CIRCLE('',#37349,10.4);
#14441=CIRCLE('',#37357,6.28269);
#14442=CIRCLE('',#37358,6.28269);
#14443=CIRCLE('',#37359,5.57784);
#14444=CIRCLE('',#37364,7.17);
#14445=CIRCLE('',#37367,7.17);
#14446=CIRCLE('',#37370,7.17);
#14447=CIRCLE('',#37373,7.17);
#14448=CIRCLE('',#37376,7.17);
#14449=CIRCLE('',#37379,7.17);
#14450=CIRCLE('',#37382,7.17);
#14451=CIRCLE('',#37385,7.17);
#14452=CIRCLE('',#37388,7.17);
#14453=CIRCLE('',#37391,7.17);
#14454=CIRCLE('',#37394,7.17);
#14455=CIRCLE('',#37397,7.17);
#14456=CIRCLE('',#37400,7.17);
#14457=CIRCLE('',#37403,7.17);
#14458=CIRCLE('',#37406,7.17);
#14459=CIRCLE('',#37409,7.17);
#14460=CIRCLE('',#37412,7.17);
#14461=CIRCLE('',#37415,7.17);
#14462=CIRCLE('',#37418,7.17);
#14463=CIRCLE('',#37421,7.17);
#14464=CIRCLE('',#37424,7.17);
#14465=CIRCLE('',#37427,7.17);
#14466=CIRCLE('',#37430,7.17);
#14467=CIRCLE('',#37433,7.17);
#14468=CIRCLE('',#37436,7.17);
#14469=CIRCLE('',#37439,7.17);
#14470=CIRCLE('',#37442,7.17);
#14471=CIRCLE('',#37445,7.17);
#14472=CIRCLE('',#37448,7.17);
#14473=CIRCLE('',#37451,7.17);
#14474=CIRCLE('',#37454,7.17);
#14475=CIRCLE('',#37457,7.17);
#14476=CIRCLE('',#37460,7.17);
#14477=CIRCLE('',#37463,7.17);
#14478=CIRCLE('',#37466,7.17);
#14479=CIRCLE('',#37467,7.17);
#14480=CIRCLE('',#37470,7.17);
#14481=CIRCLE('',#37471,7.17);
#14482=CIRCLE('',#37474,7.17);
#14483=CIRCLE('',#37477,7.17);
#14484=CIRCLE('',#37480,7.17);
#14485=CIRCLE('',#37483,7.17);
#14486=CIRCLE('',#37486,7.17);
#14487=CIRCLE('',#37489,7.17);
#14488=CIRCLE('',#37492,7.17);
#14489=CIRCLE('',#37495,7.17);
#14490=CIRCLE('',#37498,7.17);
#14491=CIRCLE('',#37501,7.17);
#14492=CIRCLE('',#37504,7.17);
#14493=CIRCLE('',#37507,7.17);
#14494=CIRCLE('',#37510,7.17);
#14495=CIRCLE('',#37513,7.17);
#14496=CIRCLE('',#37516,7.17);
#14497=CIRCLE('',#37519,7.17);
#14498=CIRCLE('',#37522,7.17);
#14499=CIRCLE('',#37525,7.17);
#14500=CIRCLE('',#37528,7.17);
#14501=CIRCLE('',#37531,7.17);
#14502=CIRCLE('',#37534,7.17);
#14503=CIRCLE('',#37537,7.17);
#14504=CIRCLE('',#37540,7.17);
#14505=CIRCLE('',#37543,7.17);
#14506=CIRCLE('',#37546,7.17);
#14507=CIRCLE('',#37549,7.17);
#14508=CIRCLE('',#37552,7.17);
#14509=CIRCLE('',#37555,7.17);
#14510=CIRCLE('',#37558,7.17);
#14511=CIRCLE('',#37561,7.17);
#14512=CIRCLE('',#37564,7.17);
#14513=CIRCLE('',#37567,7.17);
#14514=CIRCLE('',#37570,7.17);
#14515=CIRCLE('',#37573,7.17);
#14516=CIRCLE('',#37576,7.17);
#14517=CIRCLE('',#37579,7.17);
#14518=CIRCLE('',#37581,7.17);
#17032=VERTEX_POINT('',#63095);
#17033=VERTEX_POINT('',#63096);
#17034=VERTEX_POINT('',#63098);
#17035=VERTEX_POINT('',#63115);
#17036=VERTEX_POINT('',#63128);
#17037=VERTEX_POINT('',#63129);
#17038=VERTEX_POINT('',#63212);
#17039=VERTEX_POINT('',#63213);
#17040=VERTEX_POINT('',#63302);
#17041=VERTEX_POINT('',#63303);
#17042=VERTEX_POINT('',#63392);
#17043=VERTEX_POINT('',#63393);
#17044=VERTEX_POINT('',#63476);
#17045=VERTEX_POINT('',#63477);
#17046=VERTEX_POINT('',#63566);
#17047=VERTEX_POINT('',#63567);
#17048=VERTEX_POINT('',#63650);
#17049=VERTEX_POINT('',#63651);
#17050=VERTEX_POINT('',#63737);
#17051=VERTEX_POINT('',#63738);
#17052=VERTEX_POINT('',#63827);
#17053=VERTEX_POINT('',#63828);
#17054=VERTEX_POINT('',#63911);
#17055=VERTEX_POINT('',#63912);
#17056=VERTEX_POINT('',#64001);
#17057=VERTEX_POINT('',#64002);
#17058=VERTEX_POINT('',#64091);
#17059=VERTEX_POINT('',#64092);
#17060=VERTEX_POINT('',#64175);
#17061=VERTEX_POINT('',#64176);
#17062=VERTEX_POINT('',#64265);
#17063=VERTEX_POINT('',#64266);
#17064=VERTEX_POINT('',#64352);
#17065=VERTEX_POINT('',#64353);
#17066=VERTEX_POINT('',#64439);
#17067=VERTEX_POINT('',#64440);
#17068=VERTEX_POINT('',#64529);
#17069=VERTEX_POINT('',#64530);
#17070=VERTEX_POINT('',#64613);
#17071=VERTEX_POINT('',#64614);
#17072=VERTEX_POINT('',#64703);
#17073=VERTEX_POINT('',#64704);
#17074=VERTEX_POINT('',#64793);
#17075=VERTEX_POINT('',#64794);
#17076=VERTEX_POINT('',#64877);
#17077=VERTEX_POINT('',#64878);
#17078=VERTEX_POINT('',#64967);
#17079=VERTEX_POINT('',#64968);
#17080=VERTEX_POINT('',#65054);
#17081=VERTEX_POINT('',#65055);
#17082=VERTEX_POINT('',#65141);
#17083=VERTEX_POINT('',#65142);
#17084=VERTEX_POINT('',#65231);
#17085=VERTEX_POINT('',#65232);
#17086=VERTEX_POINT('',#65315);
#17087=VERTEX_POINT('',#65316);
#17088=VERTEX_POINT('',#65405);
#17089=VERTEX_POINT('',#65406);
#17090=VERTEX_POINT('',#65495);
#17091=VERTEX_POINT('',#65496);
#17092=VERTEX_POINT('',#65579);
#17093=VERTEX_POINT('',#65580);
#17094=VERTEX_POINT('',#65582);
#17095=VERTEX_POINT('',#65589);
#17096=VERTEX_POINT('',#65590);
#17097=VERTEX_POINT('',#65608);
#17098=VERTEX_POINT('',#65625);
#17099=VERTEX_POINT('',#65626);
#17100=VERTEX_POINT('',#65662);
#17101=VERTEX_POINT('',#65663);
#17102=VERTEX_POINT('',#65700);
#17103=VERTEX_POINT('',#65701);
#17104=VERTEX_POINT('',#65737);
#17105=VERTEX_POINT('',#65738);
#17106=VERTEX_POINT('',#65774);
#17107=VERTEX_POINT('',#65775);
#17108=VERTEX_POINT('',#65812);
#17109=VERTEX_POINT('',#65813);
#17110=VERTEX_POINT('',#65848);
#17111=VERTEX_POINT('',#65849);
#17112=VERTEX_POINT('',#65886);
#17113=VERTEX_POINT('',#65887);
#17114=VERTEX_POINT('',#65923);
#17115=VERTEX_POINT('',#65924);
#17116=VERTEX_POINT('',#65960);
#17117=VERTEX_POINT('',#65961);
#17118=VERTEX_POINT('',#65998);
#17119=VERTEX_POINT('',#65999);
#17120=VERTEX_POINT('',#66035);
#17121=VERTEX_POINT('',#66036);
#17122=VERTEX_POINT('',#66072);
#17123=VERTEX_POINT('',#66073);
#17124=VERTEX_POINT('',#66110);
#17125=VERTEX_POINT('',#66111);
#17126=VERTEX_POINT('',#66146);
#17127=VERTEX_POINT('',#66147);
#17128=VERTEX_POINT('',#66184);
#17129=VERTEX_POINT('',#66185);
#17130=VERTEX_POINT('',#66221);
#17131=VERTEX_POINT('',#66222);
#17132=VERTEX_POINT('',#66258);
#17133=VERTEX_POINT('',#66259);
#17134=VERTEX_POINT('',#66296);
#17135=VERTEX_POINT('',#66297);
#17136=VERTEX_POINT('',#66333);
#17137=VERTEX_POINT('',#66334);
#17138=VERTEX_POINT('',#66370);
#17139=VERTEX_POINT('',#66371);
#17140=VERTEX_POINT('',#66408);
#17141=VERTEX_POINT('',#66409);
#17142=VERTEX_POINT('',#66445);
#17143=VERTEX_POINT('',#66446);
#17144=VERTEX_POINT('',#66482);
#17145=VERTEX_POINT('',#66483);
#17146=VERTEX_POINT('',#66519);
#17147=VERTEX_POINT('',#66520);
#17148=VERTEX_POINT('',#66556);
#17149=VERTEX_POINT('',#66557);
#17150=VERTEX_POINT('',#66594);
#17151=VERTEX_POINT('',#66595);
#17152=VERTEX_POINT('',#66631);
#17153=VERTEX_POINT('',#66633);
#17154=VERTEX_POINT('',#66635);
#17155=VERTEX_POINT('',#66639);
#17156=VERTEX_POINT('',#66641);
#17157=VERTEX_POINT('',#66643);
#17158=VERTEX_POINT('',#66648);
#17159=VERTEX_POINT('',#66649);
#17160=VERTEX_POINT('',#66653);
#17161=VERTEX_POINT('',#66655);
#17162=VERTEX_POINT('',#66659);
#17163=VERTEX_POINT('',#66661);
#17164=VERTEX_POINT('',#66666);
#17165=VERTEX_POINT('',#66669);
#17166=VERTEX_POINT('',#66671);
#17167=VERTEX_POINT('',#66673);
#17168=VERTEX_POINT('',#66677);
#17169=VERTEX_POINT('',#66683);
#17170=VERTEX_POINT('',#66685);
#17171=VERTEX_POINT('',#66689);
#17172=VERTEX_POINT('',#66693);
#17173=VERTEX_POINT('',#66695);
#17174=VERTEX_POINT('',#66703);
#17175=VERTEX_POINT('',#68435);
#17176=VERTEX_POINT('',#68560);
#17177=VERTEX_POINT('',#68563);
#17178=VERTEX_POINT('',#70184);
#17179=VERTEX_POINT('',#70185);
#17180=VERTEX_POINT('',#70187);
#17181=VERTEX_POINT('',#70189);
#17182=VERTEX_POINT('',#70193);
#17183=VERTEX_POINT('',#70197);
#17184=VERTEX_POINT('',#70203);
#17185=VERTEX_POINT('',#70204);
#17186=VERTEX_POINT('',#70206);
#17187=VERTEX_POINT('',#70208);
#17188=VERTEX_POINT('',#70212);
#17189=VERTEX_POINT('',#70216);
#17190=VERTEX_POINT('',#70222);
#17191=VERTEX_POINT('',#70223);
#17192=VERTEX_POINT('',#70225);
#17193=VERTEX_POINT('',#70227);
#17194=VERTEX_POINT('',#70231);
#17195=VERTEX_POINT('',#70235);
#17196=VERTEX_POINT('',#70241);
#17197=VERTEX_POINT('',#70242);
#17198=VERTEX_POINT('',#70244);
#17199=VERTEX_POINT('',#70246);
#17200=VERTEX_POINT('',#70250);
#17201=VERTEX_POINT('',#70254);
#17202=VERTEX_POINT('',#70260);
#17203=VERTEX_POINT('',#70261);
#17204=VERTEX_POINT('',#70263);
#17205=VERTEX_POINT('',#70265);
#17206=VERTEX_POINT('',#70269);
#17207=VERTEX_POINT('',#70273);
#17208=VERTEX_POINT('',#70279);
#17209=VERTEX_POINT('',#70280);
#17210=VERTEX_POINT('',#70282);
#17211=VERTEX_POINT('',#70284);
#17212=VERTEX_POINT('',#70288);
#17213=VERTEX_POINT('',#70292);
#17214=VERTEX_POINT('',#70298);
#17215=VERTEX_POINT('',#70299);
#17216=VERTEX_POINT('',#70301);
#17217=VERTEX_POINT('',#70303);
#17218=VERTEX_POINT('',#70307);
#17219=VERTEX_POINT('',#70311);
#17220=VERTEX_POINT('',#70317);
#17221=VERTEX_POINT('',#70318);
#17222=VERTEX_POINT('',#70320);
#17223=VERTEX_POINT('',#70322);
#17224=VERTEX_POINT('',#70326);
#17225=VERTEX_POINT('',#70330);
#17226=VERTEX_POINT('',#70336);
#17227=VERTEX_POINT('',#70337);
#17228=VERTEX_POINT('',#70339);
#17229=VERTEX_POINT('',#70341);
#17230=VERTEX_POINT('',#70345);
#17231=VERTEX_POINT('',#70349);
#17232=VERTEX_POINT('',#70355);
#17233=VERTEX_POINT('',#70356);
#17234=VERTEX_POINT('',#70358);
#17235=VERTEX_POINT('',#70360);
#17236=VERTEX_POINT('',#70364);
#17237=VERTEX_POINT('',#70368);
#17238=VERTEX_POINT('',#70374);
#17239=VERTEX_POINT('',#70375);
#17240=VERTEX_POINT('',#70377);
#17241=VERTEX_POINT('',#70379);
#17242=VERTEX_POINT('',#70383);
#17243=VERTEX_POINT('',#70387);
#17244=VERTEX_POINT('',#70393);
#17245=VERTEX_POINT('',#70394);
#17246=VERTEX_POINT('',#70396);
#17247=VERTEX_POINT('',#70398);
#17248=VERTEX_POINT('',#70402);
#17249=VERTEX_POINT('',#70406);
#17250=VERTEX_POINT('',#70412);
#17251=VERTEX_POINT('',#70413);
#17252=VERTEX_POINT('',#70415);
#17253=VERTEX_POINT('',#70417);
#17254=VERTEX_POINT('',#70421);
#17255=VERTEX_POINT('',#70425);
#17256=VERTEX_POINT('',#70431);
#17257=VERTEX_POINT('',#70432);
#17258=VERTEX_POINT('',#70434);
#17259=VERTEX_POINT('',#70436);
#17260=VERTEX_POINT('',#70440);
#17261=VERTEX_POINT('',#70444);
#17262=VERTEX_POINT('',#70450);
#17263=VERTEX_POINT('',#70451);
#17264=VERTEX_POINT('',#70453);
#17265=VERTEX_POINT('',#70455);
#17266=VERTEX_POINT('',#70459);
#17267=VERTEX_POINT('',#70463);
#17268=VERTEX_POINT('',#70469);
#17269=VERTEX_POINT('',#70470);
#17270=VERTEX_POINT('',#70472);
#17271=VERTEX_POINT('',#70474);
#17272=VERTEX_POINT('',#70478);
#17273=VERTEX_POINT('',#70482);
#17274=VERTEX_POINT('',#70488);
#17275=VERTEX_POINT('',#70489);
#17276=VERTEX_POINT('',#70491);
#17277=VERTEX_POINT('',#70493);
#17278=VERTEX_POINT('',#70497);
#17279=VERTEX_POINT('',#70501);
#17280=VERTEX_POINT('',#70507);
#17281=VERTEX_POINT('',#70508);
#17282=VERTEX_POINT('',#70510);
#17283=VERTEX_POINT('',#70512);
#17284=VERTEX_POINT('',#70516);
#17285=VERTEX_POINT('',#70518);
#17286=VERTEX_POINT('',#70522);
#17287=VERTEX_POINT('',#70526);
#17288=VERTEX_POINT('',#70530);
#17289=VERTEX_POINT('',#70531);
#17290=VERTEX_POINT('',#70533);
#17291=VERTEX_POINT('',#70535);
#17292=VERTEX_POINT('',#70539);
#17293=VERTEX_POINT('',#70543);
#17294=VERTEX_POINT('',#70549);
#17295=VERTEX_POINT('',#70550);
#17296=VERTEX_POINT('',#70552);
#17297=VERTEX_POINT('',#70554);
#17298=VERTEX_POINT('',#70558);
#17299=VERTEX_POINT('',#70562);
#17300=VERTEX_POINT('',#70568);
#17301=VERTEX_POINT('',#70569);
#17302=VERTEX_POINT('',#70571);
#17303=VERTEX_POINT('',#70573);
#17304=VERTEX_POINT('',#70577);
#17305=VERTEX_POINT('',#70581);
#17306=VERTEX_POINT('',#70587);
#17307=VERTEX_POINT('',#70588);
#17308=VERTEX_POINT('',#70590);
#17309=VERTEX_POINT('',#70592);
#17310=VERTEX_POINT('',#70596);
#17311=VERTEX_POINT('',#70600);
#17312=VERTEX_POINT('',#70606);
#17313=VERTEX_POINT('',#70607);
#17314=VERTEX_POINT('',#70609);
#17315=VERTEX_POINT('',#70611);
#17316=VERTEX_POINT('',#70615);
#17317=VERTEX_POINT('',#70619);
#17318=VERTEX_POINT('',#70625);
#17319=VERTEX_POINT('',#70626);
#17320=VERTEX_POINT('',#70628);
#17321=VERTEX_POINT('',#70630);
#17322=VERTEX_POINT('',#70634);
#17323=VERTEX_POINT('',#70638);
#17324=VERTEX_POINT('',#70644);
#17325=VERTEX_POINT('',#70645);
#17326=VERTEX_POINT('',#70647);
#17327=VERTEX_POINT('',#70649);
#17328=VERTEX_POINT('',#70653);
#17329=VERTEX_POINT('',#70657);
#17330=VERTEX_POINT('',#70663);
#17331=VERTEX_POINT('',#70664);
#17332=VERTEX_POINT('',#70666);
#17333=VERTEX_POINT('',#70668);
#17334=VERTEX_POINT('',#70672);
#17335=VERTEX_POINT('',#70676);
#17336=VERTEX_POINT('',#70682);
#17337=VERTEX_POINT('',#70683);
#17338=VERTEX_POINT('',#70685);
#17339=VERTEX_POINT('',#70687);
#17340=VERTEX_POINT('',#70691);
#17341=VERTEX_POINT('',#70695);
#17342=VERTEX_POINT('',#70701);
#17343=VERTEX_POINT('',#70702);
#17344=VERTEX_POINT('',#70704);
#17345=VERTEX_POINT('',#70706);
#17346=VERTEX_POINT('',#70710);
#17347=VERTEX_POINT('',#70714);
#17348=VERTEX_POINT('',#70720);
#17349=VERTEX_POINT('',#70721);
#17350=VERTEX_POINT('',#70723);
#17351=VERTEX_POINT('',#70725);
#17352=VERTEX_POINT('',#70729);
#17353=VERTEX_POINT('',#70733);
#17354=VERTEX_POINT('',#70739);
#17355=VERTEX_POINT('',#70740);
#17356=VERTEX_POINT('',#70742);
#17357=VERTEX_POINT('',#70744);
#17358=VERTEX_POINT('',#70748);
#17359=VERTEX_POINT('',#70752);
#17360=VERTEX_POINT('',#70758);
#17361=VERTEX_POINT('',#70759);
#17362=VERTEX_POINT('',#70761);
#17363=VERTEX_POINT('',#70763);
#17364=VERTEX_POINT('',#70767);
#17365=VERTEX_POINT('',#70771);
#17366=VERTEX_POINT('',#70777);
#17367=VERTEX_POINT('',#70778);
#17368=VERTEX_POINT('',#70780);
#17369=VERTEX_POINT('',#70782);
#17370=VERTEX_POINT('',#70786);
#17371=VERTEX_POINT('',#70790);
#17372=VERTEX_POINT('',#70796);
#17373=VERTEX_POINT('',#70797);
#17374=VERTEX_POINT('',#70799);
#17375=VERTEX_POINT('',#70801);
#17376=VERTEX_POINT('',#70805);
#17377=VERTEX_POINT('',#70809);
#17378=VERTEX_POINT('',#70815);
#17379=VERTEX_POINT('',#70816);
#17380=VERTEX_POINT('',#70818);
#17381=VERTEX_POINT('',#70820);
#17382=VERTEX_POINT('',#70824);
#17383=VERTEX_POINT('',#70828);
#17384=VERTEX_POINT('',#70834);
#17385=VERTEX_POINT('',#70835);
#17386=VERTEX_POINT('',#70837);
#17387=VERTEX_POINT('',#70839);
#17388=VERTEX_POINT('',#70843);
#17389=VERTEX_POINT('',#70847);
#17390=VERTEX_POINT('',#70853);
#17391=VERTEX_POINT('',#70854);
#17392=VERTEX_POINT('',#70856);
#17393=VERTEX_POINT('',#70858);
#17394=VERTEX_POINT('',#70862);
#17395=VERTEX_POINT('',#70866);
#17396=VERTEX_POINT('',#70872);
#21626=EDGE_CURVE('',#17032,#17033,#10205,.T.);
#21627=EDGE_CURVE('',#17032,#17034,#682,.T.);
#21628=EDGE_CURVE('',#17034,#17035,#14427,.F.);
#21629=EDGE_CURVE('',#17035,#17033,#683,.T.);
#21630=EDGE_CURVE('',#17036,#17037,#10206,.T.);
#21631=EDGE_CURVE('',#17036,#17032,#684,.T.);
#21632=EDGE_CURVE('',#17033,#17037,#685,.T.);
#21633=EDGE_CURVE('',#17038,#17039,#10207,.T.);
#21634=EDGE_CURVE('',#17038,#17036,#686,.T.);
#21635=EDGE_CURVE('',#17037,#17039,#687,.T.);
#21636=EDGE_CURVE('',#17040,#17041,#10208,.T.);
#21637=EDGE_CURVE('',#17040,#17038,#688,.T.);
#21638=EDGE_CURVE('',#17039,#17041,#689,.T.);
#21639=EDGE_CURVE('',#17042,#17043,#10209,.T.);
#21640=EDGE_CURVE('',#17042,#17040,#690,.T.);
#21641=EDGE_CURVE('',#17041,#17043,#691,.T.);
#21642=EDGE_CURVE('',#17044,#17045,#10210,.T.);
#21643=EDGE_CURVE('',#17044,#17042,#692,.T.);
#21644=EDGE_CURVE('',#17043,#17045,#693,.T.);
#21645=EDGE_CURVE('',#17046,#17047,#10211,.T.);
#21646=EDGE_CURVE('',#17046,#17044,#694,.T.);
#21647=EDGE_CURVE('',#17045,#17047,#695,.T.);
#21648=EDGE_CURVE('',#17048,#17049,#10212,.T.);
#21649=EDGE_CURVE('',#17048,#17046,#696,.T.);
#21650=EDGE_CURVE('',#17047,#17049,#697,.T.);
#21651=EDGE_CURVE('',#17050,#17051,#10213,.T.);
#21652=EDGE_CURVE('',#17050,#17048,#698,.T.);
#21653=EDGE_CURVE('',#17049,#17051,#699,.T.);
#21654=EDGE_CURVE('',#17052,#17053,#10214,.T.);
#21655=EDGE_CURVE('',#17052,#17050,#700,.T.);
#21656=EDGE_CURVE('',#17051,#17053,#701,.T.);
#21657=EDGE_CURVE('',#17054,#17055,#10215,.T.);
#21658=EDGE_CURVE('',#17054,#17052,#702,.T.);
#21659=EDGE_CURVE('',#17053,#17055,#703,.T.);
#21660=EDGE_CURVE('',#17056,#17057,#10216,.T.);
#21661=EDGE_CURVE('',#17056,#17054,#704,.T.);
#21662=EDGE_CURVE('',#17055,#17057,#705,.T.);
#21663=EDGE_CURVE('',#17058,#17059,#10217,.T.);
#21664=EDGE_CURVE('',#17058,#17056,#706,.T.);
#21665=EDGE_CURVE('',#17057,#17059,#707,.T.);
#21666=EDGE_CURVE('',#17060,#17061,#10218,.T.);
#21667=EDGE_CURVE('',#17060,#17058,#708,.T.);
#21668=EDGE_CURVE('',#17059,#17061,#709,.T.);
#21669=EDGE_CURVE('',#17062,#17063,#10219,.T.);
#21670=EDGE_CURVE('',#17062,#17060,#710,.T.);
#21671=EDGE_CURVE('',#17061,#17063,#711,.T.);
#21672=EDGE_CURVE('',#17064,#17065,#10220,.T.);
#21673=EDGE_CURVE('',#17064,#17062,#712,.T.);
#21674=EDGE_CURVE('',#17063,#17065,#713,.T.);
#21675=EDGE_CURVE('',#17066,#17067,#10221,.T.);
#21676=EDGE_CURVE('',#17066,#17064,#714,.T.);
#21677=EDGE_CURVE('',#17065,#17067,#715,.T.);
#21678=EDGE_CURVE('',#17068,#17069,#10222,.T.);
#21679=EDGE_CURVE('',#17068,#17066,#716,.T.);
#21680=EDGE_CURVE('',#17067,#17069,#717,.T.);
#21681=EDGE_CURVE('',#17070,#17071,#10223,.T.);
#21682=EDGE_CURVE('',#17070,#17068,#718,.T.);
#21683=EDGE_CURVE('',#17069,#17071,#719,.T.);
#21684=EDGE_CURVE('',#17072,#17073,#10224,.T.);
#21685=EDGE_CURVE('',#17072,#17070,#720,.T.);
#21686=EDGE_CURVE('',#17071,#17073,#721,.T.);
#21687=EDGE_CURVE('',#17074,#17075,#10225,.T.);
#21688=EDGE_CURVE('',#17074,#17072,#722,.T.);
#21689=EDGE_CURVE('',#17073,#17075,#723,.T.);
#21690=EDGE_CURVE('',#17076,#17077,#10226,.T.);
#21691=EDGE_CURVE('',#17076,#17074,#724,.T.);
#21692=EDGE_CURVE('',#17075,#17077,#725,.T.);
#21693=EDGE_CURVE('',#17078,#17079,#10227,.T.);
#21694=EDGE_CURVE('',#17078,#17076,#726,.T.);
#21695=EDGE_CURVE('',#17077,#17079,#727,.T.);
#21696=EDGE_CURVE('',#17080,#17081,#10228,.T.);
#21697=EDGE_CURVE('',#17080,#17078,#728,.T.);
#21698=EDGE_CURVE('',#17079,#17081,#729,.T.);
#21699=EDGE_CURVE('',#17082,#17083,#10229,.T.);
#21700=EDGE_CURVE('',#17082,#17080,#730,.T.);
#21701=EDGE_CURVE('',#17081,#17083,#731,.T.);
#21702=EDGE_CURVE('',#17084,#17085,#10230,.T.);
#21703=EDGE_CURVE('',#17084,#17082,#732,.T.);
#21704=EDGE_CURVE('',#17083,#17085,#733,.T.);
#21705=EDGE_CURVE('',#17086,#17087,#10231,.T.);
#21706=EDGE_CURVE('',#17086,#17084,#734,.T.);
#21707=EDGE_CURVE('',#17085,#17087,#735,.T.);
#21708=EDGE_CURVE('',#17088,#17089,#10232,.T.);
#21709=EDGE_CURVE('',#17088,#17086,#736,.T.);
#21710=EDGE_CURVE('',#17087,#17089,#737,.T.);
#21711=EDGE_CURVE('',#17090,#17091,#10233,.T.);
#21712=EDGE_CURVE('',#17090,#17088,#738,.T.);
#21713=EDGE_CURVE('',#17089,#17091,#739,.T.);
#21714=EDGE_CURVE('',#17092,#17093,#10234,.T.);
#21715=EDGE_CURVE('',#17092,#17094,#740,.T.);
#21716=EDGE_CURVE('',#17093,#17094,#14428,.T.);
#21717=EDGE_CURVE('',#17095,#17096,#10235,.T.);
#21718=EDGE_CURVE('',#17095,#17092,#741,.T.);
#21719=EDGE_CURVE('',#17097,#17093,#14429,.T.);
#21720=EDGE_CURVE('',#17096,#17097,#742,.T.);
#21721=EDGE_CURVE('',#17098,#17099,#10236,.T.);
#21722=EDGE_CURVE('',#17098,#17095,#743,.T.);
#21723=EDGE_CURVE('',#17099,#17096,#744,.T.);
#21724=EDGE_CURVE('',#17100,#17101,#10237,.T.);
#21725=EDGE_CURVE('',#17100,#17098,#745,.T.);
#21726=EDGE_CURVE('',#17101,#17099,#746,.T.);
#21727=EDGE_CURVE('',#17102,#17103,#10238,.T.);
#21728=EDGE_CURVE('',#17102,#17100,#747,.T.);
#21729=EDGE_CURVE('',#17103,#17101,#748,.T.);
#21730=EDGE_CURVE('',#17104,#17105,#10239,.T.);
#21731=EDGE_CURVE('',#17104,#17102,#749,.T.);
#21732=EDGE_CURVE('',#17105,#17103,#750,.T.);
#21733=EDGE_CURVE('',#17106,#17107,#10240,.T.);
#21734=EDGE_CURVE('',#17106,#17104,#751,.T.);
#21735=EDGE_CURVE('',#17107,#17105,#752,.T.);
#21736=EDGE_CURVE('',#17108,#17109,#10241,.T.);
#21737=EDGE_CURVE('',#17108,#17106,#753,.T.);
#21738=EDGE_CURVE('',#17109,#17107,#754,.T.);
#21739=EDGE_CURVE('',#17110,#17111,#10242,.T.);
#21740=EDGE_CURVE('',#17110,#17108,#755,.T.);
#21741=EDGE_CURVE('',#17111,#17109,#756,.T.);
#21742=EDGE_CURVE('',#17112,#17113,#10243,.T.);
#21743=EDGE_CURVE('',#17112,#17110,#757,.T.);
#21744=EDGE_CURVE('',#17113,#17111,#758,.T.);
#21745=EDGE_CURVE('',#17114,#17115,#10244,.T.);
#21746=EDGE_CURVE('',#17114,#17112,#759,.T.);
#21747=EDGE_CURVE('',#17115,#17113,#760,.T.);
#21748=EDGE_CURVE('',#17116,#17117,#10245,.T.);
#21749=EDGE_CURVE('',#17116,#17114,#761,.T.);
#21750=EDGE_CURVE('',#17117,#17115,#762,.T.);
#21751=EDGE_CURVE('',#17118,#17119,#10246,.T.);
#21752=EDGE_CURVE('',#17118,#17116,#763,.T.);
#21753=EDGE_CURVE('',#17119,#17117,#764,.T.);
#21754=EDGE_CURVE('',#17120,#17121,#10247,.T.);
#21755=EDGE_CURVE('',#17120,#17118,#765,.T.);
#21756=EDGE_CURVE('',#17121,#17119,#766,.T.);
#21757=EDGE_CURVE('',#17122,#17123,#10248,.T.);
#21758=EDGE_CURVE('',#17122,#17120,#767,.T.);
#21759=EDGE_CURVE('',#17123,#17121,#768,.T.);
#21760=EDGE_CURVE('',#17124,#17125,#10249,.T.);
#21761=EDGE_CURVE('',#17124,#17122,#769,.T.);
#21762=EDGE_CURVE('',#17125,#17123,#770,.T.);
#21763=EDGE_CURVE('',#17126,#17127,#10250,.T.);
#21764=EDGE_CURVE('',#17126,#17124,#771,.T.);
#21765=EDGE_CURVE('',#17127,#17125,#772,.T.);
#21766=EDGE_CURVE('',#17128,#17129,#10251,.T.);
#21767=EDGE_CURVE('',#17128,#17126,#773,.T.);
#21768=EDGE_CURVE('',#17129,#17127,#774,.T.);
#21769=EDGE_CURVE('',#17130,#17131,#10252,.T.);
#21770=EDGE_CURVE('',#17130,#17128,#775,.T.);
#21771=EDGE_CURVE('',#17131,#17129,#776,.T.);
#21772=EDGE_CURVE('',#17132,#17133,#10253,.T.);
#21773=EDGE_CURVE('',#17132,#17130,#777,.T.);
#21774=EDGE_CURVE('',#17133,#17131,#778,.T.);
#21775=EDGE_CURVE('',#17134,#17135,#10254,.T.);
#21776=EDGE_CURVE('',#17134,#17132,#779,.T.);
#21777=EDGE_CURVE('',#17135,#17133,#780,.T.);
#21778=EDGE_CURVE('',#17136,#17137,#10255,.T.);
#21779=EDGE_CURVE('',#17136,#17134,#781,.T.);
#21780=EDGE_CURVE('',#17137,#17135,#782,.T.);
#21781=EDGE_CURVE('',#17138,#17139,#10256,.T.);
#21782=EDGE_CURVE('',#17138,#17136,#783,.T.);
#21783=EDGE_CURVE('',#17139,#17137,#784,.T.);
#21784=EDGE_CURVE('',#17140,#17141,#10257,.T.);
#21785=EDGE_CURVE('',#17140,#17138,#785,.T.);
#21786=EDGE_CURVE('',#17141,#17139,#786,.T.);
#21787=EDGE_CURVE('',#17142,#17143,#10258,.T.);
#21788=EDGE_CURVE('',#17142,#17140,#787,.T.);
#21789=EDGE_CURVE('',#17143,#17141,#788,.T.);
#21790=EDGE_CURVE('',#17144,#17145,#10259,.T.);
#21791=EDGE_CURVE('',#17144,#17142,#789,.T.);
#21792=EDGE_CURVE('',#17145,#17143,#790,.T.);
#21793=EDGE_CURVE('',#17146,#17147,#10260,.T.);
#21794=EDGE_CURVE('',#17146,#17144,#791,.T.);
#21795=EDGE_CURVE('',#17147,#17145,#792,.T.);
#21796=EDGE_CURVE('',#17148,#17149,#10261,.T.);
#21797=EDGE_CURVE('',#17148,#17146,#793,.T.);
#21798=EDGE_CURVE('',#17149,#17147,#794,.T.);
#21799=EDGE_CURVE('',#17150,#17151,#10262,.T.);
#21800=EDGE_CURVE('',#17150,#17148,#795,.T.);
#21801=EDGE_CURVE('',#17151,#17149,#796,.T.);
#21802=EDGE_CURVE('',#17152,#17152,#14430,.T.);
#21803=EDGE_CURVE('',#17152,#17153,#10263,.T.);
#21804=EDGE_CURVE('',#17153,#17154,#14431,.T.);
#21805=EDGE_CURVE('',#17154,#17153,#14432,.T.);
#21806=EDGE_CURVE('',#17154,#17155,#10264,.T.);
#21807=EDGE_CURVE('',#17155,#17156,#14433,.F.);
#21808=EDGE_CURVE('',#17156,#17157,#14434,.F.);
#21809=EDGE_CURVE('',#17157,#17155,#14435,.F.);
#21810=EDGE_CURVE('',#17158,#17159,#267,.T.);
#21811=EDGE_CURVE('',#17159,#17160,#10265,.T.);
#21812=EDGE_CURVE('',#17160,#17161,#268,.T.);
#21813=EDGE_CURVE('',#17161,#17162,#10266,.T.);
#21814=EDGE_CURVE('',#17162,#17163,#10267,.T.);
#21815=EDGE_CURVE('',#17163,#17158,#10268,.T.);
#21816=EDGE_CURVE('',#17159,#17160,#14436,.T.);
#21817=EDGE_CURVE('',#17164,#17164,#14437,.T.);
#21818=EDGE_CURVE('',#17163,#17165,#10269,.T.);
#21819=EDGE_CURVE('',#17165,#17166,#10270,.T.);
#21820=EDGE_CURVE('',#17166,#17167,#269,.T.);
#21821=EDGE_CURVE('',#17167,#17168,#10271,.T.);
#21822=EDGE_CURVE('',#17168,#17158,#270,.T.);
#21823=EDGE_CURVE('',#17167,#17169,#14438,.T.);
#21824=EDGE_CURVE('',#17170,#17169,#10272,.T.);
#21825=EDGE_CURVE('',#17168,#17170,#14439,.T.);
#21826=EDGE_CURVE('',#17171,#17166,#271,.T.);
#21827=EDGE_CURVE('',#17171,#17172,#14440,.T.);
#21828=EDGE_CURVE('',#17173,#17172,#272,.T.);
#21829=EDGE_CURVE('',#17169,#17173,#273,.T.);
#21830=EDGE_CURVE('',#17165,#17174,#10273,.T.);
#21831=EDGE_CURVE('',#17174,#17173,#10274,.T.);
#21832=EDGE_CURVE('',#17172,#17171,#10275,.T.);
#21833=EDGE_CURVE('',#17174,#17162,#10276,.T.);
#21834=EDGE_CURVE('',#17161,#17170,#274,.T.);
#21835=EDGE_CURVE('',#17094,#17156,#797,.T.);
#21836=EDGE_CURVE('',#17157,#17097,#798,.T.);
#21837=EDGE_CURVE('',#17091,#17157,#799,.T.);
#21838=EDGE_CURVE('',#17175,#17035,#800,.T.);
#21839=EDGE_CURVE('',#17175,#17151,#801,.T.);
#21840=EDGE_CURVE('',#17035,#17176,#14441,.F.);
#21841=EDGE_CURVE('',#17176,#17034,#14442,.F.);
#21842=EDGE_CURVE('',#17034,#17177,#802,.T.);
#21843=EDGE_CURVE('',#17177,#17175,#14443,.T.);
#21844=EDGE_CURVE('',#17177,#17150,#803,.T.);
#21845=EDGE_CURVE('',#17156,#17090,#804,.T.);
#21846=EDGE_CURVE('',#17178,#17179,#10277,.T.);
#21847=EDGE_CURVE('',#17178,#17180,#10278,.T.);
#21848=EDGE_CURVE('',#17181,#17180,#10279,.T.);
#21849=EDGE_CURVE('',#17179,#17181,#10280,.T.);
#21850=EDGE_CURVE('',#17179,#17182,#14444,.T.);
#21851=EDGE_CURVE('',#17181,#17182,#10281,.T.);
#21852=EDGE_CURVE('',#17182,#17183,#10282,.T.);
#21853=EDGE_CURVE('',#17180,#17183,#10283,.T.);
#21854=EDGE_CURVE('',#17183,#17178,#14445,.T.);
#21855=EDGE_CURVE('',#17184,#17185,#10284,.T.);
#21856=EDGE_CURVE('',#17184,#17186,#10285,.T.);
#21857=EDGE_CURVE('',#17187,#17186,#10286,.T.);
#21858=EDGE_CURVE('',#17185,#17187,#10287,.T.);
#21859=EDGE_CURVE('',#17185,#17188,#14446,.T.);
#21860=EDGE_CURVE('',#17187,#17188,#10288,.T.);
#21861=EDGE_CURVE('',#17188,#17189,#10289,.T.);
#21862=EDGE_CURVE('',#17186,#17189,#10290,.T.);
#21863=EDGE_CURVE('',#17189,#17184,#14447,.T.);
#21864=EDGE_CURVE('',#17190,#17191,#10291,.T.);
#21865=EDGE_CURVE('',#17190,#17192,#10292,.T.);
#21866=EDGE_CURVE('',#17193,#17192,#10293,.T.);
#21867=EDGE_CURVE('',#17191,#17193,#10294,.T.);
#21868=EDGE_CURVE('',#17191,#17194,#14448,.T.);
#21869=EDGE_CURVE('',#17193,#17194,#10295,.T.);
#21870=EDGE_CURVE('',#17194,#17195,#10296,.T.);
#21871=EDGE_CURVE('',#17192,#17195,#10297,.T.);
#21872=EDGE_CURVE('',#17195,#17190,#14449,.T.);
#21873=EDGE_CURVE('',#17196,#17197,#10298,.T.);
#21874=EDGE_CURVE('',#17196,#17198,#10299,.T.);
#21875=EDGE_CURVE('',#17199,#17198,#10300,.T.);
#21876=EDGE_CURVE('',#17197,#17199,#10301,.T.);
#21877=EDGE_CURVE('',#17197,#17200,#14450,.T.);
#21878=EDGE_CURVE('',#17199,#17200,#10302,.T.);
#21879=EDGE_CURVE('',#17200,#17201,#10303,.T.);
#21880=EDGE_CURVE('',#17198,#17201,#10304,.T.);
#21881=EDGE_CURVE('',#17201,#17196,#14451,.T.);
#21882=EDGE_CURVE('',#17202,#17203,#10305,.T.);
#21883=EDGE_CURVE('',#17202,#17204,#10306,.T.);
#21884=EDGE_CURVE('',#17205,#17204,#10307,.T.);
#21885=EDGE_CURVE('',#17203,#17205,#10308,.T.);
#21886=EDGE_CURVE('',#17203,#17206,#14452,.T.);
#21887=EDGE_CURVE('',#17205,#17206,#10309,.T.);
#21888=EDGE_CURVE('',#17206,#17207,#10310,.T.);
#21889=EDGE_CURVE('',#17204,#17207,#10311,.T.);
#21890=EDGE_CURVE('',#17207,#17202,#14453,.T.);
#21891=EDGE_CURVE('',#17208,#17209,#10312,.T.);
#21892=EDGE_CURVE('',#17208,#17210,#10313,.T.);
#21893=EDGE_CURVE('',#17211,#17210,#10314,.T.);
#21894=EDGE_CURVE('',#17209,#17211,#10315,.T.);
#21895=EDGE_CURVE('',#17209,#17212,#14454,.T.);
#21896=EDGE_CURVE('',#17211,#17212,#10316,.T.);
#21897=EDGE_CURVE('',#17212,#17213,#10317,.T.);
#21898=EDGE_CURVE('',#17210,#17213,#10318,.T.);
#21899=EDGE_CURVE('',#17213,#17208,#14455,.T.);
#21900=EDGE_CURVE('',#17214,#17215,#10319,.T.);
#21901=EDGE_CURVE('',#17214,#17216,#10320,.T.);
#21902=EDGE_CURVE('',#17217,#17216,#10321,.T.);
#21903=EDGE_CURVE('',#17215,#17217,#10322,.T.);
#21904=EDGE_CURVE('',#17215,#17218,#14456,.T.);
#21905=EDGE_CURVE('',#17217,#17218,#10323,.T.);
#21906=EDGE_CURVE('',#17218,#17219,#10324,.T.);
#21907=EDGE_CURVE('',#17216,#17219,#10325,.T.);
#21908=EDGE_CURVE('',#17219,#17214,#14457,.T.);
#21909=EDGE_CURVE('',#17220,#17221,#10326,.T.);
#21910=EDGE_CURVE('',#17220,#17222,#10327,.T.);
#21911=EDGE_CURVE('',#17223,#17222,#10328,.T.);
#21912=EDGE_CURVE('',#17221,#17223,#10329,.T.);
#21913=EDGE_CURVE('',#17221,#17224,#14458,.T.);
#21914=EDGE_CURVE('',#17223,#17224,#10330,.T.);
#21915=EDGE_CURVE('',#17224,#17225,#10331,.T.);
#21916=EDGE_CURVE('',#17222,#17225,#10332,.T.);
#21917=EDGE_CURVE('',#17225,#17220,#14459,.T.);
#21918=EDGE_CURVE('',#17226,#17227,#10333,.T.);
#21919=EDGE_CURVE('',#17226,#17228,#10334,.T.);
#21920=EDGE_CURVE('',#17229,#17228,#10335,.T.);
#21921=EDGE_CURVE('',#17227,#17229,#10336,.T.);
#21922=EDGE_CURVE('',#17227,#17230,#14460,.T.);
#21923=EDGE_CURVE('',#17229,#17230,#10337,.T.);
#21924=EDGE_CURVE('',#17230,#17231,#10338,.T.);
#21925=EDGE_CURVE('',#17228,#17231,#10339,.T.);
#21926=EDGE_CURVE('',#17231,#17226,#14461,.T.);
#21927=EDGE_CURVE('',#17232,#17233,#10340,.T.);
#21928=EDGE_CURVE('',#17232,#17234,#10341,.T.);
#21929=EDGE_CURVE('',#17235,#17234,#10342,.T.);
#21930=EDGE_CURVE('',#17233,#17235,#10343,.T.);
#21931=EDGE_CURVE('',#17233,#17236,#14462,.T.);
#21932=EDGE_CURVE('',#17235,#17236,#10344,.T.);
#21933=EDGE_CURVE('',#17236,#17237,#10345,.T.);
#21934=EDGE_CURVE('',#17234,#17237,#10346,.T.);
#21935=EDGE_CURVE('',#17237,#17232,#14463,.T.);
#21936=EDGE_CURVE('',#17238,#17239,#10347,.T.);
#21937=EDGE_CURVE('',#17238,#17240,#10348,.T.);
#21938=EDGE_CURVE('',#17241,#17240,#10349,.T.);
#21939=EDGE_CURVE('',#17239,#17241,#10350,.T.);
#21940=EDGE_CURVE('',#17239,#17242,#14464,.T.);
#21941=EDGE_CURVE('',#17241,#17242,#10351,.T.);
#21942=EDGE_CURVE('',#17242,#17243,#10352,.T.);
#21943=EDGE_CURVE('',#17240,#17243,#10353,.T.);
#21944=EDGE_CURVE('',#17243,#17238,#14465,.T.);
#21945=EDGE_CURVE('',#17244,#17245,#10354,.T.);
#21946=EDGE_CURVE('',#17244,#17246,#10355,.T.);
#21947=EDGE_CURVE('',#17247,#17246,#10356,.T.);
#21948=EDGE_CURVE('',#17245,#17247,#10357,.T.);
#21949=EDGE_CURVE('',#17245,#17248,#14466,.T.);
#21950=EDGE_CURVE('',#17247,#17248,#10358,.T.);
#21951=EDGE_CURVE('',#17248,#17249,#10359,.T.);
#21952=EDGE_CURVE('',#17246,#17249,#10360,.T.);
#21953=EDGE_CURVE('',#17249,#17244,#14467,.T.);
#21954=EDGE_CURVE('',#17250,#17251,#10361,.T.);
#21955=EDGE_CURVE('',#17250,#17252,#10362,.T.);
#21956=EDGE_CURVE('',#17253,#17252,#10363,.T.);
#21957=EDGE_CURVE('',#17251,#17253,#10364,.T.);
#21958=EDGE_CURVE('',#17251,#17254,#14468,.T.);
#21959=EDGE_CURVE('',#17253,#17254,#10365,.T.);
#21960=EDGE_CURVE('',#17254,#17255,#10366,.T.);
#21961=EDGE_CURVE('',#17252,#17255,#10367,.T.);
#21962=EDGE_CURVE('',#17255,#17250,#14469,.T.);
#21963=EDGE_CURVE('',#17256,#17257,#10368,.T.);
#21964=EDGE_CURVE('',#17256,#17258,#10369,.T.);
#21965=EDGE_CURVE('',#17259,#17258,#10370,.T.);
#21966=EDGE_CURVE('',#17257,#17259,#10371,.T.);
#21967=EDGE_CURVE('',#17257,#17260,#14470,.T.);
#21968=EDGE_CURVE('',#17259,#17260,#10372,.T.);
#21969=EDGE_CURVE('',#17260,#17261,#10373,.T.);
#21970=EDGE_CURVE('',#17258,#17261,#10374,.T.);
#21971=EDGE_CURVE('',#17261,#17256,#14471,.T.);
#21972=EDGE_CURVE('',#17262,#17263,#10375,.T.);
#21973=EDGE_CURVE('',#17262,#17264,#10376,.T.);
#21974=EDGE_CURVE('',#17265,#17264,#10377,.T.);
#21975=EDGE_CURVE('',#17263,#17265,#10378,.T.);
#21976=EDGE_CURVE('',#17263,#17266,#14472,.T.);
#21977=EDGE_CURVE('',#17265,#17266,#10379,.T.);
#21978=EDGE_CURVE('',#17266,#17267,#10380,.T.);
#21979=EDGE_CURVE('',#17264,#17267,#10381,.T.);
#21980=EDGE_CURVE('',#17267,#17262,#14473,.T.);
#21981=EDGE_CURVE('',#17268,#17269,#10382,.T.);
#21982=EDGE_CURVE('',#17268,#17270,#10383,.T.);
#21983=EDGE_CURVE('',#17271,#17270,#10384,.T.);
#21984=EDGE_CURVE('',#17269,#17271,#10385,.T.);
#21985=EDGE_CURVE('',#17269,#17272,#14474,.T.);
#21986=EDGE_CURVE('',#17271,#17272,#10386,.T.);
#21987=EDGE_CURVE('',#17272,#17273,#10387,.T.);
#21988=EDGE_CURVE('',#17270,#17273,#10388,.T.);
#21989=EDGE_CURVE('',#17273,#17268,#14475,.T.);
#21990=EDGE_CURVE('',#17274,#17275,#10389,.T.);
#21991=EDGE_CURVE('',#17274,#17276,#10390,.T.);
#21992=EDGE_CURVE('',#17277,#17276,#10391,.T.);
#21993=EDGE_CURVE('',#17275,#17277,#10392,.T.);
#21994=EDGE_CURVE('',#17275,#17278,#14476,.T.);
#21995=EDGE_CURVE('',#17277,#17278,#10393,.T.);
#21996=EDGE_CURVE('',#17278,#17279,#10394,.T.);
#21997=EDGE_CURVE('',#17276,#17279,#10395,.T.);
#21998=EDGE_CURVE('',#17279,#17274,#14477,.T.);
#21999=EDGE_CURVE('',#17280,#17281,#10396,.T.);
#22000=EDGE_CURVE('',#17280,#17282,#10397,.T.);
#22001=EDGE_CURVE('',#17283,#17282,#10398,.T.);
#22002=EDGE_CURVE('',#17281,#17283,#10399,.T.);
#22003=EDGE_CURVE('',#17281,#17284,#14478,.T.);
#22004=EDGE_CURVE('',#17283,#17285,#10400,.T.);
#22005=EDGE_CURVE('',#17284,#17285,#14479,.T.);
#22006=EDGE_CURVE('',#17285,#17286,#10401,.T.);
#22007=EDGE_CURVE('',#17282,#17286,#10402,.T.);
#22008=EDGE_CURVE('',#17286,#17287,#14480,.T.);
#22009=EDGE_CURVE('',#17287,#17280,#14481,.T.);
#22010=EDGE_CURVE('',#17288,#17289,#10403,.T.);
#22011=EDGE_CURVE('',#17288,#17290,#10404,.T.);
#22012=EDGE_CURVE('',#17291,#17290,#10405,.T.);
#22013=EDGE_CURVE('',#17289,#17291,#10406,.T.);
#22014=EDGE_CURVE('',#17289,#17292,#14482,.T.);
#22015=EDGE_CURVE('',#17291,#17292,#10407,.T.);
#22016=EDGE_CURVE('',#17292,#17293,#10408,.T.);
#22017=EDGE_CURVE('',#17290,#17293,#10409,.T.);
#22018=EDGE_CURVE('',#17293,#17288,#14483,.T.);
#22019=EDGE_CURVE('',#17294,#17295,#10410,.T.);
#22020=EDGE_CURVE('',#17294,#17296,#10411,.T.);
#22021=EDGE_CURVE('',#17297,#17296,#10412,.T.);
#22022=EDGE_CURVE('',#17295,#17297,#10413,.T.);
#22023=EDGE_CURVE('',#17295,#17298,#14484,.T.);
#22024=EDGE_CURVE('',#17297,#17298,#10414,.T.);
#22025=EDGE_CURVE('',#17298,#17299,#10415,.T.);
#22026=EDGE_CURVE('',#17296,#17299,#10416,.T.);
#22027=EDGE_CURVE('',#17299,#17294,#14485,.T.);
#22028=EDGE_CURVE('',#17300,#17301,#10417,.T.);
#22029=EDGE_CURVE('',#17300,#17302,#10418,.T.);
#22030=EDGE_CURVE('',#17303,#17302,#10419,.T.);
#22031=EDGE_CURVE('',#17301,#17303,#10420,.T.);
#22032=EDGE_CURVE('',#17301,#17304,#14486,.T.);
#22033=EDGE_CURVE('',#17303,#17304,#10421,.T.);
#22034=EDGE_CURVE('',#17304,#17305,#10422,.T.);
#22035=EDGE_CURVE('',#17302,#17305,#10423,.T.);
#22036=EDGE_CURVE('',#17305,#17300,#14487,.T.);
#22037=EDGE_CURVE('',#17306,#17307,#10424,.T.);
#22038=EDGE_CURVE('',#17306,#17308,#10425,.T.);
#22039=EDGE_CURVE('',#17309,#17308,#10426,.T.);
#22040=EDGE_CURVE('',#17307,#17309,#10427,.T.);
#22041=EDGE_CURVE('',#17307,#17310,#14488,.T.);
#22042=EDGE_CURVE('',#17309,#17310,#10428,.T.);
#22043=EDGE_CURVE('',#17310,#17311,#10429,.T.);
#22044=EDGE_CURVE('',#17308,#17311,#10430,.T.);
#22045=EDGE_CURVE('',#17311,#17306,#14489,.T.);
#22046=EDGE_CURVE('',#17312,#17313,#10431,.T.);
#22047=EDGE_CURVE('',#17312,#17314,#10432,.T.);
#22048=EDGE_CURVE('',#17315,#17314,#10433,.T.);
#22049=EDGE_CURVE('',#17313,#17315,#10434,.T.);
#22050=EDGE_CURVE('',#17313,#17316,#14490,.T.);
#22051=EDGE_CURVE('',#17315,#17316,#10435,.T.);
#22052=EDGE_CURVE('',#17316,#17317,#10436,.T.);
#22053=EDGE_CURVE('',#17314,#17317,#10437,.T.);
#22054=EDGE_CURVE('',#17317,#17312,#14491,.T.);
#22055=EDGE_CURVE('',#17318,#17319,#10438,.T.);
#22056=EDGE_CURVE('',#17318,#17320,#10439,.T.);
#22057=EDGE_CURVE('',#17321,#17320,#10440,.T.);
#22058=EDGE_CURVE('',#17319,#17321,#10441,.T.);
#22059=EDGE_CURVE('',#17319,#17322,#14492,.T.);
#22060=EDGE_CURVE('',#17321,#17322,#10442,.T.);
#22061=EDGE_CURVE('',#17322,#17323,#10443,.T.);
#22062=EDGE_CURVE('',#17320,#17323,#10444,.T.);
#22063=EDGE_CURVE('',#17323,#17318,#14493,.T.);
#22064=EDGE_CURVE('',#17324,#17325,#10445,.T.);
#22065=EDGE_CURVE('',#17324,#17326,#10446,.T.);
#22066=EDGE_CURVE('',#17327,#17326,#10447,.T.);
#22067=EDGE_CURVE('',#17325,#17327,#10448,.T.);
#22068=EDGE_CURVE('',#17325,#17328,#14494,.T.);
#22069=EDGE_CURVE('',#17327,#17328,#10449,.T.);
#22070=EDGE_CURVE('',#17328,#17329,#10450,.T.);
#22071=EDGE_CURVE('',#17326,#17329,#10451,.T.);
#22072=EDGE_CURVE('',#17329,#17324,#14495,.T.);
#22073=EDGE_CURVE('',#17330,#17331,#10452,.T.);
#22074=EDGE_CURVE('',#17330,#17332,#10453,.T.);
#22075=EDGE_CURVE('',#17333,#17332,#10454,.T.);
#22076=EDGE_CURVE('',#17331,#17333,#10455,.T.);
#22077=EDGE_CURVE('',#17331,#17334,#14496,.T.);
#22078=EDGE_CURVE('',#17333,#17334,#10456,.T.);
#22079=EDGE_CURVE('',#17334,#17335,#10457,.T.);
#22080=EDGE_CURVE('',#17332,#17335,#10458,.T.);
#22081=EDGE_CURVE('',#17335,#17330,#14497,.T.);
#22082=EDGE_CURVE('',#17336,#17337,#10459,.T.);
#22083=EDGE_CURVE('',#17336,#17338,#10460,.T.);
#22084=EDGE_CURVE('',#17339,#17338,#10461,.T.);
#22085=EDGE_CURVE('',#17337,#17339,#10462,.T.);
#22086=EDGE_CURVE('',#17337,#17340,#14498,.T.);
#22087=EDGE_CURVE('',#17339,#17340,#10463,.T.);
#22088=EDGE_CURVE('',#17340,#17341,#10464,.T.);
#22089=EDGE_CURVE('',#17338,#17341,#10465,.T.);
#22090=EDGE_CURVE('',#17341,#17336,#14499,.T.);
#22091=EDGE_CURVE('',#17342,#17343,#10466,.T.);
#22092=EDGE_CURVE('',#17342,#17344,#10467,.T.);
#22093=EDGE_CURVE('',#17345,#17344,#10468,.T.);
#22094=EDGE_CURVE('',#17343,#17345,#10469,.T.);
#22095=EDGE_CURVE('',#17343,#17346,#14500,.T.);
#22096=EDGE_CURVE('',#17345,#17346,#10470,.T.);
#22097=EDGE_CURVE('',#17346,#17347,#10471,.T.);
#22098=EDGE_CURVE('',#17344,#17347,#10472,.T.);
#22099=EDGE_CURVE('',#17347,#17342,#14501,.T.);
#22100=EDGE_CURVE('',#17348,#17349,#10473,.T.);
#22101=EDGE_CURVE('',#17348,#17350,#10474,.T.);
#22102=EDGE_CURVE('',#17351,#17350,#10475,.T.);
#22103=EDGE_CURVE('',#17349,#17351,#10476,.T.);
#22104=EDGE_CURVE('',#17349,#17352,#14502,.T.);
#22105=EDGE_CURVE('',#17351,#17352,#10477,.T.);
#22106=EDGE_CURVE('',#17352,#17353,#10478,.T.);
#22107=EDGE_CURVE('',#17350,#17353,#10479,.T.);
#22108=EDGE_CURVE('',#17353,#17348,#14503,.T.);
#22109=EDGE_CURVE('',#17354,#17355,#10480,.T.);
#22110=EDGE_CURVE('',#17354,#17356,#10481,.T.);
#22111=EDGE_CURVE('',#17357,#17356,#10482,.T.);
#22112=EDGE_CURVE('',#17355,#17357,#10483,.T.);
#22113=EDGE_CURVE('',#17355,#17358,#14504,.T.);
#22114=EDGE_CURVE('',#17357,#17358,#10484,.T.);
#22115=EDGE_CURVE('',#17358,#17359,#10485,.T.);
#22116=EDGE_CURVE('',#17356,#17359,#10486,.T.);
#22117=EDGE_CURVE('',#17359,#17354,#14505,.T.);
#22118=EDGE_CURVE('',#17360,#17361,#10487,.T.);
#22119=EDGE_CURVE('',#17360,#17362,#10488,.T.);
#22120=EDGE_CURVE('',#17363,#17362,#10489,.T.);
#22121=EDGE_CURVE('',#17361,#17363,#10490,.T.);
#22122=EDGE_CURVE('',#17361,#17364,#14506,.T.);
#22123=EDGE_CURVE('',#17363,#17364,#10491,.T.);
#22124=EDGE_CURVE('',#17364,#17365,#10492,.T.);
#22125=EDGE_CURVE('',#17362,#17365,#10493,.T.);
#22126=EDGE_CURVE('',#17365,#17360,#14507,.T.);
#22127=EDGE_CURVE('',#17366,#17367,#10494,.T.);
#22128=EDGE_CURVE('',#17366,#17368,#10495,.T.);
#22129=EDGE_CURVE('',#17369,#17368,#10496,.T.);
#22130=EDGE_CURVE('',#17367,#17369,#10497,.T.);
#22131=EDGE_CURVE('',#17367,#17370,#14508,.T.);
#22132=EDGE_CURVE('',#17369,#17370,#10498,.T.);
#22133=EDGE_CURVE('',#17370,#17371,#10499,.T.);
#22134=EDGE_CURVE('',#17368,#17371,#10500,.T.);
#22135=EDGE_CURVE('',#17371,#17366,#14509,.T.);
#22136=EDGE_CURVE('',#17372,#17373,#10501,.T.);
#22137=EDGE_CURVE('',#17372,#17374,#10502,.T.);
#22138=EDGE_CURVE('',#17375,#17374,#10503,.T.);
#22139=EDGE_CURVE('',#17373,#17375,#10504,.T.);
#22140=EDGE_CURVE('',#17373,#17376,#14510,.T.);
#22141=EDGE_CURVE('',#17375,#17376,#10505,.T.);
#22142=EDGE_CURVE('',#17376,#17377,#10506,.T.);
#22143=EDGE_CURVE('',#17374,#17377,#10507,.T.);
#22144=EDGE_CURVE('',#17377,#17372,#14511,.T.);
#22145=EDGE_CURVE('',#17378,#17379,#10508,.T.);
#22146=EDGE_CURVE('',#17378,#17380,#10509,.T.);
#22147=EDGE_CURVE('',#17381,#17380,#10510,.T.);
#22148=EDGE_CURVE('',#17379,#17381,#10511,.T.);
#22149=EDGE_CURVE('',#17379,#17382,#14512,.T.);
#22150=EDGE_CURVE('',#17381,#17382,#10512,.T.);
#22151=EDGE_CURVE('',#17382,#17383,#10513,.T.);
#22152=EDGE_CURVE('',#17380,#17383,#10514,.T.);
#22153=EDGE_CURVE('',#17383,#17378,#14513,.T.);
#22154=EDGE_CURVE('',#17384,#17385,#10515,.T.);
#22155=EDGE_CURVE('',#17384,#17386,#10516,.T.);
#22156=EDGE_CURVE('',#17387,#17386,#10517,.T.);
#22157=EDGE_CURVE('',#17385,#17387,#10518,.T.);
#22158=EDGE_CURVE('',#17385,#17388,#14514,.T.);
#22159=EDGE_CURVE('',#17387,#17388,#10519,.T.);
#22160=EDGE_CURVE('',#17388,#17389,#10520,.T.);
#22161=EDGE_CURVE('',#17386,#17389,#10521,.T.);
#22162=EDGE_CURVE('',#17389,#17384,#14515,.T.);
#22163=EDGE_CURVE('',#17390,#17391,#10522,.T.);
#22164=EDGE_CURVE('',#17390,#17392,#10523,.T.);
#22165=EDGE_CURVE('',#17393,#17392,#10524,.T.);
#22166=EDGE_CURVE('',#17391,#17393,#10525,.T.);
#22167=EDGE_CURVE('',#17391,#17394,#14516,.T.);
#22168=EDGE_CURVE('',#17393,#17394,#10526,.T.);
#22169=EDGE_CURVE('',#17394,#17395,#10527,.T.);
#22170=EDGE_CURVE('',#17392,#17395,#10528,.T.);
#22171=EDGE_CURVE('',#17395,#17390,#14517,.T.);
#22172=EDGE_CURVE('',#17396,#17396,#14518,.T.);
#22173=EDGE_CURVE('',#17396,#17287,#10529,.T.);
#22174=EDGE_CURVE('',#17284,#17164,#10530,.T.);
#22175=EDGE_CURVE('',#17176,#17396,#10531,.T.);
#30624=ORIENTED_EDGE('',*,*,#21626,.F.);
#30625=ORIENTED_EDGE('',*,*,#21627,.T.);
#30626=ORIENTED_EDGE('',*,*,#21628,.T.);
#30627=ORIENTED_EDGE('',*,*,#21629,.T.);
#30628=ORIENTED_EDGE('',*,*,#21630,.F.);
#30629=ORIENTED_EDGE('',*,*,#21631,.T.);
#30630=ORIENTED_EDGE('',*,*,#21626,.T.);
#30631=ORIENTED_EDGE('',*,*,#21632,.T.);
#30632=ORIENTED_EDGE('',*,*,#21633,.F.);
#30633=ORIENTED_EDGE('',*,*,#21634,.T.);
#30634=ORIENTED_EDGE('',*,*,#21630,.T.);
#30635=ORIENTED_EDGE('',*,*,#21635,.T.);
#30636=ORIENTED_EDGE('',*,*,#21636,.F.);
#30637=ORIENTED_EDGE('',*,*,#21637,.T.);
#30638=ORIENTED_EDGE('',*,*,#21633,.T.);
#30639=ORIENTED_EDGE('',*,*,#21638,.T.);
#30640=ORIENTED_EDGE('',*,*,#21639,.F.);
#30641=ORIENTED_EDGE('',*,*,#21640,.T.);
#30642=ORIENTED_EDGE('',*,*,#21636,.T.);
#30643=ORIENTED_EDGE('',*,*,#21641,.T.);
#30644=ORIENTED_EDGE('',*,*,#21642,.F.);
#30645=ORIENTED_EDGE('',*,*,#21643,.T.);
#30646=ORIENTED_EDGE('',*,*,#21639,.T.);
#30647=ORIENTED_EDGE('',*,*,#21644,.T.);
#30648=ORIENTED_EDGE('',*,*,#21645,.F.);
#30649=ORIENTED_EDGE('',*,*,#21646,.T.);
#30650=ORIENTED_EDGE('',*,*,#21642,.T.);
#30651=ORIENTED_EDGE('',*,*,#21647,.T.);
#30652=ORIENTED_EDGE('',*,*,#21648,.F.);
#30653=ORIENTED_EDGE('',*,*,#21649,.T.);
#30654=ORIENTED_EDGE('',*,*,#21645,.T.);
#30655=ORIENTED_EDGE('',*,*,#21650,.T.);
#30656=ORIENTED_EDGE('',*,*,#21651,.F.);
#30657=ORIENTED_EDGE('',*,*,#21652,.T.);
#30658=ORIENTED_EDGE('',*,*,#21648,.T.);
#30659=ORIENTED_EDGE('',*,*,#21653,.T.);
#30660=ORIENTED_EDGE('',*,*,#21654,.F.);
#30661=ORIENTED_EDGE('',*,*,#21655,.T.);
#30662=ORIENTED_EDGE('',*,*,#21651,.T.);
#30663=ORIENTED_EDGE('',*,*,#21656,.T.);
#30664=ORIENTED_EDGE('',*,*,#21657,.F.);
#30665=ORIENTED_EDGE('',*,*,#21658,.T.);
#30666=ORIENTED_EDGE('',*,*,#21654,.T.);
#30667=ORIENTED_EDGE('',*,*,#21659,.T.);
#30668=ORIENTED_EDGE('',*,*,#21660,.F.);
#30669=ORIENTED_EDGE('',*,*,#21661,.T.);
#30670=ORIENTED_EDGE('',*,*,#21657,.T.);
#30671=ORIENTED_EDGE('',*,*,#21662,.T.);
#30672=ORIENTED_EDGE('',*,*,#21663,.F.);
#30673=ORIENTED_EDGE('',*,*,#21664,.T.);
#30674=ORIENTED_EDGE('',*,*,#21660,.T.);
#30675=ORIENTED_EDGE('',*,*,#21665,.T.);
#30676=ORIENTED_EDGE('',*,*,#21666,.F.);
#30677=ORIENTED_EDGE('',*,*,#21667,.T.);
#30678=ORIENTED_EDGE('',*,*,#21663,.T.);
#30679=ORIENTED_EDGE('',*,*,#21668,.T.);
#30680=ORIENTED_EDGE('',*,*,#21669,.F.);
#30681=ORIENTED_EDGE('',*,*,#21670,.T.);
#30682=ORIENTED_EDGE('',*,*,#21666,.T.);
#30683=ORIENTED_EDGE('',*,*,#21671,.T.);
#30684=ORIENTED_EDGE('',*,*,#21672,.F.);
#30685=ORIENTED_EDGE('',*,*,#21673,.T.);
#30686=ORIENTED_EDGE('',*,*,#21669,.T.);
#30687=ORIENTED_EDGE('',*,*,#21674,.T.);
#30688=ORIENTED_EDGE('',*,*,#21675,.F.);
#30689=ORIENTED_EDGE('',*,*,#21676,.T.);
#30690=ORIENTED_EDGE('',*,*,#21672,.T.);
#30691=ORIENTED_EDGE('',*,*,#21677,.T.);
#30692=ORIENTED_EDGE('',*,*,#21678,.F.);
#30693=ORIENTED_EDGE('',*,*,#21679,.T.);
#30694=ORIENTED_EDGE('',*,*,#21675,.T.);
#30695=ORIENTED_EDGE('',*,*,#21680,.T.);
#30696=ORIENTED_EDGE('',*,*,#21681,.F.);
#30697=ORIENTED_EDGE('',*,*,#21682,.T.);
#30698=ORIENTED_EDGE('',*,*,#21678,.T.);
#30699=ORIENTED_EDGE('',*,*,#21683,.T.);
#30700=ORIENTED_EDGE('',*,*,#21684,.F.);
#30701=ORIENTED_EDGE('',*,*,#21685,.T.);
#30702=ORIENTED_EDGE('',*,*,#21681,.T.);
#30703=ORIENTED_EDGE('',*,*,#21686,.T.);
#30704=ORIENTED_EDGE('',*,*,#21687,.F.);
#30705=ORIENTED_EDGE('',*,*,#21688,.T.);
#30706=ORIENTED_EDGE('',*,*,#21684,.T.);
#30707=ORIENTED_EDGE('',*,*,#21689,.T.);
#30708=ORIENTED_EDGE('',*,*,#21690,.F.);
#30709=ORIENTED_EDGE('',*,*,#21691,.T.);
#30710=ORIENTED_EDGE('',*,*,#21687,.T.);
#30711=ORIENTED_EDGE('',*,*,#21692,.T.);
#30712=ORIENTED_EDGE('',*,*,#21693,.F.);
#30713=ORIENTED_EDGE('',*,*,#21694,.T.);
#30714=ORIENTED_EDGE('',*,*,#21690,.T.);
#30715=ORIENTED_EDGE('',*,*,#21695,.T.);
#30716=ORIENTED_EDGE('',*,*,#21696,.F.);
#30717=ORIENTED_EDGE('',*,*,#21697,.T.);
#30718=ORIENTED_EDGE('',*,*,#21693,.T.);
#30719=ORIENTED_EDGE('',*,*,#21698,.T.);
#30720=ORIENTED_EDGE('',*,*,#21699,.F.);
#30721=ORIENTED_EDGE('',*,*,#21700,.T.);
#30722=ORIENTED_EDGE('',*,*,#21696,.T.);
#30723=ORIENTED_EDGE('',*,*,#21701,.T.);
#30724=ORIENTED_EDGE('',*,*,#21702,.F.);
#30725=ORIENTED_EDGE('',*,*,#21703,.T.);
#30726=ORIENTED_EDGE('',*,*,#21699,.T.);
#30727=ORIENTED_EDGE('',*,*,#21704,.T.);
#30728=ORIENTED_EDGE('',*,*,#21705,.F.);
#30729=ORIENTED_EDGE('',*,*,#21706,.T.);
#30730=ORIENTED_EDGE('',*,*,#21702,.T.);
#30731=ORIENTED_EDGE('',*,*,#21707,.T.);
#30732=ORIENTED_EDGE('',*,*,#21708,.F.);
#30733=ORIENTED_EDGE('',*,*,#21709,.T.);
#30734=ORIENTED_EDGE('',*,*,#21705,.T.);
#30735=ORIENTED_EDGE('',*,*,#21710,.T.);
#30736=ORIENTED_EDGE('',*,*,#21711,.F.);
#30737=ORIENTED_EDGE('',*,*,#21712,.T.);
#30738=ORIENTED_EDGE('',*,*,#21708,.T.);
#30739=ORIENTED_EDGE('',*,*,#21713,.T.);
#30740=ORIENTED_EDGE('',*,*,#21714,.F.);
#30741=ORIENTED_EDGE('',*,*,#21715,.T.);
#30742=ORIENTED_EDGE('',*,*,#21716,.F.);
#30743=ORIENTED_EDGE('',*,*,#21717,.F.);
#30744=ORIENTED_EDGE('',*,*,#21718,.T.);
#30745=ORIENTED_EDGE('',*,*,#21714,.T.);
#30746=ORIENTED_EDGE('',*,*,#21719,.F.);
#30747=ORIENTED_EDGE('',*,*,#21720,.F.);
#30748=ORIENTED_EDGE('',*,*,#21721,.F.);
#30749=ORIENTED_EDGE('',*,*,#21722,.T.);
#30750=ORIENTED_EDGE('',*,*,#21717,.T.);
#30751=ORIENTED_EDGE('',*,*,#21723,.F.);
#30752=ORIENTED_EDGE('',*,*,#21724,.F.);
#30753=ORIENTED_EDGE('',*,*,#21725,.T.);
#30754=ORIENTED_EDGE('',*,*,#21721,.T.);
#30755=ORIENTED_EDGE('',*,*,#21726,.F.);
#30756=ORIENTED_EDGE('',*,*,#21727,.F.);
#30757=ORIENTED_EDGE('',*,*,#21728,.T.);
#30758=ORIENTED_EDGE('',*,*,#21724,.T.);
#30759=ORIENTED_EDGE('',*,*,#21729,.F.);
#30760=ORIENTED_EDGE('',*,*,#21730,.F.);
#30761=ORIENTED_EDGE('',*,*,#21731,.T.);
#30762=ORIENTED_EDGE('',*,*,#21727,.T.);
#30763=ORIENTED_EDGE('',*,*,#21732,.F.);
#30764=ORIENTED_EDGE('',*,*,#21733,.F.);
#30765=ORIENTED_EDGE('',*,*,#21734,.T.);
#30766=ORIENTED_EDGE('',*,*,#21730,.T.);
#30767=ORIENTED_EDGE('',*,*,#21735,.F.);
#30768=ORIENTED_EDGE('',*,*,#21736,.F.);
#30769=ORIENTED_EDGE('',*,*,#21737,.T.);
#30770=ORIENTED_EDGE('',*,*,#21733,.T.);
#30771=ORIENTED_EDGE('',*,*,#21738,.F.);
#30772=ORIENTED_EDGE('',*,*,#21739,.F.);
#30773=ORIENTED_EDGE('',*,*,#21740,.T.);
#30774=ORIENTED_EDGE('',*,*,#21736,.T.);
#30775=ORIENTED_EDGE('',*,*,#21741,.F.);
#30776=ORIENTED_EDGE('',*,*,#21742,.F.);
#30777=ORIENTED_EDGE('',*,*,#21743,.T.);
#30778=ORIENTED_EDGE('',*,*,#21739,.T.);
#30779=ORIENTED_EDGE('',*,*,#21744,.F.);
#30780=ORIENTED_EDGE('',*,*,#21745,.F.);
#30781=ORIENTED_EDGE('',*,*,#21746,.T.);
#30782=ORIENTED_EDGE('',*,*,#21742,.T.);
#30783=ORIENTED_EDGE('',*,*,#21747,.F.);
#30784=ORIENTED_EDGE('',*,*,#21748,.F.);
#30785=ORIENTED_EDGE('',*,*,#21749,.T.);
#30786=ORIENTED_EDGE('',*,*,#21745,.T.);
#30787=ORIENTED_EDGE('',*,*,#21750,.F.);
#30788=ORIENTED_EDGE('',*,*,#21751,.F.);
#30789=ORIENTED_EDGE('',*,*,#21752,.T.);
#30790=ORIENTED_EDGE('',*,*,#21748,.T.);
#30791=ORIENTED_EDGE('',*,*,#21753,.F.);
#30792=ORIENTED_EDGE('',*,*,#21754,.F.);
#30793=ORIENTED_EDGE('',*,*,#21755,.T.);
#30794=ORIENTED_EDGE('',*,*,#21751,.T.);
#30795=ORIENTED_EDGE('',*,*,#21756,.F.);
#30796=ORIENTED_EDGE('',*,*,#21757,.F.);
#30797=ORIENTED_EDGE('',*,*,#21758,.T.);
#30798=ORIENTED_EDGE('',*,*,#21754,.T.);
#30799=ORIENTED_EDGE('',*,*,#21759,.F.);
#30800=ORIENTED_EDGE('',*,*,#21760,.F.);
#30801=ORIENTED_EDGE('',*,*,#21761,.T.);
#30802=ORIENTED_EDGE('',*,*,#21757,.T.);
#30803=ORIENTED_EDGE('',*,*,#21762,.F.);
#30804=ORIENTED_EDGE('',*,*,#21763,.F.);
#30805=ORIENTED_EDGE('',*,*,#21764,.T.);
#30806=ORIENTED_EDGE('',*,*,#21760,.T.);
#30807=ORIENTED_EDGE('',*,*,#21765,.F.);
#30808=ORIENTED_EDGE('',*,*,#21766,.F.);
#30809=ORIENTED_EDGE('',*,*,#21767,.T.);
#30810=ORIENTED_EDGE('',*,*,#21763,.T.);
#30811=ORIENTED_EDGE('',*,*,#21768,.F.);
#30812=ORIENTED_EDGE('',*,*,#21769,.F.);
#30813=ORIENTED_EDGE('',*,*,#21770,.T.);
#30814=ORIENTED_EDGE('',*,*,#21766,.T.);
#30815=ORIENTED_EDGE('',*,*,#21771,.F.);
#30816=ORIENTED_EDGE('',*,*,#21772,.F.);
#30817=ORIENTED_EDGE('',*,*,#21773,.T.);
#30818=ORIENTED_EDGE('',*,*,#21769,.T.);
#30819=ORIENTED_EDGE('',*,*,#21774,.F.);
#30820=ORIENTED_EDGE('',*,*,#21775,.F.);
#30821=ORIENTED_EDGE('',*,*,#21776,.T.);
#30822=ORIENTED_EDGE('',*,*,#21772,.T.);
#30823=ORIENTED_EDGE('',*,*,#21777,.F.);
#30824=ORIENTED_EDGE('',*,*,#21778,.F.);
#30825=ORIENTED_EDGE('',*,*,#21779,.T.);
#30826=ORIENTED_EDGE('',*,*,#21775,.T.);
#30827=ORIENTED_EDGE('',*,*,#21780,.F.);
#30828=ORIENTED_EDGE('',*,*,#21781,.F.);
#30829=ORIENTED_EDGE('',*,*,#21782,.T.);
#30830=ORIENTED_EDGE('',*,*,#21778,.T.);
#30831=ORIENTED_EDGE('',*,*,#21783,.F.);
#30832=ORIENTED_EDGE('',*,*,#21784,.F.);
#30833=ORIENTED_EDGE('',*,*,#21785,.T.);
#30834=ORIENTED_EDGE('',*,*,#21781,.T.);
#30835=ORIENTED_EDGE('',*,*,#21786,.F.);
#30836=ORIENTED_EDGE('',*,*,#21787,.F.);
#30837=ORIENTED_EDGE('',*,*,#21788,.T.);
#30838=ORIENTED_EDGE('',*,*,#21784,.T.);
#30839=ORIENTED_EDGE('',*,*,#21789,.F.);
#30840=ORIENTED_EDGE('',*,*,#21790,.F.);
#30841=ORIENTED_EDGE('',*,*,#21791,.T.);
#30842=ORIENTED_EDGE('',*,*,#21787,.T.);
#30843=ORIENTED_EDGE('',*,*,#21792,.F.);
#30844=ORIENTED_EDGE('',*,*,#21793,.F.);
#30845=ORIENTED_EDGE('',*,*,#21794,.T.);
#30846=ORIENTED_EDGE('',*,*,#21790,.T.);
#30847=ORIENTED_EDGE('',*,*,#21795,.F.);
#30848=ORIENTED_EDGE('',*,*,#21796,.F.);
#30849=ORIENTED_EDGE('',*,*,#21797,.T.);
#30850=ORIENTED_EDGE('',*,*,#21793,.T.);
#30851=ORIENTED_EDGE('',*,*,#21798,.F.);
#30852=ORIENTED_EDGE('',*,*,#21799,.F.);
#30853=ORIENTED_EDGE('',*,*,#21800,.T.);
#30854=ORIENTED_EDGE('',*,*,#21796,.T.);
#30855=ORIENTED_EDGE('',*,*,#21801,.F.);
#30856=ORIENTED_EDGE('',*,*,#21802,.T.);
#30857=ORIENTED_EDGE('',*,*,#21803,.T.);
#30858=ORIENTED_EDGE('',*,*,#21804,.T.);
#30859=ORIENTED_EDGE('',*,*,#21805,.T.);
#30860=ORIENTED_EDGE('',*,*,#21803,.F.);
#30861=ORIENTED_EDGE('',*,*,#21804,.F.);
#30862=ORIENTED_EDGE('',*,*,#21805,.F.);
#30863=ORIENTED_EDGE('',*,*,#21806,.T.);
#30864=ORIENTED_EDGE('',*,*,#21807,.T.);
#30865=ORIENTED_EDGE('',*,*,#21808,.T.);
#30866=ORIENTED_EDGE('',*,*,#21809,.T.);
#30867=ORIENTED_EDGE('',*,*,#21806,.F.);
#30868=ORIENTED_EDGE('',*,*,#21802,.F.);
#30869=ORIENTED_EDGE('',*,*,#21810,.T.);
#30870=ORIENTED_EDGE('',*,*,#21811,.T.);
#30871=ORIENTED_EDGE('',*,*,#21812,.T.);
#30872=ORIENTED_EDGE('',*,*,#21813,.T.);
#30873=ORIENTED_EDGE('',*,*,#21814,.T.);
#30874=ORIENTED_EDGE('',*,*,#21815,.T.);
#30875=ORIENTED_EDGE('',*,*,#21811,.F.);
#30876=ORIENTED_EDGE('',*,*,#21816,.T.);
#30877=ORIENTED_EDGE('',*,*,#21817,.F.);
#30878=ORIENTED_EDGE('',*,*,#21815,.F.);
#30879=ORIENTED_EDGE('',*,*,#21818,.T.);
#30880=ORIENTED_EDGE('',*,*,#21819,.T.);
#30881=ORIENTED_EDGE('',*,*,#21820,.T.);
#30882=ORIENTED_EDGE('',*,*,#21821,.T.);
#30883=ORIENTED_EDGE('',*,*,#21822,.T.);
#30884=ORIENTED_EDGE('',*,*,#21821,.F.);
#30885=ORIENTED_EDGE('',*,*,#21823,.T.);
#30886=ORIENTED_EDGE('',*,*,#21824,.F.);
#30887=ORIENTED_EDGE('',*,*,#21825,.F.);
#30888=ORIENTED_EDGE('',*,*,#21820,.F.);
#30889=ORIENTED_EDGE('',*,*,#21826,.F.);
#30890=ORIENTED_EDGE('',*,*,#21827,.T.);
#30891=ORIENTED_EDGE('',*,*,#21828,.F.);
#30892=ORIENTED_EDGE('',*,*,#21829,.F.);
#30893=ORIENTED_EDGE('',*,*,#21823,.F.);
#30894=ORIENTED_EDGE('',*,*,#21819,.F.);
#30895=ORIENTED_EDGE('',*,*,#21830,.T.);
#30896=ORIENTED_EDGE('',*,*,#21831,.T.);
#30897=ORIENTED_EDGE('',*,*,#21828,.T.);
#30898=ORIENTED_EDGE('',*,*,#21832,.T.);
#30899=ORIENTED_EDGE('',*,*,#21826,.T.);
#30900=ORIENTED_EDGE('',*,*,#21814,.F.);
#30901=ORIENTED_EDGE('',*,*,#21833,.F.);
#30902=ORIENTED_EDGE('',*,*,#21830,.F.);
#30903=ORIENTED_EDGE('',*,*,#21818,.F.);
#30904=ORIENTED_EDGE('',*,*,#21832,.F.);
#30905=ORIENTED_EDGE('',*,*,#21827,.F.);
#30906=ORIENTED_EDGE('',*,*,#21813,.F.);
#30907=ORIENTED_EDGE('',*,*,#21834,.T.);
#30908=ORIENTED_EDGE('',*,*,#21824,.T.);
#30909=ORIENTED_EDGE('',*,*,#21829,.T.);
#30910=ORIENTED_EDGE('',*,*,#21831,.F.);
#30911=ORIENTED_EDGE('',*,*,#21833,.T.);
#30912=ORIENTED_EDGE('',*,*,#21812,.F.);
#30913=ORIENTED_EDGE('',*,*,#21816,.F.);
#30914=ORIENTED_EDGE('',*,*,#21810,.F.);
#30915=ORIENTED_EDGE('',*,*,#21822,.F.);
#30916=ORIENTED_EDGE('',*,*,#21825,.T.);
#30917=ORIENTED_EDGE('',*,*,#21834,.F.);
#30918=ORIENTED_EDGE('',*,*,#21719,.T.);
#30919=ORIENTED_EDGE('',*,*,#21716,.T.);
#30920=ORIENTED_EDGE('',*,*,#21835,.T.);
#30921=ORIENTED_EDGE('',*,*,#21807,.F.);
#30922=ORIENTED_EDGE('',*,*,#21809,.F.);
#30923=ORIENTED_EDGE('',*,*,#21836,.T.);
#30924=ORIENTED_EDGE('',*,*,#21836,.F.);
#30925=ORIENTED_EDGE('',*,*,#21837,.F.);
#30926=ORIENTED_EDGE('',*,*,#21713,.F.);
#30927=ORIENTED_EDGE('',*,*,#21710,.F.);
#30928=ORIENTED_EDGE('',*,*,#21707,.F.);
#30929=ORIENTED_EDGE('',*,*,#21704,.F.);
#30930=ORIENTED_EDGE('',*,*,#21701,.F.);
#30931=ORIENTED_EDGE('',*,*,#21698,.F.);
#30932=ORIENTED_EDGE('',*,*,#21695,.F.);
#30933=ORIENTED_EDGE('',*,*,#21692,.F.);
#30934=ORIENTED_EDGE('',*,*,#21689,.F.);
#30935=ORIENTED_EDGE('',*,*,#21686,.F.);
#30936=ORIENTED_EDGE('',*,*,#21683,.F.);
#30937=ORIENTED_EDGE('',*,*,#21680,.F.);
#30938=ORIENTED_EDGE('',*,*,#21677,.F.);
#30939=ORIENTED_EDGE('',*,*,#21674,.F.);
#30940=ORIENTED_EDGE('',*,*,#21671,.F.);
#30941=ORIENTED_EDGE('',*,*,#21668,.F.);
#30942=ORIENTED_EDGE('',*,*,#21665,.F.);
#30943=ORIENTED_EDGE('',*,*,#21662,.F.);
#30944=ORIENTED_EDGE('',*,*,#21659,.F.);
#30945=ORIENTED_EDGE('',*,*,#21656,.F.);
#30946=ORIENTED_EDGE('',*,*,#21653,.F.);
#30947=ORIENTED_EDGE('',*,*,#21650,.F.);
#30948=ORIENTED_EDGE('',*,*,#21647,.F.);
#30949=ORIENTED_EDGE('',*,*,#21644,.F.);
#30950=ORIENTED_EDGE('',*,*,#21641,.F.);
#30951=ORIENTED_EDGE('',*,*,#21638,.F.);
#30952=ORIENTED_EDGE('',*,*,#21635,.F.);
#30953=ORIENTED_EDGE('',*,*,#21632,.F.);
#30954=ORIENTED_EDGE('',*,*,#21629,.F.);
#30955=ORIENTED_EDGE('',*,*,#21838,.F.);
#30956=ORIENTED_EDGE('',*,*,#21839,.T.);
#30957=ORIENTED_EDGE('',*,*,#21801,.T.);
#30958=ORIENTED_EDGE('',*,*,#21798,.T.);
#30959=ORIENTED_EDGE('',*,*,#21795,.T.);
#30960=ORIENTED_EDGE('',*,*,#21792,.T.);
#30961=ORIENTED_EDGE('',*,*,#21789,.T.);
#30962=ORIENTED_EDGE('',*,*,#21786,.T.);
#30963=ORIENTED_EDGE('',*,*,#21783,.T.);
#30964=ORIENTED_EDGE('',*,*,#21780,.T.);
#30965=ORIENTED_EDGE('',*,*,#21777,.T.);
#30966=ORIENTED_EDGE('',*,*,#21774,.T.);
#30967=ORIENTED_EDGE('',*,*,#21771,.T.);
#30968=ORIENTED_EDGE('',*,*,#21768,.T.);
#30969=ORIENTED_EDGE('',*,*,#21765,.T.);
#30970=ORIENTED_EDGE('',*,*,#21762,.T.);
#30971=ORIENTED_EDGE('',*,*,#21759,.T.);
#30972=ORIENTED_EDGE('',*,*,#21756,.T.);
#30973=ORIENTED_EDGE('',*,*,#21753,.T.);
#30974=ORIENTED_EDGE('',*,*,#21750,.T.);
#30975=ORIENTED_EDGE('',*,*,#21747,.T.);
#30976=ORIENTED_EDGE('',*,*,#21744,.T.);
#30977=ORIENTED_EDGE('',*,*,#21741,.T.);
#30978=ORIENTED_EDGE('',*,*,#21738,.T.);
#30979=ORIENTED_EDGE('',*,*,#21735,.T.);
#30980=ORIENTED_EDGE('',*,*,#21732,.T.);
#30981=ORIENTED_EDGE('',*,*,#21729,.T.);
#30982=ORIENTED_EDGE('',*,*,#21726,.T.);
#30983=ORIENTED_EDGE('',*,*,#21723,.T.);
#30984=ORIENTED_EDGE('',*,*,#21720,.T.);
#30985=ORIENTED_EDGE('',*,*,#21840,.T.);
#30986=ORIENTED_EDGE('',*,*,#21841,.T.);
#30987=ORIENTED_EDGE('',*,*,#21842,.T.);
#30988=ORIENTED_EDGE('',*,*,#21843,.T.);
#30989=ORIENTED_EDGE('',*,*,#21838,.T.);
#30990=ORIENTED_EDGE('',*,*,#21799,.T.);
#30991=ORIENTED_EDGE('',*,*,#21839,.F.);
#30992=ORIENTED_EDGE('',*,*,#21843,.F.);
#30993=ORIENTED_EDGE('',*,*,#21844,.T.);
#30994=ORIENTED_EDGE('',*,*,#21835,.F.);
#30995=ORIENTED_EDGE('',*,*,#21715,.F.);
#30996=ORIENTED_EDGE('',*,*,#21718,.F.);
#30997=ORIENTED_EDGE('',*,*,#21722,.F.);
#30998=ORIENTED_EDGE('',*,*,#21725,.F.);
#30999=ORIENTED_EDGE('',*,*,#21728,.F.);
#31000=ORIENTED_EDGE('',*,*,#21731,.F.);
#31001=ORIENTED_EDGE('',*,*,#21734,.F.);
#31002=ORIENTED_EDGE('',*,*,#21737,.F.);
#31003=ORIENTED_EDGE('',*,*,#21740,.F.);
#31004=ORIENTED_EDGE('',*,*,#21743,.F.);
#31005=ORIENTED_EDGE('',*,*,#21746,.F.);
#31006=ORIENTED_EDGE('',*,*,#21749,.F.);
#31007=ORIENTED_EDGE('',*,*,#21752,.F.);
#31008=ORIENTED_EDGE('',*,*,#21755,.F.);
#31009=ORIENTED_EDGE('',*,*,#21758,.F.);
#31010=ORIENTED_EDGE('',*,*,#21761,.F.);
#31011=ORIENTED_EDGE('',*,*,#21764,.F.);
#31012=ORIENTED_EDGE('',*,*,#21767,.F.);
#31013=ORIENTED_EDGE('',*,*,#21770,.F.);
#31014=ORIENTED_EDGE('',*,*,#21773,.F.);
#31015=ORIENTED_EDGE('',*,*,#21776,.F.);
#31016=ORIENTED_EDGE('',*,*,#21779,.F.);
#31017=ORIENTED_EDGE('',*,*,#21782,.F.);
#31018=ORIENTED_EDGE('',*,*,#21785,.F.);
#31019=ORIENTED_EDGE('',*,*,#21788,.F.);
#31020=ORIENTED_EDGE('',*,*,#21791,.F.);
#31021=ORIENTED_EDGE('',*,*,#21794,.F.);
#31022=ORIENTED_EDGE('',*,*,#21797,.F.);
#31023=ORIENTED_EDGE('',*,*,#21800,.F.);
#31024=ORIENTED_EDGE('',*,*,#21844,.F.);
#31025=ORIENTED_EDGE('',*,*,#21842,.F.);
#31026=ORIENTED_EDGE('',*,*,#21627,.F.);
#31027=ORIENTED_EDGE('',*,*,#21631,.F.);
#31028=ORIENTED_EDGE('',*,*,#21634,.F.);
#31029=ORIENTED_EDGE('',*,*,#21637,.F.);
#31030=ORIENTED_EDGE('',*,*,#21640,.F.);
#31031=ORIENTED_EDGE('',*,*,#21643,.F.);
#31032=ORIENTED_EDGE('',*,*,#21646,.F.);
#31033=ORIENTED_EDGE('',*,*,#21649,.F.);
#31034=ORIENTED_EDGE('',*,*,#21652,.F.);
#31035=ORIENTED_EDGE('',*,*,#21655,.F.);
#31036=ORIENTED_EDGE('',*,*,#21658,.F.);
#31037=ORIENTED_EDGE('',*,*,#21661,.F.);
#31038=ORIENTED_EDGE('',*,*,#21664,.F.);
#31039=ORIENTED_EDGE('',*,*,#21667,.F.);
#31040=ORIENTED_EDGE('',*,*,#21670,.F.);
#31041=ORIENTED_EDGE('',*,*,#21673,.F.);
#31042=ORIENTED_EDGE('',*,*,#21676,.F.);
#31043=ORIENTED_EDGE('',*,*,#21679,.F.);
#31044=ORIENTED_EDGE('',*,*,#21682,.F.);
#31045=ORIENTED_EDGE('',*,*,#21685,.F.);
#31046=ORIENTED_EDGE('',*,*,#21688,.F.);
#31047=ORIENTED_EDGE('',*,*,#21691,.F.);
#31048=ORIENTED_EDGE('',*,*,#21694,.F.);
#31049=ORIENTED_EDGE('',*,*,#21697,.F.);
#31050=ORIENTED_EDGE('',*,*,#21700,.F.);
#31051=ORIENTED_EDGE('',*,*,#21703,.F.);
#31052=ORIENTED_EDGE('',*,*,#21706,.F.);
#31053=ORIENTED_EDGE('',*,*,#21709,.F.);
#31054=ORIENTED_EDGE('',*,*,#21712,.F.);
#31055=ORIENTED_EDGE('',*,*,#21845,.F.);
#31056=ORIENTED_EDGE('',*,*,#21711,.T.);
#31057=ORIENTED_EDGE('',*,*,#21837,.T.);
#31058=ORIENTED_EDGE('',*,*,#21808,.F.);
#31059=ORIENTED_EDGE('',*,*,#21845,.T.);
#31060=ORIENTED_EDGE('',*,*,#21846,.F.);
#31061=ORIENTED_EDGE('',*,*,#21847,.T.);
#31062=ORIENTED_EDGE('',*,*,#21848,.F.);
#31063=ORIENTED_EDGE('',*,*,#21849,.F.);
#31064=ORIENTED_EDGE('',*,*,#21850,.F.);
#31065=ORIENTED_EDGE('',*,*,#21849,.T.);
#31066=ORIENTED_EDGE('',*,*,#21851,.T.);
#31067=ORIENTED_EDGE('',*,*,#21852,.F.);
#31068=ORIENTED_EDGE('',*,*,#21851,.F.);
#31069=ORIENTED_EDGE('',*,*,#21848,.T.);
#31070=ORIENTED_EDGE('',*,*,#21853,.T.);
#31071=ORIENTED_EDGE('',*,*,#21854,.F.);
#31072=ORIENTED_EDGE('',*,*,#21853,.F.);
#31073=ORIENTED_EDGE('',*,*,#21847,.F.);
#31074=ORIENTED_EDGE('',*,*,#21855,.F.);
#31075=ORIENTED_EDGE('',*,*,#21856,.T.);
#31076=ORIENTED_EDGE('',*,*,#21857,.F.);
#31077=ORIENTED_EDGE('',*,*,#21858,.F.);
#31078=ORIENTED_EDGE('',*,*,#21859,.F.);
#31079=ORIENTED_EDGE('',*,*,#21858,.T.);
#31080=ORIENTED_EDGE('',*,*,#21860,.T.);
#31081=ORIENTED_EDGE('',*,*,#21861,.F.);
#31082=ORIENTED_EDGE('',*,*,#21860,.F.);
#31083=ORIENTED_EDGE('',*,*,#21857,.T.);
#31084=ORIENTED_EDGE('',*,*,#21862,.T.);
#31085=ORIENTED_EDGE('',*,*,#21863,.F.);
#31086=ORIENTED_EDGE('',*,*,#21862,.F.);
#31087=ORIENTED_EDGE('',*,*,#21856,.F.);
#31088=ORIENTED_EDGE('',*,*,#21864,.F.);
#31089=ORIENTED_EDGE('',*,*,#21865,.T.);
#31090=ORIENTED_EDGE('',*,*,#21866,.F.);
#31091=ORIENTED_EDGE('',*,*,#21867,.F.);
#31092=ORIENTED_EDGE('',*,*,#21868,.F.);
#31093=ORIENTED_EDGE('',*,*,#21867,.T.);
#31094=ORIENTED_EDGE('',*,*,#21869,.T.);
#31095=ORIENTED_EDGE('',*,*,#21870,.F.);
#31096=ORIENTED_EDGE('',*,*,#21869,.F.);
#31097=ORIENTED_EDGE('',*,*,#21866,.T.);
#31098=ORIENTED_EDGE('',*,*,#21871,.T.);
#31099=ORIENTED_EDGE('',*,*,#21872,.F.);
#31100=ORIENTED_EDGE('',*,*,#21871,.F.);
#31101=ORIENTED_EDGE('',*,*,#21865,.F.);
#31102=ORIENTED_EDGE('',*,*,#21873,.F.);
#31103=ORIENTED_EDGE('',*,*,#21874,.T.);
#31104=ORIENTED_EDGE('',*,*,#21875,.F.);
#31105=ORIENTED_EDGE('',*,*,#21876,.F.);
#31106=ORIENTED_EDGE('',*,*,#21877,.F.);
#31107=ORIENTED_EDGE('',*,*,#21876,.T.);
#31108=ORIENTED_EDGE('',*,*,#21878,.T.);
#31109=ORIENTED_EDGE('',*,*,#21879,.F.);
#31110=ORIENTED_EDGE('',*,*,#21878,.F.);
#31111=ORIENTED_EDGE('',*,*,#21875,.T.);
#31112=ORIENTED_EDGE('',*,*,#21880,.T.);
#31113=ORIENTED_EDGE('',*,*,#21881,.F.);
#31114=ORIENTED_EDGE('',*,*,#21880,.F.);
#31115=ORIENTED_EDGE('',*,*,#21874,.F.);
#31116=ORIENTED_EDGE('',*,*,#21882,.F.);
#31117=ORIENTED_EDGE('',*,*,#21883,.T.);
#31118=ORIENTED_EDGE('',*,*,#21884,.F.);
#31119=ORIENTED_EDGE('',*,*,#21885,.F.);
#31120=ORIENTED_EDGE('',*,*,#21886,.F.);
#31121=ORIENTED_EDGE('',*,*,#21885,.T.);
#31122=ORIENTED_EDGE('',*,*,#21887,.T.);
#31123=ORIENTED_EDGE('',*,*,#21888,.F.);
#31124=ORIENTED_EDGE('',*,*,#21887,.F.);
#31125=ORIENTED_EDGE('',*,*,#21884,.T.);
#31126=ORIENTED_EDGE('',*,*,#21889,.T.);
#31127=ORIENTED_EDGE('',*,*,#21890,.F.);
#31128=ORIENTED_EDGE('',*,*,#21889,.F.);
#31129=ORIENTED_EDGE('',*,*,#21883,.F.);
#31130=ORIENTED_EDGE('',*,*,#21891,.F.);
#31131=ORIENTED_EDGE('',*,*,#21892,.T.);
#31132=ORIENTED_EDGE('',*,*,#21893,.F.);
#31133=ORIENTED_EDGE('',*,*,#21894,.F.);
#31134=ORIENTED_EDGE('',*,*,#21895,.F.);
#31135=ORIENTED_EDGE('',*,*,#21894,.T.);
#31136=ORIENTED_EDGE('',*,*,#21896,.T.);
#31137=ORIENTED_EDGE('',*,*,#21897,.F.);
#31138=ORIENTED_EDGE('',*,*,#21896,.F.);
#31139=ORIENTED_EDGE('',*,*,#21893,.T.);
#31140=ORIENTED_EDGE('',*,*,#21898,.T.);
#31141=ORIENTED_EDGE('',*,*,#21899,.F.);
#31142=ORIENTED_EDGE('',*,*,#21898,.F.);
#31143=ORIENTED_EDGE('',*,*,#21892,.F.);
#31144=ORIENTED_EDGE('',*,*,#21900,.F.);
#31145=ORIENTED_EDGE('',*,*,#21901,.T.);
#31146=ORIENTED_EDGE('',*,*,#21902,.F.);
#31147=ORIENTED_EDGE('',*,*,#21903,.F.);
#31148=ORIENTED_EDGE('',*,*,#21904,.F.);
#31149=ORIENTED_EDGE('',*,*,#21903,.T.);
#31150=ORIENTED_EDGE('',*,*,#21905,.T.);
#31151=ORIENTED_EDGE('',*,*,#21906,.F.);
#31152=ORIENTED_EDGE('',*,*,#21905,.F.);
#31153=ORIENTED_EDGE('',*,*,#21902,.T.);
#31154=ORIENTED_EDGE('',*,*,#21907,.T.);
#31155=ORIENTED_EDGE('',*,*,#21908,.F.);
#31156=ORIENTED_EDGE('',*,*,#21907,.F.);
#31157=ORIENTED_EDGE('',*,*,#21901,.F.);
#31158=ORIENTED_EDGE('',*,*,#21909,.F.);
#31159=ORIENTED_EDGE('',*,*,#21910,.T.);
#31160=ORIENTED_EDGE('',*,*,#21911,.F.);
#31161=ORIENTED_EDGE('',*,*,#21912,.F.);
#31162=ORIENTED_EDGE('',*,*,#21913,.F.);
#31163=ORIENTED_EDGE('',*,*,#21912,.T.);
#31164=ORIENTED_EDGE('',*,*,#21914,.T.);
#31165=ORIENTED_EDGE('',*,*,#21915,.F.);
#31166=ORIENTED_EDGE('',*,*,#21914,.F.);
#31167=ORIENTED_EDGE('',*,*,#21911,.T.);
#31168=ORIENTED_EDGE('',*,*,#21916,.T.);
#31169=ORIENTED_EDGE('',*,*,#21917,.F.);
#31170=ORIENTED_EDGE('',*,*,#21916,.F.);
#31171=ORIENTED_EDGE('',*,*,#21910,.F.);
#31172=ORIENTED_EDGE('',*,*,#21918,.F.);
#31173=ORIENTED_EDGE('',*,*,#21919,.T.);
#31174=ORIENTED_EDGE('',*,*,#21920,.F.);
#31175=ORIENTED_EDGE('',*,*,#21921,.F.);
#31176=ORIENTED_EDGE('',*,*,#21922,.F.);
#31177=ORIENTED_EDGE('',*,*,#21921,.T.);
#31178=ORIENTED_EDGE('',*,*,#21923,.T.);
#31179=ORIENTED_EDGE('',*,*,#21924,.F.);
#31180=ORIENTED_EDGE('',*,*,#21923,.F.);
#31181=ORIENTED_EDGE('',*,*,#21920,.T.);
#31182=ORIENTED_EDGE('',*,*,#21925,.T.);
#31183=ORIENTED_EDGE('',*,*,#21926,.F.);
#31184=ORIENTED_EDGE('',*,*,#21925,.F.);
#31185=ORIENTED_EDGE('',*,*,#21919,.F.);
#31186=ORIENTED_EDGE('',*,*,#21927,.F.);
#31187=ORIENTED_EDGE('',*,*,#21928,.T.);
#31188=ORIENTED_EDGE('',*,*,#21929,.F.);
#31189=ORIENTED_EDGE('',*,*,#21930,.F.);
#31190=ORIENTED_EDGE('',*,*,#21931,.F.);
#31191=ORIENTED_EDGE('',*,*,#21930,.T.);
#31192=ORIENTED_EDGE('',*,*,#21932,.T.);
#31193=ORIENTED_EDGE('',*,*,#21933,.F.);
#31194=ORIENTED_EDGE('',*,*,#21932,.F.);
#31195=ORIENTED_EDGE('',*,*,#21929,.T.);
#31196=ORIENTED_EDGE('',*,*,#21934,.T.);
#31197=ORIENTED_EDGE('',*,*,#21935,.F.);
#31198=ORIENTED_EDGE('',*,*,#21934,.F.);
#31199=ORIENTED_EDGE('',*,*,#21928,.F.);
#31200=ORIENTED_EDGE('',*,*,#21936,.F.);
#31201=ORIENTED_EDGE('',*,*,#21937,.T.);
#31202=ORIENTED_EDGE('',*,*,#21938,.F.);
#31203=ORIENTED_EDGE('',*,*,#21939,.F.);
#31204=ORIENTED_EDGE('',*,*,#21940,.F.);
#31205=ORIENTED_EDGE('',*,*,#21939,.T.);
#31206=ORIENTED_EDGE('',*,*,#21941,.T.);
#31207=ORIENTED_EDGE('',*,*,#21942,.F.);
#31208=ORIENTED_EDGE('',*,*,#21941,.F.);
#31209=ORIENTED_EDGE('',*,*,#21938,.T.);
#31210=ORIENTED_EDGE('',*,*,#21943,.T.);
#31211=ORIENTED_EDGE('',*,*,#21944,.F.);
#31212=ORIENTED_EDGE('',*,*,#21943,.F.);
#31213=ORIENTED_EDGE('',*,*,#21937,.F.);
#31214=ORIENTED_EDGE('',*,*,#21945,.F.);
#31215=ORIENTED_EDGE('',*,*,#21946,.T.);
#31216=ORIENTED_EDGE('',*,*,#21947,.F.);
#31217=ORIENTED_EDGE('',*,*,#21948,.F.);
#31218=ORIENTED_EDGE('',*,*,#21949,.F.);
#31219=ORIENTED_EDGE('',*,*,#21948,.T.);
#31220=ORIENTED_EDGE('',*,*,#21950,.T.);
#31221=ORIENTED_EDGE('',*,*,#21951,.F.);
#31222=ORIENTED_EDGE('',*,*,#21950,.F.);
#31223=ORIENTED_EDGE('',*,*,#21947,.T.);
#31224=ORIENTED_EDGE('',*,*,#21952,.T.);
#31225=ORIENTED_EDGE('',*,*,#21953,.F.);
#31226=ORIENTED_EDGE('',*,*,#21952,.F.);
#31227=ORIENTED_EDGE('',*,*,#21946,.F.);
#31228=ORIENTED_EDGE('',*,*,#21954,.F.);
#31229=ORIENTED_EDGE('',*,*,#21955,.T.);
#31230=ORIENTED_EDGE('',*,*,#21956,.F.);
#31231=ORIENTED_EDGE('',*,*,#21957,.F.);
#31232=ORIENTED_EDGE('',*,*,#21958,.F.);
#31233=ORIENTED_EDGE('',*,*,#21957,.T.);
#31234=ORIENTED_EDGE('',*,*,#21959,.T.);
#31235=ORIENTED_EDGE('',*,*,#21960,.F.);
#31236=ORIENTED_EDGE('',*,*,#21959,.F.);
#31237=ORIENTED_EDGE('',*,*,#21956,.T.);
#31238=ORIENTED_EDGE('',*,*,#21961,.T.);
#31239=ORIENTED_EDGE('',*,*,#21962,.F.);
#31240=ORIENTED_EDGE('',*,*,#21961,.F.);
#31241=ORIENTED_EDGE('',*,*,#21955,.F.);
#31242=ORIENTED_EDGE('',*,*,#21963,.F.);
#31243=ORIENTED_EDGE('',*,*,#21964,.T.);
#31244=ORIENTED_EDGE('',*,*,#21965,.F.);
#31245=ORIENTED_EDGE('',*,*,#21966,.F.);
#31246=ORIENTED_EDGE('',*,*,#21967,.F.);
#31247=ORIENTED_EDGE('',*,*,#21966,.T.);
#31248=ORIENTED_EDGE('',*,*,#21968,.T.);
#31249=ORIENTED_EDGE('',*,*,#21969,.F.);
#31250=ORIENTED_EDGE('',*,*,#21968,.F.);
#31251=ORIENTED_EDGE('',*,*,#21965,.T.);
#31252=ORIENTED_EDGE('',*,*,#21970,.T.);
#31253=ORIENTED_EDGE('',*,*,#21971,.F.);
#31254=ORIENTED_EDGE('',*,*,#21970,.F.);
#31255=ORIENTED_EDGE('',*,*,#21964,.F.);
#31256=ORIENTED_EDGE('',*,*,#21972,.F.);
#31257=ORIENTED_EDGE('',*,*,#21973,.T.);
#31258=ORIENTED_EDGE('',*,*,#21974,.F.);
#31259=ORIENTED_EDGE('',*,*,#21975,.F.);
#31260=ORIENTED_EDGE('',*,*,#21976,.F.);
#31261=ORIENTED_EDGE('',*,*,#21975,.T.);
#31262=ORIENTED_EDGE('',*,*,#21977,.T.);
#31263=ORIENTED_EDGE('',*,*,#21978,.F.);
#31264=ORIENTED_EDGE('',*,*,#21977,.F.);
#31265=ORIENTED_EDGE('',*,*,#21974,.T.);
#31266=ORIENTED_EDGE('',*,*,#21979,.T.);
#31267=ORIENTED_EDGE('',*,*,#21980,.F.);
#31268=ORIENTED_EDGE('',*,*,#21979,.F.);
#31269=ORIENTED_EDGE('',*,*,#21973,.F.);
#31270=ORIENTED_EDGE('',*,*,#21981,.F.);
#31271=ORIENTED_EDGE('',*,*,#21982,.T.);
#31272=ORIENTED_EDGE('',*,*,#21983,.F.);
#31273=ORIENTED_EDGE('',*,*,#21984,.F.);
#31274=ORIENTED_EDGE('',*,*,#21985,.F.);
#31275=ORIENTED_EDGE('',*,*,#21984,.T.);
#31276=ORIENTED_EDGE('',*,*,#21986,.T.);
#31277=ORIENTED_EDGE('',*,*,#21987,.F.);
#31278=ORIENTED_EDGE('',*,*,#21986,.F.);
#31279=ORIENTED_EDGE('',*,*,#21983,.T.);
#31280=ORIENTED_EDGE('',*,*,#21988,.T.);
#31281=ORIENTED_EDGE('',*,*,#21989,.F.);
#31282=ORIENTED_EDGE('',*,*,#21988,.F.);
#31283=ORIENTED_EDGE('',*,*,#21982,.F.);
#31284=ORIENTED_EDGE('',*,*,#21990,.F.);
#31285=ORIENTED_EDGE('',*,*,#21991,.T.);
#31286=ORIENTED_EDGE('',*,*,#21992,.F.);
#31287=ORIENTED_EDGE('',*,*,#21993,.F.);
#31288=ORIENTED_EDGE('',*,*,#21994,.F.);
#31289=ORIENTED_EDGE('',*,*,#21993,.T.);
#31290=ORIENTED_EDGE('',*,*,#21995,.T.);
#31291=ORIENTED_EDGE('',*,*,#21996,.F.);
#31292=ORIENTED_EDGE('',*,*,#21995,.F.);
#31293=ORIENTED_EDGE('',*,*,#21992,.T.);
#31294=ORIENTED_EDGE('',*,*,#21997,.T.);
#31295=ORIENTED_EDGE('',*,*,#21998,.F.);
#31296=ORIENTED_EDGE('',*,*,#21997,.F.);
#31297=ORIENTED_EDGE('',*,*,#21991,.F.);
#31298=ORIENTED_EDGE('',*,*,#21999,.F.);
#31299=ORIENTED_EDGE('',*,*,#22000,.T.);
#31300=ORIENTED_EDGE('',*,*,#22001,.F.);
#31301=ORIENTED_EDGE('',*,*,#22002,.F.);
#31302=ORIENTED_EDGE('',*,*,#22003,.F.);
#31303=ORIENTED_EDGE('',*,*,#22002,.T.);
#31304=ORIENTED_EDGE('',*,*,#22004,.T.);
#31305=ORIENTED_EDGE('',*,*,#22005,.F.);
#31306=ORIENTED_EDGE('',*,*,#22006,.F.);
#31307=ORIENTED_EDGE('',*,*,#22004,.F.);
#31308=ORIENTED_EDGE('',*,*,#22001,.T.);
#31309=ORIENTED_EDGE('',*,*,#22007,.T.);
#31310=ORIENTED_EDGE('',*,*,#22008,.F.);
#31311=ORIENTED_EDGE('',*,*,#22007,.F.);
#31312=ORIENTED_EDGE('',*,*,#22000,.F.);
#31313=ORIENTED_EDGE('',*,*,#22009,.F.);
#31314=ORIENTED_EDGE('',*,*,#22010,.F.);
#31315=ORIENTED_EDGE('',*,*,#22011,.T.);
#31316=ORIENTED_EDGE('',*,*,#22012,.F.);
#31317=ORIENTED_EDGE('',*,*,#22013,.F.);
#31318=ORIENTED_EDGE('',*,*,#22014,.F.);
#31319=ORIENTED_EDGE('',*,*,#22013,.T.);
#31320=ORIENTED_EDGE('',*,*,#22015,.T.);
#31321=ORIENTED_EDGE('',*,*,#22016,.F.);
#31322=ORIENTED_EDGE('',*,*,#22015,.F.);
#31323=ORIENTED_EDGE('',*,*,#22012,.T.);
#31324=ORIENTED_EDGE('',*,*,#22017,.T.);
#31325=ORIENTED_EDGE('',*,*,#22018,.F.);
#31326=ORIENTED_EDGE('',*,*,#22017,.F.);
#31327=ORIENTED_EDGE('',*,*,#22011,.F.);
#31328=ORIENTED_EDGE('',*,*,#22019,.F.);
#31329=ORIENTED_EDGE('',*,*,#22020,.T.);
#31330=ORIENTED_EDGE('',*,*,#22021,.F.);
#31331=ORIENTED_EDGE('',*,*,#22022,.F.);
#31332=ORIENTED_EDGE('',*,*,#22023,.F.);
#31333=ORIENTED_EDGE('',*,*,#22022,.T.);
#31334=ORIENTED_EDGE('',*,*,#22024,.T.);
#31335=ORIENTED_EDGE('',*,*,#22025,.F.);
#31336=ORIENTED_EDGE('',*,*,#22024,.F.);
#31337=ORIENTED_EDGE('',*,*,#22021,.T.);
#31338=ORIENTED_EDGE('',*,*,#22026,.T.);
#31339=ORIENTED_EDGE('',*,*,#22027,.F.);
#31340=ORIENTED_EDGE('',*,*,#22026,.F.);
#31341=ORIENTED_EDGE('',*,*,#22020,.F.);
#31342=ORIENTED_EDGE('',*,*,#22028,.F.);
#31343=ORIENTED_EDGE('',*,*,#22029,.T.);
#31344=ORIENTED_EDGE('',*,*,#22030,.F.);
#31345=ORIENTED_EDGE('',*,*,#22031,.F.);
#31346=ORIENTED_EDGE('',*,*,#22032,.F.);
#31347=ORIENTED_EDGE('',*,*,#22031,.T.);
#31348=ORIENTED_EDGE('',*,*,#22033,.T.);
#31349=ORIENTED_EDGE('',*,*,#22034,.F.);
#31350=ORIENTED_EDGE('',*,*,#22033,.F.);
#31351=ORIENTED_EDGE('',*,*,#22030,.T.);
#31352=ORIENTED_EDGE('',*,*,#22035,.T.);
#31353=ORIENTED_EDGE('',*,*,#22036,.F.);
#31354=ORIENTED_EDGE('',*,*,#22035,.F.);
#31355=ORIENTED_EDGE('',*,*,#22029,.F.);
#31356=ORIENTED_EDGE('',*,*,#22037,.F.);
#31357=ORIENTED_EDGE('',*,*,#22038,.T.);
#31358=ORIENTED_EDGE('',*,*,#22039,.F.);
#31359=ORIENTED_EDGE('',*,*,#22040,.F.);
#31360=ORIENTED_EDGE('',*,*,#22041,.F.);
#31361=ORIENTED_EDGE('',*,*,#22040,.T.);
#31362=ORIENTED_EDGE('',*,*,#22042,.T.);
#31363=ORIENTED_EDGE('',*,*,#22043,.F.);
#31364=ORIENTED_EDGE('',*,*,#22042,.F.);
#31365=ORIENTED_EDGE('',*,*,#22039,.T.);
#31366=ORIENTED_EDGE('',*,*,#22044,.T.);
#31367=ORIENTED_EDGE('',*,*,#22045,.F.);
#31368=ORIENTED_EDGE('',*,*,#22044,.F.);
#31369=ORIENTED_EDGE('',*,*,#22038,.F.);
#31370=ORIENTED_EDGE('',*,*,#22046,.F.);
#31371=ORIENTED_EDGE('',*,*,#22047,.T.);
#31372=ORIENTED_EDGE('',*,*,#22048,.F.);
#31373=ORIENTED_EDGE('',*,*,#22049,.F.);
#31374=ORIENTED_EDGE('',*,*,#22050,.F.);
#31375=ORIENTED_EDGE('',*,*,#22049,.T.);
#31376=ORIENTED_EDGE('',*,*,#22051,.T.);
#31377=ORIENTED_EDGE('',*,*,#22052,.F.);
#31378=ORIENTED_EDGE('',*,*,#22051,.F.);
#31379=ORIENTED_EDGE('',*,*,#22048,.T.);
#31380=ORIENTED_EDGE('',*,*,#22053,.T.);
#31381=ORIENTED_EDGE('',*,*,#22054,.F.);
#31382=ORIENTED_EDGE('',*,*,#22053,.F.);
#31383=ORIENTED_EDGE('',*,*,#22047,.F.);
#31384=ORIENTED_EDGE('',*,*,#22055,.F.);
#31385=ORIENTED_EDGE('',*,*,#22056,.T.);
#31386=ORIENTED_EDGE('',*,*,#22057,.F.);
#31387=ORIENTED_EDGE('',*,*,#22058,.F.);
#31388=ORIENTED_EDGE('',*,*,#22059,.F.);
#31389=ORIENTED_EDGE('',*,*,#22058,.T.);
#31390=ORIENTED_EDGE('',*,*,#22060,.T.);
#31391=ORIENTED_EDGE('',*,*,#22061,.F.);
#31392=ORIENTED_EDGE('',*,*,#22060,.F.);
#31393=ORIENTED_EDGE('',*,*,#22057,.T.);
#31394=ORIENTED_EDGE('',*,*,#22062,.T.);
#31395=ORIENTED_EDGE('',*,*,#22063,.F.);
#31396=ORIENTED_EDGE('',*,*,#22062,.F.);
#31397=ORIENTED_EDGE('',*,*,#22056,.F.);
#31398=ORIENTED_EDGE('',*,*,#22064,.F.);
#31399=ORIENTED_EDGE('',*,*,#22065,.T.);
#31400=ORIENTED_EDGE('',*,*,#22066,.F.);
#31401=ORIENTED_EDGE('',*,*,#22067,.F.);
#31402=ORIENTED_EDGE('',*,*,#22068,.F.);
#31403=ORIENTED_EDGE('',*,*,#22067,.T.);
#31404=ORIENTED_EDGE('',*,*,#22069,.T.);
#31405=ORIENTED_EDGE('',*,*,#22070,.F.);
#31406=ORIENTED_EDGE('',*,*,#22069,.F.);
#31407=ORIENTED_EDGE('',*,*,#22066,.T.);
#31408=ORIENTED_EDGE('',*,*,#22071,.T.);
#31409=ORIENTED_EDGE('',*,*,#22072,.F.);
#31410=ORIENTED_EDGE('',*,*,#22071,.F.);
#31411=ORIENTED_EDGE('',*,*,#22065,.F.);
#31412=ORIENTED_EDGE('',*,*,#22073,.F.);
#31413=ORIENTED_EDGE('',*,*,#22074,.T.);
#31414=ORIENTED_EDGE('',*,*,#22075,.F.);
#31415=ORIENTED_EDGE('',*,*,#22076,.F.);
#31416=ORIENTED_EDGE('',*,*,#22077,.F.);
#31417=ORIENTED_EDGE('',*,*,#22076,.T.);
#31418=ORIENTED_EDGE('',*,*,#22078,.T.);
#31419=ORIENTED_EDGE('',*,*,#22079,.F.);
#31420=ORIENTED_EDGE('',*,*,#22078,.F.);
#31421=ORIENTED_EDGE('',*,*,#22075,.T.);
#31422=ORIENTED_EDGE('',*,*,#22080,.T.);
#31423=ORIENTED_EDGE('',*,*,#22081,.F.);
#31424=ORIENTED_EDGE('',*,*,#22080,.F.);
#31425=ORIENTED_EDGE('',*,*,#22074,.F.);
#31426=ORIENTED_EDGE('',*,*,#22082,.F.);
#31427=ORIENTED_EDGE('',*,*,#22083,.T.);
#31428=ORIENTED_EDGE('',*,*,#22084,.F.);
#31429=ORIENTED_EDGE('',*,*,#22085,.F.);
#31430=ORIENTED_EDGE('',*,*,#22086,.F.);
#31431=ORIENTED_EDGE('',*,*,#22085,.T.);
#31432=ORIENTED_EDGE('',*,*,#22087,.T.);
#31433=ORIENTED_EDGE('',*,*,#22088,.F.);
#31434=ORIENTED_EDGE('',*,*,#22087,.F.);
#31435=ORIENTED_EDGE('',*,*,#22084,.T.);
#31436=ORIENTED_EDGE('',*,*,#22089,.T.);
#31437=ORIENTED_EDGE('',*,*,#22090,.F.);
#31438=ORIENTED_EDGE('',*,*,#22089,.F.);
#31439=ORIENTED_EDGE('',*,*,#22083,.F.);
#31440=ORIENTED_EDGE('',*,*,#22091,.F.);
#31441=ORIENTED_EDGE('',*,*,#22092,.T.);
#31442=ORIENTED_EDGE('',*,*,#22093,.F.);
#31443=ORIENTED_EDGE('',*,*,#22094,.F.);
#31444=ORIENTED_EDGE('',*,*,#22095,.F.);
#31445=ORIENTED_EDGE('',*,*,#22094,.T.);
#31446=ORIENTED_EDGE('',*,*,#22096,.T.);
#31447=ORIENTED_EDGE('',*,*,#22097,.F.);
#31448=ORIENTED_EDGE('',*,*,#22096,.F.);
#31449=ORIENTED_EDGE('',*,*,#22093,.T.);
#31450=ORIENTED_EDGE('',*,*,#22098,.T.);
#31451=ORIENTED_EDGE('',*,*,#22099,.F.);
#31452=ORIENTED_EDGE('',*,*,#22098,.F.);
#31453=ORIENTED_EDGE('',*,*,#22092,.F.);
#31454=ORIENTED_EDGE('',*,*,#22100,.F.);
#31455=ORIENTED_EDGE('',*,*,#22101,.T.);
#31456=ORIENTED_EDGE('',*,*,#22102,.F.);
#31457=ORIENTED_EDGE('',*,*,#22103,.F.);
#31458=ORIENTED_EDGE('',*,*,#22104,.F.);
#31459=ORIENTED_EDGE('',*,*,#22103,.T.);
#31460=ORIENTED_EDGE('',*,*,#22105,.T.);
#31461=ORIENTED_EDGE('',*,*,#22106,.F.);
#31462=ORIENTED_EDGE('',*,*,#22105,.F.);
#31463=ORIENTED_EDGE('',*,*,#22102,.T.);
#31464=ORIENTED_EDGE('',*,*,#22107,.T.);
#31465=ORIENTED_EDGE('',*,*,#22108,.F.);
#31466=ORIENTED_EDGE('',*,*,#22107,.F.);
#31467=ORIENTED_EDGE('',*,*,#22101,.F.);
#31468=ORIENTED_EDGE('',*,*,#22109,.F.);
#31469=ORIENTED_EDGE('',*,*,#22110,.T.);
#31470=ORIENTED_EDGE('',*,*,#22111,.F.);
#31471=ORIENTED_EDGE('',*,*,#22112,.F.);
#31472=ORIENTED_EDGE('',*,*,#22113,.F.);
#31473=ORIENTED_EDGE('',*,*,#22112,.T.);
#31474=ORIENTED_EDGE('',*,*,#22114,.T.);
#31475=ORIENTED_EDGE('',*,*,#22115,.F.);
#31476=ORIENTED_EDGE('',*,*,#22114,.F.);
#31477=ORIENTED_EDGE('',*,*,#22111,.T.);
#31478=ORIENTED_EDGE('',*,*,#22116,.T.);
#31479=ORIENTED_EDGE('',*,*,#22117,.F.);
#31480=ORIENTED_EDGE('',*,*,#22116,.F.);
#31481=ORIENTED_EDGE('',*,*,#22110,.F.);
#31482=ORIENTED_EDGE('',*,*,#22118,.F.);
#31483=ORIENTED_EDGE('',*,*,#22119,.T.);
#31484=ORIENTED_EDGE('',*,*,#22120,.F.);
#31485=ORIENTED_EDGE('',*,*,#22121,.F.);
#31486=ORIENTED_EDGE('',*,*,#22122,.F.);
#31487=ORIENTED_EDGE('',*,*,#22121,.T.);
#31488=ORIENTED_EDGE('',*,*,#22123,.T.);
#31489=ORIENTED_EDGE('',*,*,#22124,.F.);
#31490=ORIENTED_EDGE('',*,*,#22123,.F.);
#31491=ORIENTED_EDGE('',*,*,#22120,.T.);
#31492=ORIENTED_EDGE('',*,*,#22125,.T.);
#31493=ORIENTED_EDGE('',*,*,#22126,.F.);
#31494=ORIENTED_EDGE('',*,*,#22125,.F.);
#31495=ORIENTED_EDGE('',*,*,#22119,.F.);
#31496=ORIENTED_EDGE('',*,*,#22127,.F.);
#31497=ORIENTED_EDGE('',*,*,#22128,.T.);
#31498=ORIENTED_EDGE('',*,*,#22129,.F.);
#31499=ORIENTED_EDGE('',*,*,#22130,.F.);
#31500=ORIENTED_EDGE('',*,*,#22131,.F.);
#31501=ORIENTED_EDGE('',*,*,#22130,.T.);
#31502=ORIENTED_EDGE('',*,*,#22132,.T.);
#31503=ORIENTED_EDGE('',*,*,#22133,.F.);
#31504=ORIENTED_EDGE('',*,*,#22132,.F.);
#31505=ORIENTED_EDGE('',*,*,#22129,.T.);
#31506=ORIENTED_EDGE('',*,*,#22134,.T.);
#31507=ORIENTED_EDGE('',*,*,#22135,.F.);
#31508=ORIENTED_EDGE('',*,*,#22134,.F.);
#31509=ORIENTED_EDGE('',*,*,#22128,.F.);
#31510=ORIENTED_EDGE('',*,*,#22136,.F.);
#31511=ORIENTED_EDGE('',*,*,#22137,.T.);
#31512=ORIENTED_EDGE('',*,*,#22138,.F.);
#31513=ORIENTED_EDGE('',*,*,#22139,.F.);
#31514=ORIENTED_EDGE('',*,*,#22140,.F.);
#31515=ORIENTED_EDGE('',*,*,#22139,.T.);
#31516=ORIENTED_EDGE('',*,*,#22141,.T.);
#31517=ORIENTED_EDGE('',*,*,#22142,.F.);
#31518=ORIENTED_EDGE('',*,*,#22141,.F.);
#31519=ORIENTED_EDGE('',*,*,#22138,.T.);
#31520=ORIENTED_EDGE('',*,*,#22143,.T.);
#31521=ORIENTED_EDGE('',*,*,#22144,.F.);
#31522=ORIENTED_EDGE('',*,*,#22143,.F.);
#31523=ORIENTED_EDGE('',*,*,#22137,.F.);
#31524=ORIENTED_EDGE('',*,*,#22145,.F.);
#31525=ORIENTED_EDGE('',*,*,#22146,.T.);
#31526=ORIENTED_EDGE('',*,*,#22147,.F.);
#31527=ORIENTED_EDGE('',*,*,#22148,.F.);
#31528=ORIENTED_EDGE('',*,*,#22149,.F.);
#31529=ORIENTED_EDGE('',*,*,#22148,.T.);
#31530=ORIENTED_EDGE('',*,*,#22150,.T.);
#31531=ORIENTED_EDGE('',*,*,#22151,.F.);
#31532=ORIENTED_EDGE('',*,*,#22150,.F.);
#31533=ORIENTED_EDGE('',*,*,#22147,.T.);
#31534=ORIENTED_EDGE('',*,*,#22152,.T.);
#31535=ORIENTED_EDGE('',*,*,#22153,.F.);
#31536=ORIENTED_EDGE('',*,*,#22152,.F.);
#31537=ORIENTED_EDGE('',*,*,#22146,.F.);
#31538=ORIENTED_EDGE('',*,*,#22154,.F.);
#31539=ORIENTED_EDGE('',*,*,#22155,.T.);
#31540=ORIENTED_EDGE('',*,*,#22156,.F.);
#31541=ORIENTED_EDGE('',*,*,#22157,.F.);
#31542=ORIENTED_EDGE('',*,*,#22158,.F.);
#31543=ORIENTED_EDGE('',*,*,#22157,.T.);
#31544=ORIENTED_EDGE('',*,*,#22159,.T.);
#31545=ORIENTED_EDGE('',*,*,#22160,.F.);
#31546=ORIENTED_EDGE('',*,*,#22159,.F.);
#31547=ORIENTED_EDGE('',*,*,#22156,.T.);
#31548=ORIENTED_EDGE('',*,*,#22161,.T.);
#31549=ORIENTED_EDGE('',*,*,#22162,.F.);
#31550=ORIENTED_EDGE('',*,*,#22161,.F.);
#31551=ORIENTED_EDGE('',*,*,#22155,.F.);
#31552=ORIENTED_EDGE('',*,*,#22163,.F.);
#31553=ORIENTED_EDGE('',*,*,#22164,.T.);
#31554=ORIENTED_EDGE('',*,*,#22165,.F.);
#31555=ORIENTED_EDGE('',*,*,#22166,.F.);
#31556=ORIENTED_EDGE('',*,*,#22167,.F.);
#31557=ORIENTED_EDGE('',*,*,#22166,.T.);
#31558=ORIENTED_EDGE('',*,*,#22168,.T.);
#31559=ORIENTED_EDGE('',*,*,#22169,.F.);
#31560=ORIENTED_EDGE('',*,*,#22168,.F.);
#31561=ORIENTED_EDGE('',*,*,#22165,.T.);
#31562=ORIENTED_EDGE('',*,*,#22170,.T.);
#31563=ORIENTED_EDGE('',*,*,#22171,.F.);
#31564=ORIENTED_EDGE('',*,*,#22170,.F.);
#31565=ORIENTED_EDGE('',*,*,#22164,.F.);
#31566=ORIENTED_EDGE('',*,*,#22172,.F.);
#31567=ORIENTED_EDGE('',*,*,#22173,.T.);
#31568=ORIENTED_EDGE('',*,*,#22009,.T.);
#31569=ORIENTED_EDGE('',*,*,#21999,.T.);
#31570=ORIENTED_EDGE('',*,*,#22003,.T.);
#31571=ORIENTED_EDGE('',*,*,#22174,.T.);
#31572=ORIENTED_EDGE('',*,*,#21817,.T.);
#31573=ORIENTED_EDGE('',*,*,#22174,.F.);
#31574=ORIENTED_EDGE('',*,*,#22005,.T.);
#31575=ORIENTED_EDGE('',*,*,#22006,.T.);
#31576=ORIENTED_EDGE('',*,*,#22008,.T.);
#31577=ORIENTED_EDGE('',*,*,#22173,.F.);
#31578=ORIENTED_EDGE('',*,*,#21852,.T.);
#31579=ORIENTED_EDGE('',*,*,#21854,.T.);
#31580=ORIENTED_EDGE('',*,*,#21846,.T.);
#31581=ORIENTED_EDGE('',*,*,#21850,.T.);
#31582=ORIENTED_EDGE('',*,*,#21861,.T.);
#31583=ORIENTED_EDGE('',*,*,#21863,.T.);
#31584=ORIENTED_EDGE('',*,*,#21855,.T.);
#31585=ORIENTED_EDGE('',*,*,#21859,.T.);
#31586=ORIENTED_EDGE('',*,*,#21870,.T.);
#31587=ORIENTED_EDGE('',*,*,#21872,.T.);
#31588=ORIENTED_EDGE('',*,*,#21864,.T.);
#31589=ORIENTED_EDGE('',*,*,#21868,.T.);
#31590=ORIENTED_EDGE('',*,*,#21879,.T.);
#31591=ORIENTED_EDGE('',*,*,#21881,.T.);
#31592=ORIENTED_EDGE('',*,*,#21873,.T.);
#31593=ORIENTED_EDGE('',*,*,#21877,.T.);
#31594=ORIENTED_EDGE('',*,*,#21888,.T.);
#31595=ORIENTED_EDGE('',*,*,#21890,.T.);
#31596=ORIENTED_EDGE('',*,*,#21882,.T.);
#31597=ORIENTED_EDGE('',*,*,#21886,.T.);
#31598=ORIENTED_EDGE('',*,*,#21897,.T.);
#31599=ORIENTED_EDGE('',*,*,#21899,.T.);
#31600=ORIENTED_EDGE('',*,*,#21891,.T.);
#31601=ORIENTED_EDGE('',*,*,#21895,.T.);
#31602=ORIENTED_EDGE('',*,*,#21906,.T.);
#31603=ORIENTED_EDGE('',*,*,#21908,.T.);
#31604=ORIENTED_EDGE('',*,*,#21900,.T.);
#31605=ORIENTED_EDGE('',*,*,#21904,.T.);
#31606=ORIENTED_EDGE('',*,*,#21915,.T.);
#31607=ORIENTED_EDGE('',*,*,#21917,.T.);
#31608=ORIENTED_EDGE('',*,*,#21909,.T.);
#31609=ORIENTED_EDGE('',*,*,#21913,.T.);
#31610=ORIENTED_EDGE('',*,*,#21924,.T.);
#31611=ORIENTED_EDGE('',*,*,#21926,.T.);
#31612=ORIENTED_EDGE('',*,*,#21918,.T.);
#31613=ORIENTED_EDGE('',*,*,#21922,.T.);
#31614=ORIENTED_EDGE('',*,*,#21933,.T.);
#31615=ORIENTED_EDGE('',*,*,#21935,.T.);
#31616=ORIENTED_EDGE('',*,*,#21927,.T.);
#31617=ORIENTED_EDGE('',*,*,#21931,.T.);
#31618=ORIENTED_EDGE('',*,*,#21942,.T.);
#31619=ORIENTED_EDGE('',*,*,#21944,.T.);
#31620=ORIENTED_EDGE('',*,*,#21936,.T.);
#31621=ORIENTED_EDGE('',*,*,#21940,.T.);
#31622=ORIENTED_EDGE('',*,*,#21951,.T.);
#31623=ORIENTED_EDGE('',*,*,#21953,.T.);
#31624=ORIENTED_EDGE('',*,*,#21945,.T.);
#31625=ORIENTED_EDGE('',*,*,#21949,.T.);
#31626=ORIENTED_EDGE('',*,*,#21960,.T.);
#31627=ORIENTED_EDGE('',*,*,#21962,.T.);
#31628=ORIENTED_EDGE('',*,*,#21954,.T.);
#31629=ORIENTED_EDGE('',*,*,#21958,.T.);
#31630=ORIENTED_EDGE('',*,*,#21969,.T.);
#31631=ORIENTED_EDGE('',*,*,#21971,.T.);
#31632=ORIENTED_EDGE('',*,*,#21963,.T.);
#31633=ORIENTED_EDGE('',*,*,#21967,.T.);
#31634=ORIENTED_EDGE('',*,*,#21978,.T.);
#31635=ORIENTED_EDGE('',*,*,#21980,.T.);
#31636=ORIENTED_EDGE('',*,*,#21972,.T.);
#31637=ORIENTED_EDGE('',*,*,#21976,.T.);
#31638=ORIENTED_EDGE('',*,*,#21987,.T.);
#31639=ORIENTED_EDGE('',*,*,#21989,.T.);
#31640=ORIENTED_EDGE('',*,*,#21981,.T.);
#31641=ORIENTED_EDGE('',*,*,#21985,.T.);
#31642=ORIENTED_EDGE('',*,*,#21996,.T.);
#31643=ORIENTED_EDGE('',*,*,#21998,.T.);
#31644=ORIENTED_EDGE('',*,*,#21990,.T.);
#31645=ORIENTED_EDGE('',*,*,#21994,.T.);
#31646=ORIENTED_EDGE('',*,*,#22016,.T.);
#31647=ORIENTED_EDGE('',*,*,#22018,.T.);
#31648=ORIENTED_EDGE('',*,*,#22010,.T.);
#31649=ORIENTED_EDGE('',*,*,#22014,.T.);
#31650=ORIENTED_EDGE('',*,*,#22025,.T.);
#31651=ORIENTED_EDGE('',*,*,#22027,.T.);
#31652=ORIENTED_EDGE('',*,*,#22019,.T.);
#31653=ORIENTED_EDGE('',*,*,#22023,.T.);
#31654=ORIENTED_EDGE('',*,*,#22034,.T.);
#31655=ORIENTED_EDGE('',*,*,#22036,.T.);
#31656=ORIENTED_EDGE('',*,*,#22028,.T.);
#31657=ORIENTED_EDGE('',*,*,#22032,.T.);
#31658=ORIENTED_EDGE('',*,*,#22043,.T.);
#31659=ORIENTED_EDGE('',*,*,#22045,.T.);
#31660=ORIENTED_EDGE('',*,*,#22037,.T.);
#31661=ORIENTED_EDGE('',*,*,#22041,.T.);
#31662=ORIENTED_EDGE('',*,*,#22052,.T.);
#31663=ORIENTED_EDGE('',*,*,#22054,.T.);
#31664=ORIENTED_EDGE('',*,*,#22046,.T.);
#31665=ORIENTED_EDGE('',*,*,#22050,.T.);
#31666=ORIENTED_EDGE('',*,*,#22061,.T.);
#31667=ORIENTED_EDGE('',*,*,#22063,.T.);
#31668=ORIENTED_EDGE('',*,*,#22055,.T.);
#31669=ORIENTED_EDGE('',*,*,#22059,.T.);
#31670=ORIENTED_EDGE('',*,*,#22070,.T.);
#31671=ORIENTED_EDGE('',*,*,#22072,.T.);
#31672=ORIENTED_EDGE('',*,*,#22064,.T.);
#31673=ORIENTED_EDGE('',*,*,#22068,.T.);
#31674=ORIENTED_EDGE('',*,*,#22079,.T.);
#31675=ORIENTED_EDGE('',*,*,#22081,.T.);
#31676=ORIENTED_EDGE('',*,*,#22073,.T.);
#31677=ORIENTED_EDGE('',*,*,#22077,.T.);
#31678=ORIENTED_EDGE('',*,*,#22088,.T.);
#31679=ORIENTED_EDGE('',*,*,#22090,.T.);
#31680=ORIENTED_EDGE('',*,*,#22082,.T.);
#31681=ORIENTED_EDGE('',*,*,#22086,.T.);
#31682=ORIENTED_EDGE('',*,*,#22097,.T.);
#31683=ORIENTED_EDGE('',*,*,#22099,.T.);
#31684=ORIENTED_EDGE('',*,*,#22091,.T.);
#31685=ORIENTED_EDGE('',*,*,#22095,.T.);
#31686=ORIENTED_EDGE('',*,*,#22106,.T.);
#31687=ORIENTED_EDGE('',*,*,#22108,.T.);
#31688=ORIENTED_EDGE('',*,*,#22100,.T.);
#31689=ORIENTED_EDGE('',*,*,#22104,.T.);
#31690=ORIENTED_EDGE('',*,*,#22115,.T.);
#31691=ORIENTED_EDGE('',*,*,#22117,.T.);
#31692=ORIENTED_EDGE('',*,*,#22109,.T.);
#31693=ORIENTED_EDGE('',*,*,#22113,.T.);
#31694=ORIENTED_EDGE('',*,*,#22124,.T.);
#31695=ORIENTED_EDGE('',*,*,#22126,.T.);
#31696=ORIENTED_EDGE('',*,*,#22118,.T.);
#31697=ORIENTED_EDGE('',*,*,#22122,.T.);
#31698=ORIENTED_EDGE('',*,*,#22133,.T.);
#31699=ORIENTED_EDGE('',*,*,#22135,.T.);
#31700=ORIENTED_EDGE('',*,*,#22127,.T.);
#31701=ORIENTED_EDGE('',*,*,#22131,.T.);
#31702=ORIENTED_EDGE('',*,*,#22142,.T.);
#31703=ORIENTED_EDGE('',*,*,#22144,.T.);
#31704=ORIENTED_EDGE('',*,*,#22136,.T.);
#31705=ORIENTED_EDGE('',*,*,#22140,.T.);
#31706=ORIENTED_EDGE('',*,*,#22151,.T.);
#31707=ORIENTED_EDGE('',*,*,#22153,.T.);
#31708=ORIENTED_EDGE('',*,*,#22145,.T.);
#31709=ORIENTED_EDGE('',*,*,#22149,.T.);
#31710=ORIENTED_EDGE('',*,*,#22160,.T.);
#31711=ORIENTED_EDGE('',*,*,#22162,.T.);
#31712=ORIENTED_EDGE('',*,*,#22154,.T.);
#31713=ORIENTED_EDGE('',*,*,#22158,.T.);
#31714=ORIENTED_EDGE('',*,*,#22169,.T.);
#31715=ORIENTED_EDGE('',*,*,#22171,.T.);
#31716=ORIENTED_EDGE('',*,*,#22163,.T.);
#31717=ORIENTED_EDGE('',*,*,#22167,.T.);
#31718=ORIENTED_EDGE('',*,*,#21840,.F.);
#31719=ORIENTED_EDGE('',*,*,#21628,.F.);
#31720=ORIENTED_EDGE('',*,*,#21841,.F.);
#31721=ORIENTED_EDGE('',*,*,#22175,.T.);
#31722=ORIENTED_EDGE('',*,*,#22172,.T.);
#31723=ORIENTED_EDGE('',*,*,#22175,.F.);
#32099=CONICAL_SURFACE('',#37331,5.47677669529664,1.17809724509618);
#32100=CONICAL_SURFACE('',#37335,5.95,0.785398163397454);
#32101=CONICAL_SURFACE('',#37348,10.7,0.876058050598193);
#32102=CONICAL_SURFACE('',#37354,10.7,0.785398163397449);
#32103=CONICAL_SURFACE('',#37582,6.76,0.797743215241672);
#33936=ADVANCED_FACE('',(#4962),#3076,.T.);
#33937=ADVANCED_FACE('',(#4963),#3077,.T.);
#33938=ADVANCED_FACE('',(#4964),#3078,.T.);
#33939=ADVANCED_FACE('',(#4965),#3079,.T.);
#33940=ADVANCED_FACE('',(#4966),#3080,.T.);
#33941=ADVANCED_FACE('',(#4967),#3081,.T.);
#33942=ADVANCED_FACE('',(#4968),#3082,.T.);
#33943=ADVANCED_FACE('',(#4969),#3083,.T.);
#33944=ADVANCED_FACE('',(#4970),#3084,.T.);
#33945=ADVANCED_FACE('',(#4971),#3085,.T.);
#33946=ADVANCED_FACE('',(#4972),#3086,.T.);
#33947=ADVANCED_FACE('',(#4973),#3087,.T.);
#33948=ADVANCED_FACE('',(#4974),#3088,.T.);
#33949=ADVANCED_FACE('',(#4975),#3089,.T.);
#33950=ADVANCED_FACE('',(#4976),#3090,.T.);
#33951=ADVANCED_FACE('',(#4977),#3091,.T.);
#33952=ADVANCED_FACE('',(#4978),#3092,.T.);
#33953=ADVANCED_FACE('',(#4979),#3093,.T.);
#33954=ADVANCED_FACE('',(#4980),#3094,.T.);
#33955=ADVANCED_FACE('',(#4981),#3095,.T.);
#33956=ADVANCED_FACE('',(#4982),#3096,.T.);
#33957=ADVANCED_FACE('',(#4983),#3097,.T.);
#33958=ADVANCED_FACE('',(#4984),#3098,.T.);
#33959=ADVANCED_FACE('',(#4985),#3099,.T.);
#33960=ADVANCED_FACE('',(#4986),#3100,.T.);
#33961=ADVANCED_FACE('',(#4987),#3101,.T.);
#33962=ADVANCED_FACE('',(#4988),#3102,.T.);
#33963=ADVANCED_FACE('',(#4989),#3103,.T.);
#33964=ADVANCED_FACE('',(#4990),#3104,.T.);
#33965=ADVANCED_FACE('',(#4991),#3105,.T.);
#33966=ADVANCED_FACE('',(#4992),#3106,.T.);
#33967=ADVANCED_FACE('',(#4993),#3107,.T.);
#33968=ADVANCED_FACE('',(#4994),#3108,.T.);
#33969=ADVANCED_FACE('',(#4995),#3109,.T.);
#33970=ADVANCED_FACE('',(#4996),#3110,.T.);
#33971=ADVANCED_FACE('',(#4997),#3111,.T.);
#33972=ADVANCED_FACE('',(#4998),#3112,.T.);
#33973=ADVANCED_FACE('',(#4999),#3113,.T.);
#33974=ADVANCED_FACE('',(#5000),#3114,.T.);
#33975=ADVANCED_FACE('',(#5001),#3115,.T.);
#33976=ADVANCED_FACE('',(#5002),#3116,.T.);
#33977=ADVANCED_FACE('',(#5003),#3117,.T.);
#33978=ADVANCED_FACE('',(#5004),#3118,.T.);
#33979=ADVANCED_FACE('',(#5005),#3119,.T.);
#33980=ADVANCED_FACE('',(#5006),#3120,.T.);
#33981=ADVANCED_FACE('',(#5007),#3121,.T.);
#33982=ADVANCED_FACE('',(#5008),#3122,.T.);
#33983=ADVANCED_FACE('',(#5009),#3123,.T.);
#33984=ADVANCED_FACE('',(#5010),#3124,.T.);
#33985=ADVANCED_FACE('',(#5011),#3125,.T.);
#33986=ADVANCED_FACE('',(#5012),#3126,.T.);
#33987=ADVANCED_FACE('',(#5013),#3127,.T.);
#33988=ADVANCED_FACE('',(#5014),#3128,.T.);
#33989=ADVANCED_FACE('',(#5015),#3129,.T.);
#33990=ADVANCED_FACE('',(#5016),#3130,.T.);
#33991=ADVANCED_FACE('',(#5017),#3131,.T.);
#33992=ADVANCED_FACE('',(#5018),#3132,.T.);
#33993=ADVANCED_FACE('',(#5019),#3133,.T.);
#33994=ADVANCED_FACE('',(#5020),#32099,.T.);
#33995=ADVANCED_FACE('',(#5021),#32100,.T.);
#33996=ADVANCED_FACE('',(#5022),#2805,.T.);
#33997=ADVANCED_FACE('',(#5023),#2806,.T.);
#33998=ADVANCED_FACE('',(#5024,#1296),#2807,.T.);
#33999=ADVANCED_FACE('',(#5025),#2808,.T.);
#34000=ADVANCED_FACE('',(#5026),#3134,.T.);
#34001=ADVANCED_FACE('',(#5027),#32101,.T.);
#34002=ADVANCED_FACE('',(#5028),#2809,.T.);
#34003=ADVANCED_FACE('',(#5029),#2810,.F.);
#34004=ADVANCED_FACE('',(#5030),#2811,.T.);
#34005=ADVANCED_FACE('',(#5031),#2812,.T.);
#34006=ADVANCED_FACE('',(#5032),#32102,.T.);
#34007=ADVANCED_FACE('',(#5033),#2813,.F.);
#34008=ADVANCED_FACE('',(#5034),#287,.F.);
#34009=ADVANCED_FACE('',(#5035),#2814,.T.);
#34010=ADVANCED_FACE('',(#5036),#3135,.T.);
#34011=ADVANCED_FACE('',(#5037),#288,.F.);
#34012=ADVANCED_FACE('',(#5038),#3136,.T.);
#34013=ADVANCED_FACE('',(#5039),#2815,.F.);
#34014=ADVANCED_FACE('',(#5040),#2816,.T.);
#34015=ADVANCED_FACE('',(#5041),#2817,.F.);
#34016=ADVANCED_FACE('',(#5042),#2818,.F.);
#34017=ADVANCED_FACE('',(#5043),#2819,.F.);
#34018=ADVANCED_FACE('',(#5044),#2820,.T.);
#34019=ADVANCED_FACE('',(#5045),#2821,.F.);
#34020=ADVANCED_FACE('',(#5046),#2822,.F.);
#34021=ADVANCED_FACE('',(#5047),#2823,.F.);
#34022=ADVANCED_FACE('',(#5048),#2824,.T.);
#34023=ADVANCED_FACE('',(#5049),#2825,.F.);
#34024=ADVANCED_FACE('',(#5050),#2826,.F.);
#34025=ADVANCED_FACE('',(#5051),#2827,.F.);
#34026=ADVANCED_FACE('',(#5052),#2828,.T.);
#34027=ADVANCED_FACE('',(#5053),#2829,.F.);
#34028=ADVANCED_FACE('',(#5054),#2830,.F.);
#34029=ADVANCED_FACE('',(#5055),#2831,.F.);
#34030=ADVANCED_FACE('',(#5056),#2832,.T.);
#34031=ADVANCED_FACE('',(#5057),#2833,.F.);
#34032=ADVANCED_FACE('',(#5058),#2834,.F.);
#34033=ADVANCED_FACE('',(#5059),#2835,.F.);
#34034=ADVANCED_FACE('',(#5060),#2836,.T.);
#34035=ADVANCED_FACE('',(#5061),#2837,.F.);
#34036=ADVANCED_FACE('',(#5062),#2838,.F.);
#34037=ADVANCED_FACE('',(#5063),#2839,.F.);
#34038=ADVANCED_FACE('',(#5064),#2840,.T.);
#34039=ADVANCED_FACE('',(#5065),#2841,.F.);
#34040=ADVANCED_FACE('',(#5066),#2842,.F.);
#34041=ADVANCED_FACE('',(#5067),#2843,.F.);
#34042=ADVANCED_FACE('',(#5068),#2844,.T.);
#34043=ADVANCED_FACE('',(#5069),#2845,.F.);
#34044=ADVANCED_FACE('',(#5070),#2846,.F.);
#34045=ADVANCED_FACE('',(#5071),#2847,.F.);
#34046=ADVANCED_FACE('',(#5072),#2848,.T.);
#34047=ADVANCED_FACE('',(#5073),#2849,.F.);
#34048=ADVANCED_FACE('',(#5074),#2850,.F.);
#34049=ADVANCED_FACE('',(#5075),#2851,.F.);
#34050=ADVANCED_FACE('',(#5076),#2852,.T.);
#34051=ADVANCED_FACE('',(#5077),#2853,.F.);
#34052=ADVANCED_FACE('',(#5078),#2854,.F.);
#34053=ADVANCED_FACE('',(#5079),#2855,.F.);
#34054=ADVANCED_FACE('',(#5080),#2856,.T.);
#34055=ADVANCED_FACE('',(#5081),#2857,.F.);
#34056=ADVANCED_FACE('',(#5082),#2858,.F.);
#34057=ADVANCED_FACE('',(#5083),#2859,.F.);
#34058=ADVANCED_FACE('',(#5084),#2860,.T.);
#34059=ADVANCED_FACE('',(#5085),#2861,.F.);
#34060=ADVANCED_FACE('',(#5086),#2862,.F.);
#34061=ADVANCED_FACE('',(#5087),#2863,.F.);
#34062=ADVANCED_FACE('',(#5088),#2864,.T.);
#34063=ADVANCED_FACE('',(#5089),#2865,.F.);
#34064=ADVANCED_FACE('',(#5090),#2866,.F.);
#34065=ADVANCED_FACE('',(#5091),#2867,.F.);
#34066=ADVANCED_FACE('',(#5092),#2868,.T.);
#34067=ADVANCED_FACE('',(#5093),#2869,.F.);
#34068=ADVANCED_FACE('',(#5094),#2870,.F.);
#34069=ADVANCED_FACE('',(#5095),#2871,.F.);
#34070=ADVANCED_FACE('',(#5096),#2872,.T.);
#34071=ADVANCED_FACE('',(#5097),#2873,.F.);
#34072=ADVANCED_FACE('',(#5098),#2874,.F.);
#34073=ADVANCED_FACE('',(#5099),#2875,.F.);
#34074=ADVANCED_FACE('',(#5100),#2876,.T.);
#34075=ADVANCED_FACE('',(#5101),#2877,.F.);
#34076=ADVANCED_FACE('',(#5102),#2878,.F.);
#34077=ADVANCED_FACE('',(#5103),#2879,.F.);
#34078=ADVANCED_FACE('',(#5104),#2880,.T.);
#34079=ADVANCED_FACE('',(#5105),#2881,.F.);
#34080=ADVANCED_FACE('',(#5106),#2882,.F.);
#34081=ADVANCED_FACE('',(#5107),#2883,.F.);
#34082=ADVANCED_FACE('',(#5108),#2884,.T.);
#34083=ADVANCED_FACE('',(#5109),#2885,.F.);
#34084=ADVANCED_FACE('',(#5110),#2886,.F.);
#34085=ADVANCED_FACE('',(#5111),#2887,.F.);
#34086=ADVANCED_FACE('',(#5112),#2888,.T.);
#34087=ADVANCED_FACE('',(#5113),#2889,.F.);
#34088=ADVANCED_FACE('',(#5114),#2890,.F.);
#34089=ADVANCED_FACE('',(#5115),#2891,.F.);
#34090=ADVANCED_FACE('',(#5116),#2892,.T.);
#34091=ADVANCED_FACE('',(#5117),#2893,.F.);
#34092=ADVANCED_FACE('',(#5118),#2894,.F.);
#34093=ADVANCED_FACE('',(#5119),#2895,.F.);
#34094=ADVANCED_FACE('',(#5120),#2896,.T.);
#34095=ADVANCED_FACE('',(#5121),#2897,.F.);
#34096=ADVANCED_FACE('',(#5122),#2898,.F.);
#34097=ADVANCED_FACE('',(#5123),#2899,.F.);
#34098=ADVANCED_FACE('',(#5124),#2900,.T.);
#34099=ADVANCED_FACE('',(#5125),#2901,.F.);
#34100=ADVANCED_FACE('',(#5126),#2902,.F.);
#34101=ADVANCED_FACE('',(#5127),#2903,.F.);
#34102=ADVANCED_FACE('',(#5128),#2904,.T.);
#34103=ADVANCED_FACE('',(#5129),#2905,.F.);
#34104=ADVANCED_FACE('',(#5130),#2906,.F.);
#34105=ADVANCED_FACE('',(#5131),#2907,.F.);
#34106=ADVANCED_FACE('',(#5132),#2908,.T.);
#34107=ADVANCED_FACE('',(#5133),#2909,.F.);
#34108=ADVANCED_FACE('',(#5134),#2910,.F.);
#34109=ADVANCED_FACE('',(#5135),#2911,.F.);
#34110=ADVANCED_FACE('',(#5136),#2912,.T.);
#34111=ADVANCED_FACE('',(#5137),#2913,.F.);
#34112=ADVANCED_FACE('',(#5138),#2914,.F.);
#34113=ADVANCED_FACE('',(#5139),#2915,.F.);
#34114=ADVANCED_FACE('',(#5140),#2916,.T.);
#34115=ADVANCED_FACE('',(#5141),#2917,.F.);
#34116=ADVANCED_FACE('',(#5142),#2918,.F.);
#34117=ADVANCED_FACE('',(#5143),#2919,.F.);
#34118=ADVANCED_FACE('',(#5144),#2920,.T.);
#34119=ADVANCED_FACE('',(#5145),#2921,.F.);
#34120=ADVANCED_FACE('',(#5146),#2922,.F.);
#34121=ADVANCED_FACE('',(#5147),#2923,.F.);
#34122=ADVANCED_FACE('',(#5148),#2924,.T.);
#34123=ADVANCED_FACE('',(#5149),#2925,.F.);
#34124=ADVANCED_FACE('',(#5150),#2926,.F.);
#34125=ADVANCED_FACE('',(#5151),#2927,.F.);
#34126=ADVANCED_FACE('',(#5152),#2928,.T.);
#34127=ADVANCED_FACE('',(#5153),#2929,.F.);
#34128=ADVANCED_FACE('',(#5154),#2930,.F.);
#34129=ADVANCED_FACE('',(#5155),#2931,.F.);
#34130=ADVANCED_FACE('',(#5156),#2932,.T.);
#34131=ADVANCED_FACE('',(#5157),#2933,.F.);
#34132=ADVANCED_FACE('',(#5158),#2934,.F.);
#34133=ADVANCED_FACE('',(#5159),#2935,.F.);
#34134=ADVANCED_FACE('',(#5160),#2936,.T.);
#34135=ADVANCED_FACE('',(#5161),#2937,.F.);
#34136=ADVANCED_FACE('',(#5162),#2938,.F.);
#34137=ADVANCED_FACE('',(#5163),#2939,.F.);
#34138=ADVANCED_FACE('',(#5164),#2940,.T.);
#34139=ADVANCED_FACE('',(#5165),#2941,.F.);
#34140=ADVANCED_FACE('',(#5166),#2942,.F.);
#34141=ADVANCED_FACE('',(#5167),#2943,.F.);
#34142=ADVANCED_FACE('',(#5168),#2944,.T.);
#34143=ADVANCED_FACE('',(#5169),#2945,.F.);
#34144=ADVANCED_FACE('',(#5170),#2946,.F.);
#34145=ADVANCED_FACE('',(#5171),#2947,.F.);
#34146=ADVANCED_FACE('',(#5172),#2948,.T.);
#34147=ADVANCED_FACE('',(#5173),#2949,.F.);
#34148=ADVANCED_FACE('',(#5174),#2950,.F.);
#34149=ADVANCED_FACE('',(#5175),#2951,.F.);
#34150=ADVANCED_FACE('',(#5176),#2952,.T.);
#34151=ADVANCED_FACE('',(#5177),#2953,.F.);
#34152=ADVANCED_FACE('',(#5178),#2954,.F.);
#34153=ADVANCED_FACE('',(#5179),#2955,.F.);
#34154=ADVANCED_FACE('',(#5180),#2956,.T.);
#34155=ADVANCED_FACE('',(#5181),#2957,.F.);
#34156=ADVANCED_FACE('',(#5182),#2958,.F.);
#34157=ADVANCED_FACE('',(#5183,#1297,#1298,#1299,#1300,#1301,#1302,#1303,
#1304,#1305,#1306,#1307,#1308,#1309,#1310,#1311,#1312,#1313,#1314,#1315,
#1316,#1317,#1318,#1319,#1320,#1321,#1322,#1323,#1324,#1325,#1326,#1327,
#1328,#1329,#1330,#1331),#3137,.T.);
#34158=ADVANCED_FACE('',(#5184),#32103,.T.);
#34219=CLOSED_SHELL('',(#33936,#33937,#33938,#33939,#33940,#33941,#33942,
#33943,#33944,#33945,#33946,#33947,#33948,#33949,#33950,#33951,#33952,#33953,
#33954,#33955,#33956,#33957,#33958,#33959,#33960,#33961,#33962,#33963,#33964,
#33965,#33966,#33967,#33968,#33969,#33970,#33971,#33972,#33973,#33974,#33975,
#33976,#33977,#33978,#33979,#33980,#33981,#33982,#33983,#33984,#33985,#33986,
#33987,#33988,#33989,#33990,#33991,#33992,#33993,#33994,#33995,#33996,#33997,
#33998,#33999,#34000,#34001,#34002,#34003,#34004,#34005,#34006,#34007,#34008,
#34009,#34010,#34011,#34012,#34013,#34014,#34015,#34016,#34017,#34018,#34019,
#34020,#34021,#34022,#34023,#34024,#34025,#34026,#34027,#34028,#34029,#34030,
#34031,#34032,#34033,#34034,#34035,#34036,#34037,#34038,#34039,#34040,#34041,
#34042,#34043,#34044,#34045,#34046,#34047,#34048,#34049,#34050,#34051,#34052,
#34053,#34054,#34055,#34056,#34057,#34058,#34059,#34060,#34061,#34062,#34063,
#34064,#34065,#34066,#34067,#34068,#34069,#34070,#34071,#34072,#34073,#34074,
#34075,#34076,#34077,#34078,#34079,#34080,#34081,#34082,#34083,#34084,#34085,
#34086,#34087,#34088,#34089,#34090,#34091,#34092,#34093,#34094,#34095,#34096,
#34097,#34098,#34099,#34100,#34101,#34102,#34103,#34104,#34105,#34106,#34107,
#34108,#34109,#34110,#34111,#34112,#34113,#34114,#34115,#34116,#34117,#34118,
#34119,#34120,#34121,#34122,#34123,#34124,#34125,#34126,#34127,#34128,#34129,
#34130,#34131,#34132,#34133,#34134,#34135,#34136,#34137,#34138,#34139,#34140,
#34141,#34142,#34143,#34144,#34145,#34146,#34147,#34148,#34149,#34150,#34151,
#34152,#34153,#34154,#34155,#34156,#34157,#34158));
#37269=AXIS2_PLACEMENT_3D('',#63093,#46140,#46141);
#37270=AXIS2_PLACEMENT_3D('',#63094,#46142,#46143);
#37271=AXIS2_PLACEMENT_3D('',#63116,#46145,#46146);
#37272=AXIS2_PLACEMENT_3D('',#63127,#46147,#46148);
#37273=AXIS2_PLACEMENT_3D('',#63211,#46150,#46151);
#37274=AXIS2_PLACEMENT_3D('',#63301,#46153,#46154);
#37275=AXIS2_PLACEMENT_3D('',#63391,#46156,#46157);
#37276=AXIS2_PLACEMENT_3D('',#63475,#46159,#46160);
#37277=AXIS2_PLACEMENT_3D('',#63565,#46162,#46163);
#37278=AXIS2_PLACEMENT_3D('',#63649,#46165,#46166);
#37279=AXIS2_PLACEMENT_3D('',#63736,#46168,#46169);
#37280=AXIS2_PLACEMENT_3D('',#63826,#46171,#46172);
#37281=AXIS2_PLACEMENT_3D('',#63910,#46174,#46175);
#37282=AXIS2_PLACEMENT_3D('',#64000,#46177,#46178);
#37283=AXIS2_PLACEMENT_3D('',#64090,#46180,#46181);
#37284=AXIS2_PLACEMENT_3D('',#64174,#46183,#46184);
#37285=AXIS2_PLACEMENT_3D('',#64264,#46186,#46187);
#37286=AXIS2_PLACEMENT_3D('',#64351,#46189,#46190);
#37287=AXIS2_PLACEMENT_3D('',#64438,#46192,#46193);
#37288=AXIS2_PLACEMENT_3D('',#64528,#46195,#46196);
#37289=AXIS2_PLACEMENT_3D('',#64612,#46198,#46199);
#37290=AXIS2_PLACEMENT_3D('',#64702,#46201,#46202);
#37291=AXIS2_PLACEMENT_3D('',#64792,#46204,#46205);
#37292=AXIS2_PLACEMENT_3D('',#64876,#46207,#46208);
#37293=AXIS2_PLACEMENT_3D('',#64966,#46210,#46211);
#37294=AXIS2_PLACEMENT_3D('',#65053,#46213,#46214);
#37295=AXIS2_PLACEMENT_3D('',#65140,#46216,#46217);
#37296=AXIS2_PLACEMENT_3D('',#65230,#46219,#46220);
#37297=AXIS2_PLACEMENT_3D('',#65314,#46222,#46223);
#37298=AXIS2_PLACEMENT_3D('',#65404,#46225,#46226);
#37299=AXIS2_PLACEMENT_3D('',#65494,#46228,#46229);
#37300=AXIS2_PLACEMENT_3D('',#65578,#46231,#46232);
#37301=AXIS2_PLACEMENT_3D('',#65587,#46234,#46235);
#37302=AXIS2_PLACEMENT_3D('',#65588,#46236,#46237);
#37303=AXIS2_PLACEMENT_3D('',#65609,#46239,#46240);
#37304=AXIS2_PLACEMENT_3D('',#65624,#46241,#46242);
#37305=AXIS2_PLACEMENT_3D('',#65661,#46244,#46245);
#37306=AXIS2_PLACEMENT_3D('',#65699,#46247,#46248);
#37307=AXIS2_PLACEMENT_3D('',#65736,#46250,#46251);
#37308=AXIS2_PLACEMENT_3D('',#65773,#46253,#46254);
#37309=AXIS2_PLACEMENT_3D('',#65811,#46256,#46257);
#37310=AXIS2_PLACEMENT_3D('',#65847,#46259,#46260);
#37311=AXIS2_PLACEMENT_3D('',#65885,#46262,#46263);
#37312=AXIS2_PLACEMENT_3D('',#65922,#46265,#46266);
#37313=AXIS2_PLACEMENT_3D('',#65959,#46268,#46269);
#37314=AXIS2_PLACEMENT_3D('',#65997,#46271,#46272);
#37315=AXIS2_PLACEMENT_3D('',#66034,#46274,#46275);
#37316=AXIS2_PLACEMENT_3D('',#66071,#46277,#46278);
#37317=AXIS2_PLACEMENT_3D('',#66109,#46280,#46281);
#37318=AXIS2_PLACEMENT_3D('',#66145,#46283,#46284);
#37319=AXIS2_PLACEMENT_3D('',#66183,#46286,#46287);
#37320=AXIS2_PLACEMENT_3D('',#66220,#46289,#46290);
#37321=AXIS2_PLACEMENT_3D('',#66257,#46292,#46293);
#37322=AXIS2_PLACEMENT_3D('',#66295,#46295,#46296);
#37323=AXIS2_PLACEMENT_3D('',#66332,#46298,#46299);
#37324=AXIS2_PLACEMENT_3D('',#66369,#46301,#46302);
#37325=AXIS2_PLACEMENT_3D('',#66407,#46304,#46305);
#37326=AXIS2_PLACEMENT_3D('',#66444,#46307,#46308);
#37327=AXIS2_PLACEMENT_3D('',#66481,#46310,#46311);
#37328=AXIS2_PLACEMENT_3D('',#66518,#46313,#46314);
#37329=AXIS2_PLACEMENT_3D('',#66555,#46316,#46317);
#37330=AXIS2_PLACEMENT_3D('',#66593,#46319,#46320);
#37331=AXIS2_PLACEMENT_3D('',#66630,#46322,#46323);
#37332=AXIS2_PLACEMENT_3D('',#66632,#46324,#46325);
#37333=AXIS2_PLACEMENT_3D('',#66636,#46327,#46328);
#37334=AXIS2_PLACEMENT_3D('',#66637,#46329,#46330);
#37335=AXIS2_PLACEMENT_3D('',#66638,#46331,#46332);
#37336=AXIS2_PLACEMENT_3D('',#66642,#46334,#46335);
#37337=AXIS2_PLACEMENT_3D('',#66644,#46336,#46337);
#37338=AXIS2_PLACEMENT_3D('',#66645,#46338,#46339);
#37339=AXIS2_PLACEMENT_3D('',#66646,#46340,#46341);
#37340=AXIS2_PLACEMENT_3D('',#66647,#46342,#46343);
#37341=AXIS2_PLACEMENT_3D('',#66664,#46348,#46349);
#37342=AXIS2_PLACEMENT_3D('',#66665,#46350,#46351);
#37343=AXIS2_PLACEMENT_3D('',#66667,#46352,#46353);
#37344=AXIS2_PLACEMENT_3D('',#66668,#46354,#46355);
#37345=AXIS2_PLACEMENT_3D('',#66682,#46359,#46360);
#37346=AXIS2_PLACEMENT_3D('',#66684,#46361,#46362);
#37347=AXIS2_PLACEMENT_3D('',#66687,#46364,#46365);
#37348=AXIS2_PLACEMENT_3D('',#66688,#46366,#46367);
#37349=AXIS2_PLACEMENT_3D('',#66694,#46368,#46369);
#37350=AXIS2_PLACEMENT_3D('',#66702,#46370,#46371);
#37351=AXIS2_PLACEMENT_3D('',#66707,#46375,#46376);
#37352=AXIS2_PLACEMENT_3D('',#66709,#46378,#46379);
#37353=AXIS2_PLACEMENT_3D('',#66710,#46380,#46381);
#37354=AXIS2_PLACEMENT_3D('',#66714,#46382,#46383);
#37355=AXIS2_PLACEMENT_3D('',#66715,#46384,#46385);
#37356=AXIS2_PLACEMENT_3D('',#68559,#46386,#46387);
#37357=AXIS2_PLACEMENT_3D('',#68561,#46388,#46389);
#37358=AXIS2_PLACEMENT_3D('',#68562,#46390,#46391);
#37359=AXIS2_PLACEMENT_3D('',#68676,#46392,#46393);
#37360=AXIS2_PLACEMENT_3D('',#68677,#46394,#46395);
#37361=AXIS2_PLACEMENT_3D('',#70182,#46396,#46397);
#37362=AXIS2_PLACEMENT_3D('',#70183,#46398,#46399);
#37363=AXIS2_PLACEMENT_3D('',#70192,#46404,#46405);
#37364=AXIS2_PLACEMENT_3D('',#70194,#46406,#46407);
#37365=AXIS2_PLACEMENT_3D('',#70196,#46409,#46410);
#37366=AXIS2_PLACEMENT_3D('',#70200,#46413,#46414);
#37367=AXIS2_PLACEMENT_3D('',#70201,#46415,#46416);
#37368=AXIS2_PLACEMENT_3D('',#70202,#46417,#46418);
#37369=AXIS2_PLACEMENT_3D('',#70211,#46423,#46424);
#37370=AXIS2_PLACEMENT_3D('',#70213,#46425,#46426);
#37371=AXIS2_PLACEMENT_3D('',#70215,#46428,#46429);
#37372=AXIS2_PLACEMENT_3D('',#70219,#46432,#46433);
#37373=AXIS2_PLACEMENT_3D('',#70220,#46434,#46435);
#37374=AXIS2_PLACEMENT_3D('',#70221,#46436,#46437);
#37375=AXIS2_PLACEMENT_3D('',#70230,#46442,#46443);
#37376=AXIS2_PLACEMENT_3D('',#70232,#46444,#46445);
#37377=AXIS2_PLACEMENT_3D('',#70234,#46447,#46448);
#37378=AXIS2_PLACEMENT_3D('',#70238,#46451,#46452);
#37379=AXIS2_PLACEMENT_3D('',#70239,#46453,#46454);
#37380=AXIS2_PLACEMENT_3D('',#70240,#46455,#46456);
#37381=AXIS2_PLACEMENT_3D('',#70249,#46461,#46462);
#37382=AXIS2_PLACEMENT_3D('',#70251,#46463,#46464);
#37383=AXIS2_PLACEMENT_3D('',#70253,#46466,#46467);
#37384=AXIS2_PLACEMENT_3D('',#70257,#46470,#46471);
#37385=AXIS2_PLACEMENT_3D('',#70258,#46472,#46473);
#37386=AXIS2_PLACEMENT_3D('',#70259,#46474,#46475);
#37387=AXIS2_PLACEMENT_3D('',#70268,#46480,#46481);
#37388=AXIS2_PLACEMENT_3D('',#70270,#46482,#46483);
#37389=AXIS2_PLACEMENT_3D('',#70272,#46485,#46486);
#37390=AXIS2_PLACEMENT_3D('',#70276,#46489,#46490);
#37391=AXIS2_PLACEMENT_3D('',#70277,#46491,#46492);
#37392=AXIS2_PLACEMENT_3D('',#70278,#46493,#46494);
#37393=AXIS2_PLACEMENT_3D('',#70287,#46499,#46500);
#37394=AXIS2_PLACEMENT_3D('',#70289,#46501,#46502);
#37395=AXIS2_PLACEMENT_3D('',#70291,#46504,#46505);
#37396=AXIS2_PLACEMENT_3D('',#70295,#46508,#46509);
#37397=AXIS2_PLACEMENT_3D('',#70296,#46510,#46511);
#37398=AXIS2_PLACEMENT_3D('',#70297,#46512,#46513);
#37399=AXIS2_PLACEMENT_3D('',#70306,#46518,#46519);
#37400=AXIS2_PLACEMENT_3D('',#70308,#46520,#46521);
#37401=AXIS2_PLACEMENT_3D('',#70310,#46523,#46524);
#37402=AXIS2_PLACEMENT_3D('',#70314,#46527,#46528);
#37403=AXIS2_PLACEMENT_3D('',#70315,#46529,#46530);
#37404=AXIS2_PLACEMENT_3D('',#70316,#46531,#46532);
#37405=AXIS2_PLACEMENT_3D('',#70325,#46537,#46538);
#37406=AXIS2_PLACEMENT_3D('',#70327,#46539,#46540);
#37407=AXIS2_PLACEMENT_3D('',#70329,#46542,#46543);
#37408=AXIS2_PLACEMENT_3D('',#70333,#46546,#46547);
#37409=AXIS2_PLACEMENT_3D('',#70334,#46548,#46549);
#37410=AXIS2_PLACEMENT_3D('',#70335,#46550,#46551);
#37411=AXIS2_PLACEMENT_3D('',#70344,#46556,#46557);
#37412=AXIS2_PLACEMENT_3D('',#70346,#46558,#46559);
#37413=AXIS2_PLACEMENT_3D('',#70348,#46561,#46562);
#37414=AXIS2_PLACEMENT_3D('',#70352,#46565,#46566);
#37415=AXIS2_PLACEMENT_3D('',#70353,#46567,#46568);
#37416=AXIS2_PLACEMENT_3D('',#70354,#46569,#46570);
#37417=AXIS2_PLACEMENT_3D('',#70363,#46575,#46576);
#37418=AXIS2_PLACEMENT_3D('',#70365,#46577,#46578);
#37419=AXIS2_PLACEMENT_3D('',#70367,#46580,#46581);
#37420=AXIS2_PLACEMENT_3D('',#70371,#46584,#46585);
#37421=AXIS2_PLACEMENT_3D('',#70372,#46586,#46587);
#37422=AXIS2_PLACEMENT_3D('',#70373,#46588,#46589);
#37423=AXIS2_PLACEMENT_3D('',#70382,#46594,#46595);
#37424=AXIS2_PLACEMENT_3D('',#70384,#46596,#46597);
#37425=AXIS2_PLACEMENT_3D('',#70386,#46599,#46600);
#37426=AXIS2_PLACEMENT_3D('',#70390,#46603,#46604);
#37427=AXIS2_PLACEMENT_3D('',#70391,#46605,#46606);
#37428=AXIS2_PLACEMENT_3D('',#70392,#46607,#46608);
#37429=AXIS2_PLACEMENT_3D('',#70401,#46613,#46614);
#37430=AXIS2_PLACEMENT_3D('',#70403,#46615,#46616);
#37431=AXIS2_PLACEMENT_3D('',#70405,#46618,#46619);
#37432=AXIS2_PLACEMENT_3D('',#70409,#46622,#46623);
#37433=AXIS2_PLACEMENT_3D('',#70410,#46624,#46625);
#37434=AXIS2_PLACEMENT_3D('',#70411,#46626,#46627);
#37435=AXIS2_PLACEMENT_3D('',#70420,#46632,#46633);
#37436=AXIS2_PLACEMENT_3D('',#70422,#46634,#46635);
#37437=AXIS2_PLACEMENT_3D('',#70424,#46637,#46638);
#37438=AXIS2_PLACEMENT_3D('',#70428,#46641,#46642);
#37439=AXIS2_PLACEMENT_3D('',#70429,#46643,#46644);
#37440=AXIS2_PLACEMENT_3D('',#70430,#46645,#46646);
#37441=AXIS2_PLACEMENT_3D('',#70439,#46651,#46652);
#37442=AXIS2_PLACEMENT_3D('',#70441,#46653,#46654);
#37443=AXIS2_PLACEMENT_3D('',#70443,#46656,#46657);
#37444=AXIS2_PLACEMENT_3D('',#70447,#46660,#46661);
#37445=AXIS2_PLACEMENT_3D('',#70448,#46662,#46663);
#37446=AXIS2_PLACEMENT_3D('',#70449,#46664,#46665);
#37447=AXIS2_PLACEMENT_3D('',#70458,#46670,#46671);
#37448=AXIS2_PLACEMENT_3D('',#70460,#46672,#46673);
#37449=AXIS2_PLACEMENT_3D('',#70462,#46675,#46676);
#37450=AXIS2_PLACEMENT_3D('',#70466,#46679,#46680);
#37451=AXIS2_PLACEMENT_3D('',#70467,#46681,#46682);
#37452=AXIS2_PLACEMENT_3D('',#70468,#46683,#46684);
#37453=AXIS2_PLACEMENT_3D('',#70477,#46689,#46690);
#37454=AXIS2_PLACEMENT_3D('',#70479,#46691,#46692);
#37455=AXIS2_PLACEMENT_3D('',#70481,#46694,#46695);
#37456=AXIS2_PLACEMENT_3D('',#70485,#46698,#46699);
#37457=AXIS2_PLACEMENT_3D('',#70486,#46700,#46701);
#37458=AXIS2_PLACEMENT_3D('',#70487,#46702,#46703);
#37459=AXIS2_PLACEMENT_3D('',#70496,#46708,#46709);
#37460=AXIS2_PLACEMENT_3D('',#70498,#46710,#46711);
#37461=AXIS2_PLACEMENT_3D('',#70500,#46713,#46714);
#37462=AXIS2_PLACEMENT_3D('',#70504,#46717,#46718);
#37463=AXIS2_PLACEMENT_3D('',#70505,#46719,#46720);
#37464=AXIS2_PLACEMENT_3D('',#70506,#46721,#46722);
#37465=AXIS2_PLACEMENT_3D('',#70515,#46727,#46728);
#37466=AXIS2_PLACEMENT_3D('',#70517,#46729,#46730);
#37467=AXIS2_PLACEMENT_3D('',#70520,#46732,#46733);
#37468=AXIS2_PLACEMENT_3D('',#70521,#46734,#46735);
#37469=AXIS2_PLACEMENT_3D('',#70525,#46738,#46739);
#37470=AXIS2_PLACEMENT_3D('',#70527,#46740,#46741);
#37471=AXIS2_PLACEMENT_3D('',#70528,#46742,#46743);
#37472=AXIS2_PLACEMENT_3D('',#70529,#46744,#46745);
#37473=AXIS2_PLACEMENT_3D('',#70538,#46750,#46751);
#37474=AXIS2_PLACEMENT_3D('',#70540,#46752,#46753);
#37475=AXIS2_PLACEMENT_3D('',#70542,#46755,#46756);
#37476=AXIS2_PLACEMENT_3D('',#70546,#46759,#46760);
#37477=AXIS2_PLACEMENT_3D('',#70547,#46761,#46762);
#37478=AXIS2_PLACEMENT_3D('',#70548,#46763,#46764);
#37479=AXIS2_PLACEMENT_3D('',#70557,#46769,#46770);
#37480=AXIS2_PLACEMENT_3D('',#70559,#46771,#46772);
#37481=AXIS2_PLACEMENT_3D('',#70561,#46774,#46775);
#37482=AXIS2_PLACEMENT_3D('',#70565,#46778,#46779);
#37483=AXIS2_PLACEMENT_3D('',#70566,#46780,#46781);
#37484=AXIS2_PLACEMENT_3D('',#70567,#46782,#46783);
#37485=AXIS2_PLACEMENT_3D('',#70576,#46788,#46789);
#37486=AXIS2_PLACEMENT_3D('',#70578,#46790,#46791);
#37487=AXIS2_PLACEMENT_3D('',#70580,#46793,#46794);
#37488=AXIS2_PLACEMENT_3D('',#70584,#46797,#46798);
#37489=AXIS2_PLACEMENT_3D('',#70585,#46799,#46800);
#37490=AXIS2_PLACEMENT_3D('',#70586,#46801,#46802);
#37491=AXIS2_PLACEMENT_3D('',#70595,#46807,#46808);
#37492=AXIS2_PLACEMENT_3D('',#70597,#46809,#46810);
#37493=AXIS2_PLACEMENT_3D('',#70599,#46812,#46813);
#37494=AXIS2_PLACEMENT_3D('',#70603,#46816,#46817);
#37495=AXIS2_PLACEMENT_3D('',#70604,#46818,#46819);
#37496=AXIS2_PLACEMENT_3D('',#70605,#46820,#46821);
#37497=AXIS2_PLACEMENT_3D('',#70614,#46826,#46827);
#37498=AXIS2_PLACEMENT_3D('',#70616,#46828,#46829);
#37499=AXIS2_PLACEMENT_3D('',#70618,#46831,#46832);
#37500=AXIS2_PLACEMENT_3D('',#70622,#46835,#46836);
#37501=AXIS2_PLACEMENT_3D('',#70623,#46837,#46838);
#37502=AXIS2_PLACEMENT_3D('',#70624,#46839,#46840);
#37503=AXIS2_PLACEMENT_3D('',#70633,#46845,#46846);
#37504=AXIS2_PLACEMENT_3D('',#70635,#46847,#46848);
#37505=AXIS2_PLACEMENT_3D('',#70637,#46850,#46851);
#37506=AXIS2_PLACEMENT_3D('',#70641,#46854,#46855);
#37507=AXIS2_PLACEMENT_3D('',#70642,#46856,#46857);
#37508=AXIS2_PLACEMENT_3D('',#70643,#46858,#46859);
#37509=AXIS2_PLACEMENT_3D('',#70652,#46864,#46865);
#37510=AXIS2_PLACEMENT_3D('',#70654,#46866,#46867);
#37511=AXIS2_PLACEMENT_3D('',#70656,#46869,#46870);
#37512=AXIS2_PLACEMENT_3D('',#70660,#46873,#46874);
#37513=AXIS2_PLACEMENT_3D('',#70661,#46875,#46876);
#37514=AXIS2_PLACEMENT_3D('',#70662,#46877,#46878);
#37515=AXIS2_PLACEMENT_3D('',#70671,#46883,#46884);
#37516=AXIS2_PLACEMENT_3D('',#70673,#46885,#46886);
#37517=AXIS2_PLACEMENT_3D('',#70675,#46888,#46889);
#37518=AXIS2_PLACEMENT_3D('',#70679,#46892,#46893);
#37519=AXIS2_PLACEMENT_3D('',#70680,#46894,#46895);
#37520=AXIS2_PLACEMENT_3D('',#70681,#46896,#46897);
#37521=AXIS2_PLACEMENT_3D('',#70690,#46902,#46903);
#37522=AXIS2_PLACEMENT_3D('',#70692,#46904,#46905);
#37523=AXIS2_PLACEMENT_3D('',#70694,#46907,#46908);
#37524=AXIS2_PLACEMENT_3D('',#70698,#46911,#46912);
#37525=AXIS2_PLACEMENT_3D('',#70699,#46913,#46914);
#37526=AXIS2_PLACEMENT_3D('',#70700,#46915,#46916);
#37527=AXIS2_PLACEMENT_3D('',#70709,#46921,#46922);
#37528=AXIS2_PLACEMENT_3D('',#70711,#46923,#46924);
#37529=AXIS2_PLACEMENT_3D('',#70713,#46926,#46927);
#37530=AXIS2_PLACEMENT_3D('',#70717,#46930,#46931);
#37531=AXIS2_PLACEMENT_3D('',#70718,#46932,#46933);
#37532=AXIS2_PLACEMENT_3D('',#70719,#46934,#46935);
#37533=AXIS2_PLACEMENT_3D('',#70728,#46940,#46941);
#37534=AXIS2_PLACEMENT_3D('',#70730,#46942,#46943);
#37535=AXIS2_PLACEMENT_3D('',#70732,#46945,#46946);
#37536=AXIS2_PLACEMENT_3D('',#70736,#46949,#46950);
#37537=AXIS2_PLACEMENT_3D('',#70737,#46951,#46952);
#37538=AXIS2_PLACEMENT_3D('',#70738,#46953,#46954);
#37539=AXIS2_PLACEMENT_3D('',#70747,#46959,#46960);
#37540=AXIS2_PLACEMENT_3D('',#70749,#46961,#46962);
#37541=AXIS2_PLACEMENT_3D('',#70751,#46964,#46965);
#37542=AXIS2_PLACEMENT_3D('',#70755,#46968,#46969);
#37543=AXIS2_PLACEMENT_3D('',#70756,#46970,#46971);
#37544=AXIS2_PLACEMENT_3D('',#70757,#46972,#46973);
#37545=AXIS2_PLACEMENT_3D('',#70766,#46978,#46979);
#37546=AXIS2_PLACEMENT_3D('',#70768,#46980,#46981);
#37547=AXIS2_PLACEMENT_3D('',#70770,#46983,#46984);
#37548=AXIS2_PLACEMENT_3D('',#70774,#46987,#46988);
#37549=AXIS2_PLACEMENT_3D('',#70775,#46989,#46990);
#37550=AXIS2_PLACEMENT_3D('',#70776,#46991,#46992);
#37551=AXIS2_PLACEMENT_3D('',#70785,#46997,#46998);
#37552=AXIS2_PLACEMENT_3D('',#70787,#46999,#47000);
#37553=AXIS2_PLACEMENT_3D('',#70789,#47002,#47003);
#37554=AXIS2_PLACEMENT_3D('',#70793,#47006,#47007);
#37555=AXIS2_PLACEMENT_3D('',#70794,#47008,#47009);
#37556=AXIS2_PLACEMENT_3D('',#70795,#47010,#47011);
#37557=AXIS2_PLACEMENT_3D('',#70804,#47016,#47017);
#37558=AXIS2_PLACEMENT_3D('',#70806,#47018,#47019);
#37559=AXIS2_PLACEMENT_3D('',#70808,#47021,#47022);
#37560=AXIS2_PLACEMENT_3D('',#70812,#47025,#47026);
#37561=AXIS2_PLACEMENT_3D('',#70813,#47027,#47028);
#37562=AXIS2_PLACEMENT_3D('',#70814,#47029,#47030);
#37563=AXIS2_PLACEMENT_3D('',#70823,#47035,#47036);
#37564=AXIS2_PLACEMENT_3D('',#70825,#47037,#47038);
#37565=AXIS2_PLACEMENT_3D('',#70827,#47040,#47041);
#37566=AXIS2_PLACEMENT_3D('',#70831,#47044,#47045);
#37567=AXIS2_PLACEMENT_3D('',#70832,#47046,#47047);
#37568=AXIS2_PLACEMENT_3D('',#70833,#47048,#47049);
#37569=AXIS2_PLACEMENT_3D('',#70842,#47054,#47055);
#37570=AXIS2_PLACEMENT_3D('',#70844,#47056,#47057);
#37571=AXIS2_PLACEMENT_3D('',#70846,#47059,#47060);
#37572=AXIS2_PLACEMENT_3D('',#70850,#47063,#47064);
#37573=AXIS2_PLACEMENT_3D('',#70851,#47065,#47066);
#37574=AXIS2_PLACEMENT_3D('',#70852,#47067,#47068);
#37575=AXIS2_PLACEMENT_3D('',#70861,#47073,#47074);
#37576=AXIS2_PLACEMENT_3D('',#70863,#47075,#47076);
#37577=AXIS2_PLACEMENT_3D('',#70865,#47078,#47079);
#37578=AXIS2_PLACEMENT_3D('',#70869,#47082,#47083);
#37579=AXIS2_PLACEMENT_3D('',#70870,#47084,#47085);
#37580=AXIS2_PLACEMENT_3D('',#70871,#47086,#47087);
#37581=AXIS2_PLACEMENT_3D('',#70873,#47088,#47089);
#37582=AXIS2_PLACEMENT_3D('',#70876,#47092,#47093);
#46140=DIRECTION('axis',(0.,0.,1.));
#46141=DIRECTION('refdir',(1.,0.,0.));
#46142=DIRECTION('center_axis',(1.,0.,0.));
#46143=DIRECTION('ref_axis',(0.,1.,0.));
#46144=DIRECTION('',(-1.,0.,0.));
#46145=DIRECTION('center_axis',(-1.,0.,0.));
#46146=DIRECTION('ref_axis',(0.,1.,0.));
#46147=DIRECTION('center_axis',(1.,0.,0.));
#46148=DIRECTION('ref_axis',(0.,1.,0.));
#46149=DIRECTION('',(-1.,0.,0.));
#46150=DIRECTION('center_axis',(1.,0.,0.));
#46151=DIRECTION('ref_axis',(0.,1.,0.));
#46152=DIRECTION('',(-1.,0.,0.));
#46153=DIRECTION('center_axis',(1.,0.,0.));
#46154=DIRECTION('ref_axis',(0.,1.,0.));
#46155=DIRECTION('',(-1.,0.,0.));
#46156=DIRECTION('center_axis',(1.,0.,0.));
#46157=DIRECTION('ref_axis',(0.,1.,0.));
#46158=DIRECTION('',(-1.,0.,0.));
#46159=DIRECTION('center_axis',(1.,0.,0.));
#46160=DIRECTION('ref_axis',(0.,1.,0.));
#46161=DIRECTION('',(-1.,0.,0.));
#46162=DIRECTION('center_axis',(1.,0.,0.));
#46163=DIRECTION('ref_axis',(0.,1.,0.));
#46164=DIRECTION('',(-1.,0.,0.));
#46165=DIRECTION('center_axis',(1.,0.,0.));
#46166=DIRECTION('ref_axis',(0.,1.,0.));
#46167=DIRECTION('',(-1.,0.,0.));
#46168=DIRECTION('center_axis',(1.,0.,0.));
#46169=DIRECTION('ref_axis',(0.,1.,0.));
#46170=DIRECTION('',(-1.,0.,0.));
#46171=DIRECTION('center_axis',(1.,0.,0.));
#46172=DIRECTION('ref_axis',(0.,1.,0.));
#46173=DIRECTION('',(-1.,0.,0.));
#46174=DIRECTION('center_axis',(1.,0.,0.));
#46175=DIRECTION('ref_axis',(0.,1.,0.));
#46176=DIRECTION('',(-1.,0.,0.));
#46177=DIRECTION('center_axis',(1.,0.,0.));
#46178=DIRECTION('ref_axis',(0.,1.,0.));
#46179=DIRECTION('',(-1.,0.,0.));
#46180=DIRECTION('center_axis',(1.,0.,0.));
#46181=DIRECTION('ref_axis',(0.,1.,0.));
#46182=DIRECTION('',(-1.,0.,0.));
#46183=DIRECTION('center_axis',(1.,0.,0.));
#46184=DIRECTION('ref_axis',(0.,1.,0.));
#46185=DIRECTION('',(-1.,0.,0.));
#46186=DIRECTION('center_axis',(1.,0.,0.));
#46187=DIRECTION('ref_axis',(0.,1.,0.));
#46188=DIRECTION('',(-1.,0.,0.));
#46189=DIRECTION('center_axis',(1.,0.,0.));
#46190=DIRECTION('ref_axis',(0.,1.,0.));
#46191=DIRECTION('',(-1.,0.,0.));
#46192=DIRECTION('center_axis',(1.,0.,0.));
#46193=DIRECTION('ref_axis',(0.,1.,0.));
#46194=DIRECTION('',(-1.,0.,0.));
#46195=DIRECTION('center_axis',(1.,0.,0.));
#46196=DIRECTION('ref_axis',(0.,1.,0.));
#46197=DIRECTION('',(-1.,0.,0.));
#46198=DIRECTION('center_axis',(1.,0.,0.));
#46199=DIRECTION('ref_axis',(0.,1.,0.));
#46200=DIRECTION('',(-1.,0.,0.));
#46201=DIRECTION('center_axis',(1.,0.,0.));
#46202=DIRECTION('ref_axis',(0.,1.,0.));
#46203=DIRECTION('',(-1.,0.,0.));
#46204=DIRECTION('center_axis',(1.,0.,0.));
#46205=DIRECTION('ref_axis',(0.,1.,0.));
#46206=DIRECTION('',(-1.,0.,0.));
#46207=DIRECTION('center_axis',(1.,0.,0.));
#46208=DIRECTION('ref_axis',(0.,1.,0.));
#46209=DIRECTION('',(-1.,0.,0.));
#46210=DIRECTION('center_axis',(1.,0.,0.));
#46211=DIRECTION('ref_axis',(0.,1.,0.));
#46212=DIRECTION('',(-1.,0.,0.));
#46213=DIRECTION('center_axis',(1.,0.,0.));
#46214=DIRECTION('ref_axis',(0.,1.,0.));
#46215=DIRECTION('',(-1.,0.,0.));
#46216=DIRECTION('center_axis',(1.,0.,0.));
#46217=DIRECTION('ref_axis',(0.,1.,0.));
#46218=DIRECTION('',(-1.,0.,0.));
#46219=DIRECTION('center_axis',(1.,0.,0.));
#46220=DIRECTION('ref_axis',(0.,1.,0.));
#46221=DIRECTION('',(-1.,0.,0.));
#46222=DIRECTION('center_axis',(1.,0.,0.));
#46223=DIRECTION('ref_axis',(0.,1.,0.));
#46224=DIRECTION('',(-1.,0.,0.));
#46225=DIRECTION('center_axis',(1.,0.,0.));
#46226=DIRECTION('ref_axis',(0.,1.,0.));
#46227=DIRECTION('',(-1.,0.,0.));
#46228=DIRECTION('center_axis',(1.,0.,0.));
#46229=DIRECTION('ref_axis',(0.,1.,0.));
#46230=DIRECTION('',(-1.,0.,0.));
#46231=DIRECTION('center_axis',(1.,0.,0.));
#46232=DIRECTION('ref_axis',(0.,1.,-9.17622152879152E-14));
#46233=DIRECTION('',(1.,0.,0.));
#46234=DIRECTION('center_axis',(1.,0.,0.));
#46235=DIRECTION('ref_axis',(0.,1.,-9.17622152879152E-14));
#46236=DIRECTION('center_axis',(1.,0.,0.));
#46237=DIRECTION('ref_axis',(0.,1.,-9.17622152879152E-14));
#46238=DIRECTION('',(1.,0.,0.));
#46239=DIRECTION('center_axis',(1.,0.,0.));
#46240=DIRECTION('ref_axis',(0.,1.,-9.17622152879152E-14));
#46241=DIRECTION('center_axis',(1.,0.,0.));
#46242=DIRECTION('ref_axis',(0.,1.,-9.17622152879152E-14));
#46243=DIRECTION('',(1.,0.,0.));
#46244=DIRECTION('center_axis',(1.,0.,0.));
#46245=DIRECTION('ref_axis',(0.,1.,-9.17622152879152E-14));
#46246=DIRECTION('',(1.,0.,0.));
#46247=DIRECTION('center_axis',(1.,0.,0.));
#46248=DIRECTION('ref_axis',(0.,1.,-9.17622152879152E-14));
#46249=DIRECTION('',(1.,0.,0.));
#46250=DIRECTION('center_axis',(1.,0.,0.));
#46251=DIRECTION('ref_axis',(0.,1.,-9.17622152879152E-14));
#46252=DIRECTION('',(1.,0.,0.));
#46253=DIRECTION('center_axis',(1.,0.,0.));
#46254=DIRECTION('ref_axis',(0.,1.,-9.17622152879152E-14));
#46255=DIRECTION('',(1.,0.,0.));
#46256=DIRECTION('center_axis',(1.,0.,0.));
#46257=DIRECTION('ref_axis',(0.,1.,-9.17622152879152E-14));
#46258=DIRECTION('',(1.,0.,0.));
#46259=DIRECTION('center_axis',(1.,0.,0.));
#46260=DIRECTION('ref_axis',(0.,1.,-9.17622152879152E-14));
#46261=DIRECTION('',(1.,0.,0.));
#46262=DIRECTION('center_axis',(1.,0.,0.));
#46263=DIRECTION('ref_axis',(0.,1.,-9.17622152879152E-14));
#46264=DIRECTION('',(1.,0.,0.));
#46265=DIRECTION('center_axis',(1.,0.,0.));
#46266=DIRECTION('ref_axis',(0.,1.,-9.17622152879152E-14));
#46267=DIRECTION('',(1.,0.,0.));
#46268=DIRECTION('center_axis',(1.,0.,0.));
#46269=DIRECTION('ref_axis',(0.,1.,-9.17622152879152E-14));
#46270=DIRECTION('',(1.,0.,0.));
#46271=DIRECTION('center_axis',(1.,0.,0.));
#46272=DIRECTION('ref_axis',(0.,1.,-9.17622152879152E-14));
#46273=DIRECTION('',(1.,0.,0.));
#46274=DIRECTION('center_axis',(1.,0.,0.));
#46275=DIRECTION('ref_axis',(0.,1.,-9.17622152879152E-14));
#46276=DIRECTION('',(1.,0.,0.));
#46277=DIRECTION('center_axis',(1.,0.,0.));
#46278=DIRECTION('ref_axis',(0.,1.,-9.17622152879152E-14));
#46279=DIRECTION('',(1.,0.,0.));
#46280=DIRECTION('center_axis',(1.,0.,0.));
#46281=DIRECTION('ref_axis',(0.,1.,-9.17622152879152E-14));
#46282=DIRECTION('',(1.,0.,0.));
#46283=DIRECTION('center_axis',(1.,0.,0.));
#46284=DIRECTION('ref_axis',(0.,1.,-9.17622152879152E-14));
#46285=DIRECTION('',(1.,0.,0.));
#46286=DIRECTION('center_axis',(1.,0.,0.));
#46287=DIRECTION('ref_axis',(0.,1.,-9.17622152879152E-14));
#46288=DIRECTION('',(1.,0.,0.));
#46289=DIRECTION('center_axis',(1.,0.,0.));
#46290=DIRECTION('ref_axis',(0.,1.,-9.17622152879152E-14));
#46291=DIRECTION('',(1.,0.,0.));
#46292=DIRECTION('center_axis',(1.,0.,0.));
#46293=DIRECTION('ref_axis',(0.,1.,-9.17622152879152E-14));
#46294=DIRECTION('',(1.,0.,0.));
#46295=DIRECTION('center_axis',(1.,0.,0.));
#46296=DIRECTION('ref_axis',(0.,1.,-9.17622152879152E-14));
#46297=DIRECTION('',(1.,0.,0.));
#46298=DIRECTION('center_axis',(1.,0.,0.));
#46299=DIRECTION('ref_axis',(0.,1.,-9.17622152879152E-14));
#46300=DIRECTION('',(1.,0.,0.));
#46301=DIRECTION('center_axis',(1.,0.,0.));
#46302=DIRECTION('ref_axis',(0.,1.,-9.17622152879152E-14));
#46303=DIRECTION('',(1.,0.,0.));
#46304=DIRECTION('center_axis',(1.,0.,0.));
#46305=DIRECTION('ref_axis',(0.,1.,-9.17622152879152E-14));
#46306=DIRECTION('',(1.,0.,0.));
#46307=DIRECTION('center_axis',(1.,0.,0.));
#46308=DIRECTION('ref_axis',(0.,1.,-9.17622152879152E-14));
#46309=DIRECTION('',(1.,0.,0.));
#46310=DIRECTION('center_axis',(1.,0.,0.));
#46311=DIRECTION('ref_axis',(0.,1.,-9.17622152879152E-14));
#46312=DIRECTION('',(1.,0.,0.));
#46313=DIRECTION('center_axis',(1.,0.,0.));
#46314=DIRECTION('ref_axis',(0.,1.,-9.17622152879152E-14));
#46315=DIRECTION('',(1.,0.,0.));
#46316=DIRECTION('center_axis',(1.,0.,0.));
#46317=DIRECTION('ref_axis',(0.,1.,-9.17622152879152E-14));
#46318=DIRECTION('',(1.,0.,0.));
#46319=DIRECTION('center_axis',(1.,0.,0.));
#46320=DIRECTION('ref_axis',(0.,1.,-9.17622152879152E-14));
#46321=DIRECTION('',(1.,0.,0.));
#46322=DIRECTION('center_axis',(-1.,0.,-1.02244356237877E-15));
#46323=DIRECTION('ref_axis',(0.,-1.,-3.30019287147236E-17));
#46324=DIRECTION('center_axis',(-1.,0.,0.));
#46325=DIRECTION('ref_axis',(0.,-1.,0.));
#46326=DIRECTION('',(-0.382683432365087,0.923879532511288,-2.47639794148994E-16));
#46327=DIRECTION('center_axis',(1.,0.,0.));
#46328=DIRECTION('ref_axis',(0.,-1.,-6.12323399573677E-17));
#46329=DIRECTION('center_axis',(1.,0.,0.));
#46330=DIRECTION('ref_axis',(0.,-1.,-6.12323399573677E-17));
#46331=DIRECTION('center_axis',(-1.,0.,0.));
#46332=DIRECTION('ref_axis',(0.,1.,0.));
#46333=DIRECTION('',(-0.707106781186544,-0.707106781186551,-8.65956056235498E-17));
#46334=DIRECTION('center_axis',(-1.,0.,0.));
#46335=DIRECTION('ref_axis',(0.,1.,0.));
#46336=DIRECTION('center_axis',(-1.,0.,0.));
#46337=DIRECTION('ref_axis',(0.,1.,0.));
#46338=DIRECTION('center_axis',(-1.,0.,0.));
#46339=DIRECTION('ref_axis',(0.,1.,0.));
#46340=DIRECTION('center_axis',(1.,0.,0.));
#46341=DIRECTION('ref_axis',(0.,0.,-1.));
#46342=DIRECTION('center_axis',(0.707106781186548,0.707106781186547,0.));
#46343=DIRECTION('ref_axis',(0.,0.,-1.));
#46344=DIRECTION('',(0.,0.,-1.));
#46345=DIRECTION('',(-0.344817162976176,0.344817162976177,0.873041951016171));
#46346=DIRECTION('',(0.,0.,1.));
#46347=DIRECTION('',(0.344817162976176,-0.344817162976177,0.873041951016171));
#46348=DIRECTION('center_axis',(1.,0.,0.));
#46349=DIRECTION('ref_axis',(0.,0.,-1.));
#46350=DIRECTION('center_axis',(1.,0.,0.));
#46351=DIRECTION('ref_axis',(0.,0.,-1.));
#46352=DIRECTION('center_axis',(1.,0.,0.));
#46353=DIRECTION('ref_axis',(0.,0.,-1.));
#46354=DIRECTION('center_axis',(0.,0.930084132110489,0.367346576404733));
#46355=DIRECTION('ref_axis',(0.,-0.367346576404732,0.930084132110489));
#46356=DIRECTION('',(-1.,0.,0.));
#46357=DIRECTION('',(-0.344817162976176,-0.344817162976177,0.873041951016171));
#46358=DIRECTION('',(1.,0.,0.));
#46359=DIRECTION('center_axis',(1.,0.,0.));
#46360=DIRECTION('ref_axis',(0.,-1.,1.22464679914735E-16));
#46361=DIRECTION('center_axis',(1.,0.,0.));
#46362=DIRECTION('ref_axis',(0.,0.,-1.));
#46363=DIRECTION('',(-1.,0.,0.));
#46364=DIRECTION('center_axis',(1.,0.,0.));
#46365=DIRECTION('ref_axis',(0.,0.,-1.));
#46366=DIRECTION('center_axis',(1.,0.,0.));
#46367=DIRECTION('ref_axis',(0.,-1.,5.66553889764798E-16));
#46368=DIRECTION('center_axis',(1.,0.,0.));
#46369=DIRECTION('ref_axis',(0.,0.,-1.));
#46370=DIRECTION('center_axis',(-0.707106781186548,0.707106781186547,0.));
#46371=DIRECTION('ref_axis',(0.,0.,1.));
#46372=DIRECTION('',(0.,0.,-1.));
#46373=DIRECTION('',(-0.344817162976176,-0.344817162976177,-0.873041951016171));
#46374=DIRECTION('',(0.,0.,1.));
#46375=DIRECTION('center_axis',(0.,-1.,0.));
#46376=DIRECTION('ref_axis',(0.,0.,1.));
#46377=DIRECTION('',(1.,0.,0.));
#46378=DIRECTION('center_axis',(-1.,0.,0.));
#46379=DIRECTION('ref_axis',(0.,0.,1.));
#46380=DIRECTION('center_axis',(0.,0.930084132110489,-0.367346576404733));
#46381=DIRECTION('ref_axis',(0.,0.367346576404732,0.930084132110489));
#46382=DIRECTION('center_axis',(-1.,0.,0.));
#46383=DIRECTION('ref_axis',(0.,-1.,-1.22464679914735E-16));
#46384=DIRECTION('center_axis',(1.,0.,0.));
#46385=DIRECTION('ref_axis',(0.,0.,-1.));
#46386=DIRECTION('center_axis',(1.,0.,0.));
#46387=DIRECTION('ref_axis',(0.,0.,-1.));
#46388=DIRECTION('center_axis',(-1.,0.,0.));
#46389=DIRECTION('ref_axis',(0.,1.,0.));
#46390=DIRECTION('center_axis',(-1.,0.,0.));
#46391=DIRECTION('ref_axis',(0.,1.,0.));
#46392=DIRECTION('center_axis',(-1.,0.,0.));
#46393=DIRECTION('ref_axis',(0.,1.,-9.17622152879152E-14));
#46394=DIRECTION('center_axis',(1.,0.,0.));
#46395=DIRECTION('ref_axis',(0.,0.899731237029652,0.436444384902695));
#46396=DIRECTION('center_axis',(1.,0.,0.));
#46397=DIRECTION('ref_axis',(0.,1.,0.));
#46398=DIRECTION('center_axis',(0.,-0.497058334900004,0.86771712654899));
#46399=DIRECTION('ref_axis',(0.,-0.86771712654899,-0.497058334900004));
#46400=DIRECTION('',(-1.,0.,0.));
#46401=DIRECTION('',(0.,-0.86771712654899,-0.497058334900004));
#46402=DIRECTION('',(1.,0.,0.));
#46403=DIRECTION('',(0.,-0.86771712654899,-0.497058334900004));
#46404=DIRECTION('center_axis',(1.,0.,0.));
#46405=DIRECTION('ref_axis',(0.,-0.17364817766693,-0.984807753012208));
#46406=DIRECTION('center_axis',(-1.,0.,0.));
#46407=DIRECTION('ref_axis',(0.,1.,0.));
#46408=DIRECTION('',(0.,0.64538341780392,-0.763858785394087));
#46409=DIRECTION('center_axis',(0.,-0.763858785394087,-0.645383417803921));
#46410=DIRECTION('ref_axis',(0.,0.64538341780392,-0.763858785394087));
#46411=DIRECTION('',(1.,0.,0.));
#46412=DIRECTION('',(0.,0.64538341780392,-0.763858785394087));
#46413=DIRECTION('center_axis',(1.,0.,0.));
#46414=DIRECTION('ref_axis',(0.,-0.17364817766693,-0.984807753012208));
#46415=DIRECTION('center_axis',(1.,0.,0.));
#46416=DIRECTION('ref_axis',(0.,1.,0.));
#46417=DIRECTION('center_axis',(0.,-0.338829404153244,0.940847827696465));
#46418=DIRECTION('ref_axis',(0.,-0.940847827696465,-0.338829404153244));
#46419=DIRECTION('',(-1.,0.,0.));
#46420=DIRECTION('',(0.,-0.940847827696465,-0.338829404153244));
#46421=DIRECTION('',(1.,0.,0.));
#46422=DIRECTION('',(0.,-0.940847827696465,-0.338829404153244));
#46423=DIRECTION('center_axis',(1.,0.,0.));
#46424=DIRECTION('ref_axis',(0.,-0.342020143325669,-0.939692620785908));
#46425=DIRECTION('center_axis',(-1.,0.,0.));
#46426=DIRECTION('ref_axis',(0.,1.,0.));
#46427=DIRECTION('',(0.,0.502935907440259,-0.864323708460692));
#46428=DIRECTION('center_axis',(0.,-0.864323708460692,-0.502935907440259));
#46429=DIRECTION('ref_axis',(0.,0.502935907440259,-0.864323708460692));
#46430=DIRECTION('',(1.,0.,0.));
#46431=DIRECTION('',(0.,0.502935907440259,-0.864323708460692));
#46432=DIRECTION('center_axis',(1.,0.,0.));
#46433=DIRECTION('ref_axis',(0.,-0.342020143325669,-0.939692620785908));
#46434=DIRECTION('center_axis',(1.,0.,0.));
#46435=DIRECTION('ref_axis',(0.,1.,0.));
#46436=DIRECTION('center_axis',(0.,-0.170305313417241,0.985391343691356));
#46437=DIRECTION('ref_axis',(0.,-0.985391343691356,-0.170305313417241));
#46438=DIRECTION('',(-1.,0.,0.));
#46439=DIRECTION('',(0.,-0.985391343691356,-0.170305313417241));
#46440=DIRECTION('',(1.,0.,0.));
#46441=DIRECTION('',(0.,-0.985391343691356,-0.170305313417241));
#46442=DIRECTION('center_axis',(1.,0.,0.));
#46443=DIRECTION('ref_axis',(0.,-0.5,-0.866025403784438));
#46444=DIRECTION('center_axis',(-1.,0.,0.));
#46445=DIRECTION('ref_axis',(0.,1.,0.));
#46446=DIRECTION('',(0.,0.345206944026876,-0.938526593014618));
#46447=DIRECTION('center_axis',(0.,-0.938526593014618,-0.345206944026876));
#46448=DIRECTION('ref_axis',(0.,0.345206944026876,-0.938526593014618));
#46449=DIRECTION('',(1.,0.,0.));
#46450=DIRECTION('',(0.,0.345206944026876,-0.938526593014618));
#46451=DIRECTION('center_axis',(1.,0.,0.));
#46452=DIRECTION('ref_axis',(0.,-0.5,-0.866025403784438));
#46453=DIRECTION('center_axis',(1.,0.,0.));
#46454=DIRECTION('ref_axis',(0.,1.,0.));
#46455=DIRECTION('center_axis',(0.,0.00339341808829885,0.999994242340264));
#46456=DIRECTION('ref_axis',(0.,-0.999994242340264,0.00339341808829885));
#46457=DIRECTION('',(-1.,0.,0.));
#46458=DIRECTION('',(0.,-0.999994242340264,0.00339341808829885));
#46459=DIRECTION('',(1.,0.,0.));
#46460=DIRECTION('',(0.,-0.999994242340264,0.00339341808829885));
#46461=DIRECTION('center_axis',(1.,0.,0.));
#46462=DIRECTION('ref_axis',(0.,-0.64278760968654,-0.766044443118978));
#46463=DIRECTION('center_axis',(-1.,0.,0.));
#46464=DIRECTION('ref_axis',(0.,1.,0.));
#46465=DIRECTION('',(0.,0.176989042302377,-0.984212821957166));
#46466=DIRECTION('center_axis',(0.,-0.984212821957166,-0.176989042302377));
#46467=DIRECTION('ref_axis',(0.,0.176989042302377,-0.984212821957166));
#46468=DIRECTION('',(1.,0.,0.));
#46469=DIRECTION('',(0.,0.176989042302377,-0.984212821957166));
#46470=DIRECTION('center_axis',(1.,0.,0.));
#46471=DIRECTION('ref_axis',(0.,-0.64278760968654,-0.766044443118978));
#46472=DIRECTION('center_axis',(1.,0.,0.));
#46473=DIRECTION('ref_axis',(0.,1.,0.));
#46474=DIRECTION('center_axis',(0.,0.176989042302378,0.984212821957166));
#46475=DIRECTION('ref_axis',(0.,-0.984212821957165,0.176989042302378));
#46476=DIRECTION('',(-1.,0.,0.));
#46477=DIRECTION('',(0.,-0.984212821957165,0.176989042302378));
#46478=DIRECTION('',(1.,0.,0.));
#46479=DIRECTION('',(0.,-0.984212821957165,0.176989042302378));
#46480=DIRECTION('center_axis',(1.,0.,0.));
#46481=DIRECTION('ref_axis',(0.,-0.766044443118978,-0.642787609686539));
#46482=DIRECTION('center_axis',(-1.,0.,0.));
#46483=DIRECTION('ref_axis',(0.,1.,0.));
#46484=DIRECTION('',(0.,0.00339341808829835,-0.999994242340264));
#46485=DIRECTION('center_axis',(0.,-0.999994242340264,-0.00339341808829835));
#46486=DIRECTION('ref_axis',(0.,0.00339341808829835,-0.999994242340264));
#46487=DIRECTION('',(1.,0.,0.));
#46488=DIRECTION('',(0.,0.00339341808829835,-0.999994242340264));
#46489=DIRECTION('center_axis',(1.,0.,0.));
#46490=DIRECTION('ref_axis',(0.,-0.766044443118978,-0.642787609686539));
#46491=DIRECTION('center_axis',(1.,0.,0.));
#46492=DIRECTION('ref_axis',(0.,1.,0.));
#46493=DIRECTION('center_axis',(0.,0.345206944026876,0.938526593014618));
#46494=DIRECTION('ref_axis',(0.,-0.938526593014617,0.345206944026876));
#46495=DIRECTION('',(-1.,0.,0.));
#46496=DIRECTION('',(0.,-0.938526593014617,0.345206944026876));
#46497=DIRECTION('',(1.,0.,0.));
#46498=DIRECTION('',(0.,-0.938526593014617,0.345206944026876));
#46499=DIRECTION('center_axis',(1.,0.,0.));
#46500=DIRECTION('ref_axis',(0.,-0.866025403784439,-0.5));
#46501=DIRECTION('center_axis',(-1.,0.,0.));
#46502=DIRECTION('ref_axis',(0.,1.,0.));
#46503=DIRECTION('',(0.,-0.170305313417241,-0.985391343691356));
#46504=DIRECTION('center_axis',(0.,-0.985391343691356,0.170305313417241));
#46505=DIRECTION('ref_axis',(0.,-0.170305313417241,-0.985391343691356));
#46506=DIRECTION('',(1.,0.,0.));
#46507=DIRECTION('',(0.,-0.170305313417241,-0.985391343691356));
#46508=DIRECTION('center_axis',(1.,0.,0.));
#46509=DIRECTION('ref_axis',(0.,-0.866025403784439,-0.5));
#46510=DIRECTION('center_axis',(1.,0.,0.));
#46511=DIRECTION('ref_axis',(0.,1.,0.));
#46512=DIRECTION('center_axis',(0.,0.502935907440261,0.864323708460691));
#46513=DIRECTION('ref_axis',(0.,-0.864323708460691,0.502935907440261));
#46514=DIRECTION('',(-1.,0.,0.));
#46515=DIRECTION('',(0.,-0.864323708460691,0.502935907440261));
#46516=DIRECTION('',(1.,0.,0.));
#46517=DIRECTION('',(0.,-0.864323708460691,0.502935907440261));
#46518=DIRECTION('center_axis',(1.,0.,0.));
#46519=DIRECTION('ref_axis',(0.,-0.939692620785909,-0.342020143325668));
#46520=DIRECTION('center_axis',(-1.,0.,0.));
#46521=DIRECTION('ref_axis',(0.,1.,0.));
#46522=DIRECTION('',(0.,-0.338829404153245,-0.940847827696465));
#46523=DIRECTION('center_axis',(0.,-0.940847827696465,0.338829404153246));
#46524=DIRECTION('ref_axis',(0.,-0.338829404153245,-0.940847827696465));
#46525=DIRECTION('',(1.,0.,0.));
#46526=DIRECTION('',(0.,-0.338829404153245,-0.940847827696465));
#46527=DIRECTION('center_axis',(1.,0.,0.));
#46528=DIRECTION('ref_axis',(0.,-0.939692620785909,-0.342020143325668));
#46529=DIRECTION('center_axis',(1.,0.,0.));
#46530=DIRECTION('ref_axis',(0.,1.,0.));
#46531=DIRECTION('center_axis',(0.,0.645383417803921,0.763858785394087));
#46532=DIRECTION('ref_axis',(0.,-0.763858785394087,0.645383417803921));
#46533=DIRECTION('',(-1.,0.,0.));
#46534=DIRECTION('',(0.,-0.763858785394087,0.645383417803921));
#46535=DIRECTION('',(1.,0.,0.));
#46536=DIRECTION('',(0.,-0.763858785394087,0.645383417803921));
#46537=DIRECTION('center_axis',(1.,0.,0.));
#46538=DIRECTION('ref_axis',(0.,-0.984807753012208,-0.17364817766693));
#46539=DIRECTION('center_axis',(-1.,0.,0.));
#46540=DIRECTION('ref_axis',(0.,1.,0.));
#46541=DIRECTION('',(0.,-0.497058334900004,-0.86771712654899));
#46542=DIRECTION('center_axis',(0.,-0.86771712654899,0.497058334900004));
#46543=DIRECTION('ref_axis',(0.,-0.497058334900004,-0.86771712654899));
#46544=DIRECTION('',(1.,0.,0.));
#46545=DIRECTION('',(0.,-0.497058334900004,-0.86771712654899));
#46546=DIRECTION('center_axis',(1.,0.,0.));
#46547=DIRECTION('ref_axis',(0.,-0.984807753012208,-0.17364817766693));
#46548=DIRECTION('center_axis',(1.,0.,0.));
#46549=DIRECTION('ref_axis',(0.,1.,0.));
#46550=DIRECTION('center_axis',(0.,0.768221279597376,0.640184399664479));
#46551=DIRECTION('ref_axis',(0.,-0.640184399664479,0.768221279597376));
#46552=DIRECTION('',(-1.,0.,0.));
#46553=DIRECTION('',(0.,-0.640184399664479,0.768221279597376));
#46554=DIRECTION('',(1.,0.,0.));
#46555=DIRECTION('',(0.,-0.640184399664479,0.768221279597376));
#46556=DIRECTION('center_axis',(1.,0.,0.));
#46557=DIRECTION('ref_axis',(0.,-1.,1.83697019872103E-16));
#46558=DIRECTION('center_axis',(-1.,0.,0.));
#46559=DIRECTION('ref_axis',(0.,1.,0.));
#46560=DIRECTION('',(0.,-0.64018439966448,-0.768221279597376));
#46561=DIRECTION('center_axis',(0.,-0.768221279597376,0.64018439966448));
#46562=DIRECTION('ref_axis',(0.,-0.64018439966448,-0.768221279597376));
#46563=DIRECTION('',(1.,0.,0.));
#46564=DIRECTION('',(0.,-0.64018439966448,-0.768221279597376));
#46565=DIRECTION('center_axis',(1.,0.,0.));
#46566=DIRECTION('ref_axis',(0.,-1.,1.83697019872103E-16));
#46567=DIRECTION('center_axis',(1.,0.,0.));
#46568=DIRECTION('ref_axis',(0.,1.,0.));
#46569=DIRECTION('center_axis',(0.,0.86771712654899,0.497058334900004));
#46570=DIRECTION('ref_axis',(0.,-0.497058334900004,0.86771712654899));
#46571=DIRECTION('',(-1.,0.,0.));
#46572=DIRECTION('',(0.,-0.497058334900004,0.86771712654899));
#46573=DIRECTION('',(1.,0.,0.));
#46574=DIRECTION('',(0.,-0.497058334900004,0.86771712654899));
#46575=DIRECTION('center_axis',(1.,0.,0.));
#46576=DIRECTION('ref_axis',(0.,-0.984807753012208,0.17364817766693));
#46577=DIRECTION('center_axis',(-1.,0.,0.));
#46578=DIRECTION('ref_axis',(0.,1.,0.));
#46579=DIRECTION('',(0.,-0.763858785394087,-0.645383417803921));
#46580=DIRECTION('center_axis',(0.,-0.645383417803921,0.763858785394087));
#46581=DIRECTION('ref_axis',(0.,-0.763858785394087,-0.645383417803921));
#46582=DIRECTION('',(1.,0.,0.));
#46583=DIRECTION('',(0.,-0.763858785394087,-0.645383417803921));
#46584=DIRECTION('center_axis',(1.,0.,0.));
#46585=DIRECTION('ref_axis',(0.,-0.984807753012208,0.17364817766693));
#46586=DIRECTION('center_axis',(1.,0.,0.));
#46587=DIRECTION('ref_axis',(0.,1.,0.));
#46588=DIRECTION('center_axis',(0.,0.940847827696465,0.338829404153244));
#46589=DIRECTION('ref_axis',(0.,-0.338829404153244,0.940847827696465));
#46590=DIRECTION('',(-1.,0.,0.));
#46591=DIRECTION('',(0.,-0.338829404153244,0.940847827696465));
#46592=DIRECTION('',(1.,0.,0.));
#46593=DIRECTION('',(0.,-0.338829404153244,0.940847827696465));
#46594=DIRECTION('center_axis',(1.,0.,0.));
#46595=DIRECTION('ref_axis',(0.,-0.939692620785908,0.342020143325669));
#46596=DIRECTION('center_axis',(-1.,0.,0.));
#46597=DIRECTION('ref_axis',(0.,1.,0.));
#46598=DIRECTION('',(0.,-0.864323708460692,-0.50293590744026));
#46599=DIRECTION('center_axis',(0.,-0.50293590744026,0.864323708460692));
#46600=DIRECTION('ref_axis',(0.,-0.864323708460692,-0.50293590744026));
#46601=DIRECTION('',(1.,0.,0.));
#46602=DIRECTION('',(0.,-0.864323708460692,-0.50293590744026));
#46603=DIRECTION('center_axis',(1.,0.,0.));
#46604=DIRECTION('ref_axis',(0.,-0.939692620785908,0.342020143325669));
#46605=DIRECTION('center_axis',(1.,0.,0.));
#46606=DIRECTION('ref_axis',(0.,1.,0.));
#46607=DIRECTION('center_axis',(0.,0.985391343691356,0.170305313417241));
#46608=DIRECTION('ref_axis',(0.,-0.170305313417241,0.985391343691356));
#46609=DIRECTION('',(-1.,0.,0.));
#46610=DIRECTION('',(0.,-0.170305313417241,0.985391343691356));
#46611=DIRECTION('',(1.,0.,0.));
#46612=DIRECTION('',(0.,-0.170305313417241,0.985391343691356));
#46613=DIRECTION('center_axis',(1.,0.,0.));
#46614=DIRECTION('ref_axis',(0.,-0.866025403784438,0.5));
#46615=DIRECTION('center_axis',(-1.,0.,0.));
#46616=DIRECTION('ref_axis',(0.,1.,0.));
#46617=DIRECTION('',(0.,-0.938526593014618,-0.345206944026876));
#46618=DIRECTION('center_axis',(0.,-0.345206944026876,0.938526593014618));
#46619=DIRECTION('ref_axis',(0.,-0.938526593014618,-0.345206944026876));
#46620=DIRECTION('',(1.,0.,0.));
#46621=DIRECTION('',(0.,-0.938526593014618,-0.345206944026876));
#46622=DIRECTION('center_axis',(1.,0.,0.));
#46623=DIRECTION('ref_axis',(0.,-0.866025403784438,0.5));
#46624=DIRECTION('center_axis',(1.,0.,0.));
#46625=DIRECTION('ref_axis',(0.,1.,0.));
#46626=DIRECTION('center_axis',(0.,0.999994242340264,-0.00339341808829868));
#46627=DIRECTION('ref_axis',(0.,0.00339341808829868,0.999994242340264));
#46628=DIRECTION('',(-1.,0.,0.));
#46629=DIRECTION('',(0.,0.00339341808829868,0.999994242340264));
#46630=DIRECTION('',(1.,0.,0.));
#46631=DIRECTION('',(0.,0.00339341808829868,0.999994242340264));
#46632=DIRECTION('center_axis',(1.,0.,0.));
#46633=DIRECTION('ref_axis',(0.,-0.766044443118978,0.642787609686539));
#46634=DIRECTION('center_axis',(-1.,0.,0.));
#46635=DIRECTION('ref_axis',(0.,1.,0.));
#46636=DIRECTION('',(0.,-0.984212821957166,-0.176989042302378));
#46637=DIRECTION('center_axis',(0.,-0.176989042302378,0.984212821957166));
#46638=DIRECTION('ref_axis',(0.,-0.984212821957166,-0.176989042302378));
#46639=DIRECTION('',(1.,0.,0.));
#46640=DIRECTION('',(0.,-0.984212821957166,-0.176989042302378));
#46641=DIRECTION('center_axis',(1.,0.,0.));
#46642=DIRECTION('ref_axis',(0.,-0.766044443118978,0.642787609686539));
#46643=DIRECTION('center_axis',(1.,0.,0.));
#46644=DIRECTION('ref_axis',(0.,1.,0.));
#46645=DIRECTION('center_axis',(0.,0.984212821957166,-0.176989042302378));
#46646=DIRECTION('ref_axis',(0.,0.176989042302378,0.984212821957166));
#46647=DIRECTION('',(-1.,0.,0.));
#46648=DIRECTION('',(0.,0.176989042302378,0.984212821957166));
#46649=DIRECTION('',(1.,0.,0.));
#46650=DIRECTION('',(0.,0.176989042302378,0.984212821957166));
#46651=DIRECTION('center_axis',(1.,0.,0.));
#46652=DIRECTION('ref_axis',(0.,-0.642787609686539,0.766044443118978));
#46653=DIRECTION('center_axis',(-1.,0.,0.));
#46654=DIRECTION('ref_axis',(0.,1.,0.));
#46655=DIRECTION('',(0.,-0.999994242340264,-0.00339341808829846));
#46656=DIRECTION('center_axis',(0.,-0.00339341808829846,0.999994242340264));
#46657=DIRECTION('ref_axis',(0.,-0.999994242340264,-0.00339341808829846));
#46658=DIRECTION('',(1.,0.,0.));
#46659=DIRECTION('',(0.,-0.999994242340264,-0.00339341808829846));
#46660=DIRECTION('center_axis',(1.,0.,0.));
#46661=DIRECTION('ref_axis',(0.,-0.642787609686539,0.766044443118978));
#46662=DIRECTION('center_axis',(1.,0.,0.));
#46663=DIRECTION('ref_axis',(0.,1.,0.));
#46664=DIRECTION('center_axis',(0.,0.938526593014617,-0.345206944026876));
#46665=DIRECTION('ref_axis',(0.,0.345206944026876,0.938526593014617));
#46666=DIRECTION('',(-1.,0.,0.));
#46667=DIRECTION('',(0.,0.345206944026876,0.938526593014617));
#46668=DIRECTION('',(1.,0.,0.));
#46669=DIRECTION('',(0.,0.345206944026876,0.938526593014617));
#46670=DIRECTION('center_axis',(1.,0.,0.));
#46671=DIRECTION('ref_axis',(0.,-0.5,0.866025403784439));
#46672=DIRECTION('center_axis',(-1.,0.,0.));
#46673=DIRECTION('ref_axis',(0.,1.,0.));
#46674=DIRECTION('',(0.,-0.985391343691356,0.170305313417242));
#46675=DIRECTION('center_axis',(0.,0.170305313417242,0.985391343691356));
#46676=DIRECTION('ref_axis',(0.,-0.985391343691356,0.170305313417242));
#46677=DIRECTION('',(1.,0.,0.));
#46678=DIRECTION('',(0.,-0.985391343691356,0.170305313417242));
#46679=DIRECTION('center_axis',(1.,0.,0.));
#46680=DIRECTION('ref_axis',(0.,-0.5,0.866025403784439));
#46681=DIRECTION('center_axis',(1.,0.,0.));
#46682=DIRECTION('ref_axis',(0.,1.,0.));
#46683=DIRECTION('center_axis',(0.,0.864323708460691,-0.50293590744026));
#46684=DIRECTION('ref_axis',(0.,0.50293590744026,0.864323708460691));
#46685=DIRECTION('',(-1.,0.,0.));
#46686=DIRECTION('',(0.,0.50293590744026,0.864323708460691));
#46687=DIRECTION('',(1.,0.,0.));
#46688=DIRECTION('',(0.,0.50293590744026,0.864323708460691));
#46689=DIRECTION('center_axis',(1.,0.,0.));
#46690=DIRECTION('ref_axis',(0.,-0.342020143325669,0.939692620785909));
#46691=DIRECTION('center_axis',(-1.,0.,0.));
#46692=DIRECTION('ref_axis',(0.,1.,0.));
#46693=DIRECTION('',(0.,-0.940847827696465,0.338829404153245));
#46694=DIRECTION('center_axis',(0.,0.338829404153245,0.940847827696465));
#46695=DIRECTION('ref_axis',(0.,-0.940847827696465,0.338829404153245));
#46696=DIRECTION('',(1.,0.,0.));
#46697=DIRECTION('',(0.,-0.940847827696465,0.338829404153245));
#46698=DIRECTION('center_axis',(1.,0.,0.));
#46699=DIRECTION('ref_axis',(0.,-0.342020143325669,0.939692620785909));
#46700=DIRECTION('center_axis',(1.,0.,0.));
#46701=DIRECTION('ref_axis',(0.,1.,0.));
#46702=DIRECTION('center_axis',(0.,0.763858785394087,-0.645383417803921));
#46703=DIRECTION('ref_axis',(0.,0.645383417803921,0.763858785394087));
#46704=DIRECTION('',(-1.,0.,0.));
#46705=DIRECTION('',(0.,0.645383417803921,0.763858785394087));
#46706=DIRECTION('',(1.,0.,0.));
#46707=DIRECTION('',(0.,0.645383417803921,0.763858785394087));
#46708=DIRECTION('center_axis',(1.,0.,0.));
#46709=DIRECTION('ref_axis',(0.,-0.17364817766693,0.984807753012208));
#46710=DIRECTION('center_axis',(-1.,0.,0.));
#46711=DIRECTION('ref_axis',(0.,1.,0.));
#46712=DIRECTION('',(0.,-0.86771712654899,0.497058334900004));
#46713=DIRECTION('center_axis',(0.,0.497058334900004,0.86771712654899));
#46714=DIRECTION('ref_axis',(0.,-0.86771712654899,0.497058334900004));
#46715=DIRECTION('',(1.,0.,0.));
#46716=DIRECTION('',(0.,-0.86771712654899,0.497058334900004));
#46717=DIRECTION('center_axis',(1.,0.,0.));
#46718=DIRECTION('ref_axis',(0.,-0.17364817766693,0.984807753012208));
#46719=DIRECTION('center_axis',(1.,0.,0.));
#46720=DIRECTION('ref_axis',(0.,1.,0.));
#46721=DIRECTION('center_axis',(0.,0.640184399664479,-0.768221279597376));
#46722=DIRECTION('ref_axis',(0.,0.768221279597376,0.640184399664479));
#46723=DIRECTION('',(-1.,0.,0.));
#46724=DIRECTION('',(0.,0.768221279597376,0.640184399664479));
#46725=DIRECTION('',(1.,0.,0.));
#46726=DIRECTION('',(0.,0.768221279597376,0.640184399664479));
#46727=DIRECTION('center_axis',(1.,0.,0.));
#46728=DIRECTION('ref_axis',(0.,1.22464679914735E-16,1.));
#46729=DIRECTION('center_axis',(-1.,0.,0.));
#46730=DIRECTION('ref_axis',(0.,1.,0.));
#46731=DIRECTION('',(0.,-0.768221279597376,0.64018439966448));
#46732=DIRECTION('center_axis',(-1.,0.,0.));
#46733=DIRECTION('ref_axis',(0.,1.,0.));
#46734=DIRECTION('center_axis',(0.,0.64018439966448,0.768221279597376));
#46735=DIRECTION('ref_axis',(0.,-0.768221279597376,0.64018439966448));
#46736=DIRECTION('',(1.,0.,0.));
#46737=DIRECTION('',(0.,-0.768221279597376,0.64018439966448));
#46738=DIRECTION('center_axis',(1.,0.,0.));
#46739=DIRECTION('ref_axis',(0.,1.22464679914735E-16,1.));
#46740=DIRECTION('center_axis',(1.,0.,0.));
#46741=DIRECTION('ref_axis',(0.,1.,0.));
#46742=DIRECTION('center_axis',(1.,0.,0.));
#46743=DIRECTION('ref_axis',(0.,1.,0.));
#46744=DIRECTION('center_axis',(0.,0.497058334900004,-0.86771712654899));
#46745=DIRECTION('ref_axis',(0.,0.86771712654899,0.497058334900003));
#46746=DIRECTION('',(-1.,0.,0.));
#46747=DIRECTION('',(0.,0.86771712654899,0.497058334900003));
#46748=DIRECTION('',(1.,0.,0.));
#46749=DIRECTION('',(0.,0.86771712654899,0.497058334900003));
#46750=DIRECTION('center_axis',(1.,0.,0.));
#46751=DIRECTION('ref_axis',(0.,0.173648177666931,0.984807753012208));
#46752=DIRECTION('center_axis',(-1.,0.,0.));
#46753=DIRECTION('ref_axis',(0.,1.,0.));
#46754=DIRECTION('',(0.,-0.64538341780392,0.763858785394087));
#46755=DIRECTION('center_axis',(0.,0.763858785394087,0.64538341780392));
#46756=DIRECTION('ref_axis',(0.,-0.64538341780392,0.763858785394087));
#46757=DIRECTION('',(1.,0.,0.));
#46758=DIRECTION('',(0.,-0.64538341780392,0.763858785394087));
#46759=DIRECTION('center_axis',(1.,0.,0.));
#46760=DIRECTION('ref_axis',(0.,0.173648177666931,0.984807753012208));
#46761=DIRECTION('center_axis',(1.,0.,0.));
#46762=DIRECTION('ref_axis',(0.,1.,0.));
#46763=DIRECTION('center_axis',(0.,0.338829404153245,-0.940847827696465));
#46764=DIRECTION('ref_axis',(0.,0.940847827696465,0.338829404153245));
#46765=DIRECTION('',(-1.,0.,0.));
#46766=DIRECTION('',(0.,0.940847827696465,0.338829404153245));
#46767=DIRECTION('',(1.,0.,0.));
#46768=DIRECTION('',(0.,0.940847827696465,0.338829404153245));
#46769=DIRECTION('center_axis',(1.,0.,0.));
#46770=DIRECTION('ref_axis',(0.,0.342020143325669,0.939692620785908));
#46771=DIRECTION('center_axis',(-1.,0.,0.));
#46772=DIRECTION('ref_axis',(0.,1.,0.));
#46773=DIRECTION('',(0.,-0.50293590744026,0.864323708460692));
#46774=DIRECTION('center_axis',(0.,0.864323708460692,0.50293590744026));
#46775=DIRECTION('ref_axis',(0.,-0.50293590744026,0.864323708460692));
#46776=DIRECTION('',(1.,0.,0.));
#46777=DIRECTION('',(0.,-0.50293590744026,0.864323708460692));
#46778=DIRECTION('center_axis',(1.,0.,0.));
#46779=DIRECTION('ref_axis',(0.,0.342020143325669,0.939692620785908));
#46780=DIRECTION('center_axis',(1.,0.,0.));
#46781=DIRECTION('ref_axis',(0.,1.,0.));
#46782=DIRECTION('center_axis',(0.,0.170305313417241,-0.985391343691356));
#46783=DIRECTION('ref_axis',(0.,0.985391343691356,0.170305313417241));
#46784=DIRECTION('',(-1.,0.,0.));
#46785=DIRECTION('',(0.,0.985391343691356,0.170305313417241));
#46786=DIRECTION('',(1.,0.,0.));
#46787=DIRECTION('',(0.,0.985391343691356,0.170305313417241));
#46788=DIRECTION('center_axis',(1.,0.,0.));
#46789=DIRECTION('ref_axis',(0.,0.5,0.866025403784439));
#46790=DIRECTION('center_axis',(-1.,0.,0.));
#46791=DIRECTION('ref_axis',(0.,1.,0.));
#46792=DIRECTION('',(0.,-0.345206944026876,0.938526593014617));
#46793=DIRECTION('center_axis',(0.,0.938526593014617,0.345206944026876));
#46794=DIRECTION('ref_axis',(0.,-0.345206944026876,0.938526593014617));
#46795=DIRECTION('',(1.,0.,0.));
#46796=DIRECTION('',(0.,-0.345206944026876,0.938526593014617));
#46797=DIRECTION('center_axis',(1.,0.,0.));
#46798=DIRECTION('ref_axis',(0.,0.5,0.866025403784439));
#46799=DIRECTION('center_axis',(1.,0.,0.));
#46800=DIRECTION('ref_axis',(0.,1.,0.));
#46801=DIRECTION('center_axis',(0.,-0.00339341808829868,-0.999994242340264));
#46802=DIRECTION('ref_axis',(0.,0.999994242340264,-0.00339341808829868));
#46803=DIRECTION('',(-1.,0.,0.));
#46804=DIRECTION('',(0.,0.999994242340264,-0.00339341808829868));
#46805=DIRECTION('',(1.,0.,0.));
#46806=DIRECTION('',(0.,0.999994242340264,-0.00339341808829868));
#46807=DIRECTION('center_axis',(1.,0.,0.));
#46808=DIRECTION('ref_axis',(0.,0.642787609686539,0.766044443118978));
#46809=DIRECTION('center_axis',(-1.,0.,0.));
#46810=DIRECTION('ref_axis',(0.,1.,0.));
#46811=DIRECTION('',(0.,-0.176989042302378,0.984212821957166));
#46812=DIRECTION('center_axis',(0.,0.984212821957166,0.176989042302378));
#46813=DIRECTION('ref_axis',(0.,-0.176989042302378,0.984212821957166));
#46814=DIRECTION('',(1.,0.,0.));
#46815=DIRECTION('',(0.,-0.176989042302378,0.984212821957166));
#46816=DIRECTION('center_axis',(1.,0.,0.));
#46817=DIRECTION('ref_axis',(0.,0.642787609686539,0.766044443118978));
#46818=DIRECTION('center_axis',(1.,0.,0.));
#46819=DIRECTION('ref_axis',(0.,1.,0.));
#46820=DIRECTION('center_axis',(0.,-0.176989042302378,-0.984212821957166));
#46821=DIRECTION('ref_axis',(0.,0.984212821957166,-0.176989042302378));
#46822=DIRECTION('',(-1.,0.,0.));
#46823=DIRECTION('',(0.,0.984212821957166,-0.176989042302378));
#46824=DIRECTION('',(1.,0.,0.));
#46825=DIRECTION('',(0.,0.984212821957166,-0.176989042302378));
#46826=DIRECTION('center_axis',(1.,0.,0.));
#46827=DIRECTION('ref_axis',(0.,0.766044443118978,0.642787609686539));
#46828=DIRECTION('center_axis',(-1.,0.,0.));
#46829=DIRECTION('ref_axis',(0.,1.,0.));
#46830=DIRECTION('',(0.,-0.00339341808829857,0.999994242340264));
#46831=DIRECTION('center_axis',(0.,0.999994242340264,0.00339341808829857));
#46832=DIRECTION('ref_axis',(0.,-0.00339341808829857,0.999994242340264));
#46833=DIRECTION('',(1.,0.,0.));
#46834=DIRECTION('',(0.,-0.00339341808829857,0.999994242340264));
#46835=DIRECTION('center_axis',(1.,0.,0.));
#46836=DIRECTION('ref_axis',(0.,0.766044443118978,0.642787609686539));
#46837=DIRECTION('center_axis',(1.,0.,0.));
#46838=DIRECTION('ref_axis',(0.,1.,0.));
#46839=DIRECTION('center_axis',(0.,-0.345206944026876,-0.938526593014617));
#46840=DIRECTION('ref_axis',(0.,0.938526593014617,-0.345206944026876));
#46841=DIRECTION('',(-1.,0.,0.));
#46842=DIRECTION('',(0.,0.938526593014617,-0.345206944026876));
#46843=DIRECTION('',(1.,0.,0.));
#46844=DIRECTION('',(0.,0.938526593014617,-0.345206944026876));
#46845=DIRECTION('center_axis',(1.,0.,0.));
#46846=DIRECTION('ref_axis',(0.,0.866025403784439,0.5));
#46847=DIRECTION('center_axis',(-1.,0.,0.));
#46848=DIRECTION('ref_axis',(0.,1.,0.));
#46849=DIRECTION('',(0.,0.170305313417242,0.985391343691356));
#46850=DIRECTION('center_axis',(0.,0.985391343691356,-0.170305313417242));
#46851=DIRECTION('ref_axis',(0.,0.170305313417242,0.985391343691356));
#46852=DIRECTION('',(1.,0.,0.));
#46853=DIRECTION('',(0.,0.170305313417242,0.985391343691356));
#46854=DIRECTION('center_axis',(1.,0.,0.));
#46855=DIRECTION('ref_axis',(0.,0.866025403784439,0.5));
#46856=DIRECTION('center_axis',(1.,0.,0.));
#46857=DIRECTION('ref_axis',(0.,1.,0.));
#46858=DIRECTION('center_axis',(0.,-0.50293590744026,-0.864323708460692));
#46859=DIRECTION('ref_axis',(0.,0.864323708460691,-0.50293590744026));
#46860=DIRECTION('',(-1.,0.,0.));
#46861=DIRECTION('',(0.,0.864323708460691,-0.50293590744026));
#46862=DIRECTION('',(1.,0.,0.));
#46863=DIRECTION('',(0.,0.864323708460691,-0.50293590744026));
#46864=DIRECTION('center_axis',(1.,0.,0.));
#46865=DIRECTION('ref_axis',(0.,0.939692620785908,0.342020143325669));
#46866=DIRECTION('center_axis',(-1.,0.,0.));
#46867=DIRECTION('ref_axis',(0.,1.,0.));
#46868=DIRECTION('',(0.,0.338829404153245,0.940847827696465));
#46869=DIRECTION('center_axis',(0.,0.940847827696465,-0.338829404153245));
#46870=DIRECTION('ref_axis',(0.,0.338829404153245,0.940847827696465));
#46871=DIRECTION('',(1.,0.,0.));
#46872=DIRECTION('',(0.,0.338829404153245,0.940847827696465));
#46873=DIRECTION('center_axis',(1.,0.,0.));
#46874=DIRECTION('ref_axis',(0.,0.939692620785908,0.342020143325669));
#46875=DIRECTION('center_axis',(1.,0.,0.));
#46876=DIRECTION('ref_axis',(0.,1.,0.));
#46877=DIRECTION('center_axis',(0.,-0.645383417803921,-0.763858785394087));
#46878=DIRECTION('ref_axis',(0.,0.763858785394087,-0.645383417803921));
#46879=DIRECTION('',(-1.,0.,0.));
#46880=DIRECTION('',(0.,0.763858785394087,-0.645383417803921));
#46881=DIRECTION('',(1.,0.,0.));
#46882=DIRECTION('',(0.,0.763858785394087,-0.645383417803921));
#46883=DIRECTION('center_axis',(1.,0.,0.));
#46884=DIRECTION('ref_axis',(0.,0.984807753012208,0.17364817766693));
#46885=DIRECTION('center_axis',(-1.,0.,0.));
#46886=DIRECTION('ref_axis',(0.,1.,0.));
#46887=DIRECTION('',(0.,0.497058334900004,0.86771712654899));
#46888=DIRECTION('center_axis',(0.,0.86771712654899,-0.497058334900004));
#46889=DIRECTION('ref_axis',(0.,0.497058334900004,0.86771712654899));
#46890=DIRECTION('',(1.,0.,0.));
#46891=DIRECTION('',(0.,0.497058334900004,0.86771712654899));
#46892=DIRECTION('center_axis',(1.,0.,0.));
#46893=DIRECTION('ref_axis',(0.,0.984807753012208,0.17364817766693));
#46894=DIRECTION('center_axis',(1.,0.,0.));
#46895=DIRECTION('ref_axis',(0.,1.,0.));
#46896=DIRECTION('center_axis',(0.,-0.768221279597376,-0.64018439966448));
#46897=DIRECTION('ref_axis',(0.,0.640184399664479,-0.768221279597376));
#46898=DIRECTION('',(-1.,0.,0.));
#46899=DIRECTION('',(0.,0.640184399664479,-0.768221279597376));
#46900=DIRECTION('',(1.,0.,0.));
#46901=DIRECTION('',(0.,0.640184399664479,-0.768221279597376));
#46902=DIRECTION('center_axis',(1.,0.,0.));
#46903=DIRECTION('ref_axis',(0.,1.,-6.12323399573677E-17));
#46904=DIRECTION('center_axis',(-1.,0.,0.));
#46905=DIRECTION('ref_axis',(0.,1.,0.));
#46906=DIRECTION('',(0.,0.640184399664479,0.768221279597376));
#46907=DIRECTION('center_axis',(0.,0.768221279597376,-0.64018439966448));
#46908=DIRECTION('ref_axis',(0.,0.640184399664479,0.768221279597376));
#46909=DIRECTION('',(1.,0.,0.));
#46910=DIRECTION('',(0.,0.640184399664479,0.768221279597376));
#46911=DIRECTION('center_axis',(1.,0.,0.));
#46912=DIRECTION('ref_axis',(0.,1.,-6.12323399573677E-17));
#46913=DIRECTION('center_axis',(1.,0.,0.));
#46914=DIRECTION('ref_axis',(0.,1.,0.));
#46915=DIRECTION('center_axis',(0.,-0.86771712654899,-0.497058334900004));
#46916=DIRECTION('ref_axis',(0.,0.497058334900004,-0.86771712654899));
#46917=DIRECTION('',(-1.,0.,0.));
#46918=DIRECTION('',(0.,0.497058334900004,-0.86771712654899));
#46919=DIRECTION('',(1.,0.,0.));
#46920=DIRECTION('',(0.,0.497058334900004,-0.86771712654899));
#46921=DIRECTION('center_axis',(1.,0.,0.));
#46922=DIRECTION('ref_axis',(0.,0.984807753012208,-0.17364817766693));
#46923=DIRECTION('center_axis',(-1.,0.,0.));
#46924=DIRECTION('ref_axis',(0.,1.,0.));
#46925=DIRECTION('',(0.,0.763858785394087,0.64538341780392));
#46926=DIRECTION('center_axis',(0.,0.645383417803921,-0.763858785394087));
#46927=DIRECTION('ref_axis',(0.,0.763858785394087,0.64538341780392));
#46928=DIRECTION('',(1.,0.,0.));
#46929=DIRECTION('',(0.,0.763858785394087,0.64538341780392));
#46930=DIRECTION('center_axis',(1.,0.,0.));
#46931=DIRECTION('ref_axis',(0.,0.984807753012208,-0.17364817766693));
#46932=DIRECTION('center_axis',(1.,0.,0.));
#46933=DIRECTION('ref_axis',(0.,1.,0.));
#46934=DIRECTION('center_axis',(0.,-0.940847827696465,-0.338829404153245));
#46935=DIRECTION('ref_axis',(0.,0.338829404153245,-0.940847827696465));
#46936=DIRECTION('',(-1.,0.,0.));
#46937=DIRECTION('',(0.,0.338829404153245,-0.940847827696465));
#46938=DIRECTION('',(1.,0.,0.));
#46939=DIRECTION('',(0.,0.338829404153245,-0.940847827696465));
#46940=DIRECTION('center_axis',(1.,0.,0.));
#46941=DIRECTION('ref_axis',(0.,0.939692620785908,-0.342020143325669));
#46942=DIRECTION('center_axis',(-1.,0.,0.));
#46943=DIRECTION('ref_axis',(0.,1.,0.));
#46944=DIRECTION('',(0.,0.864323708460692,0.50293590744026));
#46945=DIRECTION('center_axis',(0.,0.50293590744026,-0.864323708460692));
#46946=DIRECTION('ref_axis',(0.,0.864323708460692,0.50293590744026));
#46947=DIRECTION('',(1.,0.,0.));
#46948=DIRECTION('',(0.,0.864323708460692,0.50293590744026));
#46949=DIRECTION('center_axis',(1.,0.,0.));
#46950=DIRECTION('ref_axis',(0.,0.939692620785908,-0.342020143325669));
#46951=DIRECTION('center_axis',(1.,0.,0.));
#46952=DIRECTION('ref_axis',(0.,1.,0.));
#46953=DIRECTION('center_axis',(0.,-0.985391343691356,-0.170305313417241));
#46954=DIRECTION('ref_axis',(0.,0.170305313417241,-0.985391343691356));
#46955=DIRECTION('',(-1.,0.,0.));
#46956=DIRECTION('',(0.,0.170305313417241,-0.985391343691356));
#46957=DIRECTION('',(1.,0.,0.));
#46958=DIRECTION('',(0.,0.170305313417241,-0.985391343691356));
#46959=DIRECTION('center_axis',(1.,0.,0.));
#46960=DIRECTION('ref_axis',(0.,0.866025403784439,-0.5));
#46961=DIRECTION('center_axis',(-1.,0.,0.));
#46962=DIRECTION('ref_axis',(0.,1.,0.));
#46963=DIRECTION('',(0.,0.938526593014617,0.345206944026876));
#46964=DIRECTION('center_axis',(0.,0.345206944026876,-0.938526593014618));
#46965=DIRECTION('ref_axis',(0.,0.938526593014617,0.345206944026876));
#46966=DIRECTION('',(1.,0.,0.));
#46967=DIRECTION('',(0.,0.938526593014617,0.345206944026876));
#46968=DIRECTION('center_axis',(1.,0.,0.));
#46969=DIRECTION('ref_axis',(0.,0.866025403784439,-0.5));
#46970=DIRECTION('center_axis',(1.,0.,0.));
#46971=DIRECTION('ref_axis',(0.,1.,0.));
#46972=DIRECTION('center_axis',(0.,-0.999994242340264,0.00339341808829857));
#46973=DIRECTION('ref_axis',(0.,-0.00339341808829857,-0.999994242340264));
#46974=DIRECTION('',(-1.,0.,0.));
#46975=DIRECTION('',(0.,-0.00339341808829857,-0.999994242340264));
#46976=DIRECTION('',(1.,0.,0.));
#46977=DIRECTION('',(0.,-0.00339341808829857,-0.999994242340264));
#46978=DIRECTION('center_axis',(1.,0.,0.));
#46979=DIRECTION('ref_axis',(0.,0.766044443118978,-0.642787609686539));
#46980=DIRECTION('center_axis',(-1.,0.,0.));
#46981=DIRECTION('ref_axis',(0.,1.,0.));
#46982=DIRECTION('',(0.,0.984212821957166,0.176989042302378));
#46983=DIRECTION('center_axis',(0.,0.176989042302378,-0.984212821957166));
#46984=DIRECTION('ref_axis',(0.,0.984212821957166,0.176989042302378));
#46985=DIRECTION('',(1.,0.,0.));
#46986=DIRECTION('',(0.,0.984212821957166,0.176989042302378));
#46987=DIRECTION('center_axis',(1.,0.,0.));
#46988=DIRECTION('ref_axis',(0.,0.766044443118978,-0.642787609686539));
#46989=DIRECTION('center_axis',(1.,0.,0.));
#46990=DIRECTION('ref_axis',(0.,1.,0.));
#46991=DIRECTION('center_axis',(0.,-0.984212821957166,0.176989042302378));
#46992=DIRECTION('ref_axis',(0.,-0.176989042302378,-0.984212821957166));
#46993=DIRECTION('',(-1.,0.,0.));
#46994=DIRECTION('',(0.,-0.176989042302378,-0.984212821957166));
#46995=DIRECTION('',(1.,0.,0.));
#46996=DIRECTION('',(0.,-0.176989042302378,-0.984212821957166));
#46997=DIRECTION('center_axis',(1.,0.,0.));
#46998=DIRECTION('ref_axis',(0.,0.642787609686539,-0.766044443118978));
#46999=DIRECTION('center_axis',(-1.,0.,0.));
#47000=DIRECTION('ref_axis',(0.,1.,0.));
#47001=DIRECTION('',(0.,0.999994242340264,0.00339341808829846));
#47002=DIRECTION('center_axis',(0.,0.00339341808829846,-0.999994242340264));
#47003=DIRECTION('ref_axis',(0.,0.999994242340264,0.00339341808829846));
#47004=DIRECTION('',(1.,0.,0.));
#47005=DIRECTION('',(0.,0.999994242340264,0.00339341808829846));
#47006=DIRECTION('center_axis',(1.,0.,0.));
#47007=DIRECTION('ref_axis',(0.,0.642787609686539,-0.766044443118978));
#47008=DIRECTION('center_axis',(1.,0.,0.));
#47009=DIRECTION('ref_axis',(0.,1.,0.));
#47010=DIRECTION('center_axis',(0.,-0.938526593014617,0.345206944026876));
#47011=DIRECTION('ref_axis',(0.,-0.345206944026876,-0.938526593014617));
#47012=DIRECTION('',(-1.,0.,0.));
#47013=DIRECTION('',(0.,-0.345206944026876,-0.938526593014617));
#47014=DIRECTION('',(1.,0.,0.));
#47015=DIRECTION('',(0.,-0.345206944026876,-0.938526593014617));
#47016=DIRECTION('center_axis',(1.,0.,0.));
#47017=DIRECTION('ref_axis',(0.,0.5,-0.866025403784439));
#47018=DIRECTION('center_axis',(-1.,0.,0.));
#47019=DIRECTION('ref_axis',(0.,1.,0.));
#47020=DIRECTION('',(0.,0.985391343691356,-0.170305313417241));
#47021=DIRECTION('center_axis',(0.,-0.170305313417241,-0.985391343691356));
#47022=DIRECTION('ref_axis',(0.,0.985391343691356,-0.170305313417241));
#47023=DIRECTION('',(1.,0.,0.));
#47024=DIRECTION('',(0.,0.985391343691356,-0.170305313417241));
#47025=DIRECTION('center_axis',(1.,0.,0.));
#47026=DIRECTION('ref_axis',(0.,0.5,-0.866025403784439));
#47027=DIRECTION('center_axis',(1.,0.,0.));
#47028=DIRECTION('ref_axis',(0.,1.,0.));
#47029=DIRECTION('center_axis',(0.,-0.864323708460692,0.50293590744026));
#47030=DIRECTION('ref_axis',(0.,-0.50293590744026,-0.864323708460691));
#47031=DIRECTION('',(-1.,0.,0.));
#47032=DIRECTION('',(0.,-0.50293590744026,-0.864323708460691));
#47033=DIRECTION('',(1.,0.,0.));
#47034=DIRECTION('',(0.,-0.50293590744026,-0.864323708460691));
#47035=DIRECTION('center_axis',(1.,0.,0.));
#47036=DIRECTION('ref_axis',(0.,0.342020143325669,-0.939692620785908));
#47037=DIRECTION('center_axis',(-1.,0.,0.));
#47038=DIRECTION('ref_axis',(0.,1.,0.));
#47039=DIRECTION('',(0.,0.940847827696465,-0.338829404153245));
#47040=DIRECTION('center_axis',(0.,-0.338829404153245,-0.940847827696465));
#47041=DIRECTION('ref_axis',(0.,0.940847827696465,-0.338829404153245));
#47042=DIRECTION('',(1.,0.,0.));
#47043=DIRECTION('',(0.,0.940847827696465,-0.338829404153245));
#47044=DIRECTION('center_axis',(1.,0.,0.));
#47045=DIRECTION('ref_axis',(0.,0.342020143325669,-0.939692620785908));
#47046=DIRECTION('center_axis',(1.,0.,0.));
#47047=DIRECTION('ref_axis',(0.,1.,0.));
#47048=DIRECTION('center_axis',(0.,-0.763858785394087,0.645383417803921));
#47049=DIRECTION('ref_axis',(0.,-0.645383417803921,-0.763858785394087));
#47050=DIRECTION('',(-1.,0.,0.));
#47051=DIRECTION('',(0.,-0.645383417803921,-0.763858785394087));
#47052=DIRECTION('',(1.,0.,0.));
#47053=DIRECTION('',(0.,-0.645383417803921,-0.763858785394087));
#47054=DIRECTION('center_axis',(1.,0.,0.));
#47055=DIRECTION('ref_axis',(0.,0.17364817766693,-0.984807753012208));
#47056=DIRECTION('center_axis',(-1.,0.,0.));
#47057=DIRECTION('ref_axis',(0.,1.,0.));
#47058=DIRECTION('',(0.,0.86771712654899,-0.497058334900004));
#47059=DIRECTION('center_axis',(0.,-0.497058334900004,-0.86771712654899));
#47060=DIRECTION('ref_axis',(0.,0.86771712654899,-0.497058334900004));
#47061=DIRECTION('',(1.,0.,0.));
#47062=DIRECTION('',(0.,0.86771712654899,-0.497058334900004));
#47063=DIRECTION('center_axis',(1.,0.,0.));
#47064=DIRECTION('ref_axis',(0.,0.17364817766693,-0.984807753012208));
#47065=DIRECTION('center_axis',(1.,0.,0.));
#47066=DIRECTION('ref_axis',(0.,1.,0.));
#47067=DIRECTION('center_axis',(0.,-0.64018439966448,0.768221279597376));
#47068=DIRECTION('ref_axis',(0.,-0.768221279597376,-0.640184399664479));
#47069=DIRECTION('',(-1.,0.,0.));
#47070=DIRECTION('',(0.,-0.768221279597376,-0.640184399664479));
#47071=DIRECTION('',(1.,0.,0.));
#47072=DIRECTION('',(0.,-0.768221279597376,-0.640184399664479));
#47073=DIRECTION('center_axis',(1.,0.,0.));
#47074=DIRECTION('ref_axis',(0.,0.,-1.));
#47075=DIRECTION('center_axis',(-1.,0.,0.));
#47076=DIRECTION('ref_axis',(0.,1.,0.));
#47077=DIRECTION('',(0.,0.768221279597376,-0.640184399664479));
#47078=DIRECTION('center_axis',(0.,-0.64018439966448,-0.768221279597376));
#47079=DIRECTION('ref_axis',(0.,0.768221279597376,-0.640184399664479));
#47080=DIRECTION('',(1.,0.,0.));
#47081=DIRECTION('',(0.,0.768221279597376,-0.640184399664479));
#47082=DIRECTION('center_axis',(1.,0.,0.));
#47083=DIRECTION('ref_axis',(0.,0.,-1.));
#47084=DIRECTION('center_axis',(1.,0.,0.));
#47085=DIRECTION('ref_axis',(0.,1.,0.));
#47086=DIRECTION('center_axis',(1.,0.,0.));
#47087=DIRECTION('ref_axis',(0.,1.,0.));
#47088=DIRECTION('center_axis',(1.,0.,0.));
#47089=DIRECTION('ref_axis',(0.,0.,-1.));
#47090=DIRECTION('',(-1.,0.,0.));
#47091=DIRECTION('',(-1.,0.,0.));
#47092=DIRECTION('center_axis',(-1.,0.,0.));
#47093=DIRECTION('ref_axis',(0.,1.,0.));
#47094=DIRECTION('',(-0.698323852075328,-0.71578194837721,-8.76580071967607E-17));
#63093=CARTESIAN_POINT('',(0.,0.,0.));
#63094=CARTESIAN_POINT('Origin',(37.,0.,0.));
#63095=CARTESIAN_POINT('',(19.2762984310705,-6.28301010388654,0.000123638189770958));
#63096=CARTESIAN_POINT('',(19.0900381542954,-6.28269600454591,0.000102748039740536));
#63097=CARTESIAN_POINT('',(37.,-6.28269,-7.69407619853508E-16));
#63098=CARTESIAN_POINT('',(18.8656682926829,2.79354919692123,5.6277438367973));
#63099=CARTESIAN_POINT('Ctrl Pts',(19.2762984310705,-6.28301010388654,0.000123638189770958));
#63100=CARTESIAN_POINT('Ctrl Pts',(19.2719596990827,-6.28312959062582,0.134961570516868));
#63101=CARTESIAN_POINT('Ctrl Pts',(19.2676209670948,-6.27887713223786,0.269791942307153));
#63102=CARTESIAN_POINT('Ctrl Pts',(19.263282235107,-6.27020092921872,0.404337006186821));
#63103=CARTESIAN_POINT('Ctrl Pts',(19.2297589317878,-6.20316406538669,1.44390225225943));
#63104=CARTESIAN_POINT('Ctrl Pts',(19.1962356284685,-5.87203351789313,2.46643486571543));
#63105=CARTESIAN_POINT('Ctrl Pts',(19.1627123251492,-5.31695935551413,3.34796011705817));
#63106=CARTESIAN_POINT('Ctrl Pts',(19.12918902183,-4.76188519313513,4.2294853684009));
#63107=CARTESIAN_POINT('Ctrl Pts',(19.0956657185107,-3.98286741587068,4.97000325763038));
#63108=CARTESIAN_POINT('Ctrl Pts',(19.0621424151914,-3.07436035621313,5.4797127874075));
#63109=CARTESIAN_POINT('Ctrl Pts',(19.0286191118722,-2.16585329655558,5.98942231718462));
#63110=CARTESIAN_POINT('Ctrl Pts',(18.9950958085529,-1.12785695450492,6.26832348750938));
#63111=CARTESIAN_POINT('Ctrl Pts',(18.9615725052336,-0.0862303633136496,
6.28262611703396));
#63112=CARTESIAN_POINT('Ctrl Pts',(18.9296044343834,0.907072484844297,6.29626521070058));
#63113=CARTESIAN_POINT('Ctrl Pts',(18.8976363635331,1.90367656219001,6.06928709268379));
#63114=CARTESIAN_POINT('Ctrl Pts',(18.8656682926829,2.79368235183436,5.62796419942306));
#63115=CARTESIAN_POINT('',(18.8656682926829,-2.79341604200804,5.62752347417158));
#63116=CARTESIAN_POINT('Origin',(18.8656682926829,0.,0.));
#63117=CARTESIAN_POINT('Ctrl Pts',(18.8656682926829,-2.79341604200804,5.62752347417158));
#63118=CARTESIAN_POINT('Ctrl Pts',(18.8991915960022,-3.72675688127093,5.16422744617198));
#63119=CARTESIAN_POINT('Ctrl Pts',(18.9327148993215,-4.54215990698344,4.46450958611088));
#63120=CARTESIAN_POINT('Ctrl Pts',(18.9662382026407,-5.14104950209353,3.61230023328826));
#63121=CARTESIAN_POINT('Ctrl Pts',(18.99976150596,-5.73993909720363,2.76009088046562));
#63122=CARTESIAN_POINT('Ctrl Pts',(19.0332848092793,-6.12231526171131,1.75539003488145));
#63123=CARTESIAN_POINT('Ctrl Pts',(19.0668081125985,-6.24177993240548,0.720486511882419));
#63124=CARTESIAN_POINT('Ctrl Pts',(19.0745514598308,-6.26937436181975,0.481440339905098));
#63125=CARTESIAN_POINT('Ctrl Pts',(19.0822948070631,-6.28294151243645,0.240782745884617));
#63126=CARTESIAN_POINT('Ctrl Pts',(19.0900381542954,-6.28269600454591,0.000102748039740536));
#63127=CARTESIAN_POINT('Origin',(37.,0.,0.));
#63128=CARTESIAN_POINT('',(20.5462984310705,-6.28265148386535,-0.000161171021448303));
#63129=CARTESIAN_POINT('',(20.3600381542954,-6.28297657866995,-0.000130087838368273));
#63130=CARTESIAN_POINT('',(37.,-6.28269,-7.69407619853508E-16));
#63131=CARTESIAN_POINT('Ctrl Pts',(20.5462984310705,-6.28265148386535,-0.000161171021448303));
#63132=CARTESIAN_POINT('Ctrl Pts',(20.5209060055805,-6.28185518498536,0.789107786007277));
#63133=CARTESIAN_POINT('Ctrl Pts',(20.4955135800906,-6.13264436299944,1.57866931564015));
#63134=CARTESIAN_POINT('Ctrl Pts',(20.4701211546007,-5.84225412088425,2.3123523170549));
#63135=CARTESIAN_POINT('Ctrl Pts',(20.4365978512814,-5.45887837085035,3.28096706425059));
#63136=CARTESIAN_POINT('Ctrl Pts',(20.4030745479621,-4.82943377431738,4.15218826095493));
#63137=CARTESIAN_POINT('Ctrl Pts',(20.3695512446428,-4.03024021789354,4.82038071424489));
#63138=CARTESIAN_POINT('Ctrl Pts',(20.3360279413236,-3.2310466614697,5.48857316753485));
#63139=CARTESIAN_POINT('Ctrl Pts',(20.3025046380043,-2.26210414515502,5.95373687741044));
#63140=CARTESIAN_POINT('Ctrl Pts',(20.2689813346851,-1.24089653161339,6.1594709399743));
#63141=CARTESIAN_POINT('Ctrl Pts',(20.2354580313658,-0.219688918071764,
6.36520500253816));
#63142=CARTESIAN_POINT('Ctrl Pts',(20.2019347280465,0.853783792696783,6.31150941779028));
#63143=CARTESIAN_POINT('Ctrl Pts',(20.1684114247272,1.84936349578162,6.00489476066125));
#63144=CARTESIAN_POINT('Ctrl Pts',(20.134888121408,2.84494319886647,5.69828010353222));
#63145=CARTESIAN_POINT('Ctrl Pts',(20.1013648180887,3.76262989426761,5.13874637402203));
#63146=CARTESIAN_POINT('Ctrl Pts',(20.0678415147694,4.49115446665603,4.39413677958182));
#63147=CARTESIAN_POINT('Ctrl Pts',(20.0343182114502,5.21967903904446,3.64952718514161));
#63148=CARTESIAN_POINT('Ctrl Pts',(20.0007949081309,5.75904148842017,2.71984172577137));
#63149=CARTESIAN_POINT('Ctrl Pts',(19.9672716048117,6.04384434700476,1.71780439540296));
#63150=CARTESIAN_POINT('Ctrl Pts',(19.9337483014924,6.32864720558935,0.715767065034549));
#63151=CARTESIAN_POINT('Ctrl Pts',(19.9002249981731,6.35889047338282,-0.358622136332033));
#63152=CARTESIAN_POINT('Ctrl Pts',(19.8667016948538,6.13090717293739,-1.37509404334423));
#63153=CARTESIAN_POINT('Ctrl Pts',(19.8331783915346,5.90292387249196,-2.39156595035644));
#63154=CARTESIAN_POINT('Ctrl Pts',(19.7996550882153,5.41671400380763,-3.35012056301426));
#63155=CARTESIAN_POINT('Ctrl Pts',(19.766131784896,4.73123029292878,-4.13453342405899));
#63156=CARTESIAN_POINT('Ctrl Pts',(19.7326084815768,4.04574658204992,-4.91894628510371));
#63157=CARTESIAN_POINT('Ctrl Pts',(19.6990851782575,3.16098902897655,-5.52921739453534));
#63158=CARTESIAN_POINT('Ctrl Pts',(19.6655618749382,2.18423412824459,-5.89135188379759));
#63159=CARTESIAN_POINT('Ctrl Pts',(19.632038571619,1.20747922751265,-6.25348637305983));
#63160=CARTESIAN_POINT('Ctrl Pts',(19.5985152682997,0.138726979122119,-6.36748424215271));
#63161=CARTESIAN_POINT('Ctrl Pts',(19.5649919649804,-0.892436909941828,
-6.21952282731311));
#63162=CARTESIAN_POINT('Ctrl Pts',(19.5314686616612,-1.92360079900578,-6.07156141247351));
#63163=CARTESIAN_POINT('Ctrl Pts',(19.4979453583419,-2.91717632874314,-5.66164071370144));
#63164=CARTESIAN_POINT('Ctrl Pts',(19.4644220550226,-3.75269280943037,-5.03946436137122));
#63165=CARTESIAN_POINT('Ctrl Pts',(19.4308987517034,-4.5882092901176,-4.417288009041));
#63166=CARTESIAN_POINT('Ctrl Pts',(19.3973754483841,-5.26566672175468,-3.58285600315263));
#63167=CARTESIAN_POINT('Ctrl Pts',(19.3638521450648,-5.70292384748797,-2.63734106086383));
#63168=CARTESIAN_POINT('Ctrl Pts',(19.3346675737334,-6.08358925073353,-1.81419878233041));
#63169=CARTESIAN_POINT('Ctrl Pts',(19.3054830024019,-6.28220637383928,-0.906866529731437));
#63170=CARTESIAN_POINT('Ctrl Pts',(19.2762984310705,-6.28301010388654,0.000123638189770958));
#63171=CARTESIAN_POINT('Ctrl Pts',(19.0900381542954,-6.28269600454591,0.000102748039740536));
#63172=CARTESIAN_POINT('Ctrl Pts',(19.1158181103824,-6.2818786341701,-0.801194105803656));
#63173=CARTESIAN_POINT('Ctrl Pts',(19.1415980664694,-6.12795810464849,-1.60273928956053));
#63174=CARTESIAN_POINT('Ctrl Pts',(19.1673780225563,-5.82885452380126,-2.34589344717355));
#63175=CARTESIAN_POINT('Ctrl Pts',(19.2009013258756,-5.4399112676222,-3.31226368281658));
#63176=CARTESIAN_POINT('Ctrl Pts',(19.2344246291949,-4.80547157838342,-4.17989795368874));
#63177=CARTESIAN_POINT('Ctrl Pts',(19.2679479325141,-4.00244931177914,-4.84349431763947));
#63178=CARTESIAN_POINT('Ctrl Pts',(19.3014712358334,-3.19942704517486,-5.50709068159019));
#63179=CARTESIAN_POINT('Ctrl Pts',(19.3349945391527,-2.22782220120508,-5.96664913861948));
#63180=CARTESIAN_POINT('Ctrl Pts',(19.3685178424719,-1.20544745056172,-6.16650007909134));
#63181=CARTESIAN_POINT('Ctrl Pts',(19.4020411457912,-0.183072699918368,
-6.3663510195632));
#63182=CARTESIAN_POINT('Ctrl Pts',(19.4355644491105,0.890071957398561,-6.30649444347763));
#63183=CARTESIAN_POINT('Ctrl Pts',(19.4690877524297,1.88387126298836,-5.99416156852824));
#63184=CARTESIAN_POINT('Ctrl Pts',(19.502611055749,2.87767056857816,-5.68182869357886));
#63185=CARTESIAN_POINT('Ctrl Pts',(19.5361343590683,3.79212452244082,-5.11701951976566));
#63186=CARTESIAN_POINT('Ctrl Pts',(19.5696576623875,4.516354407704,-4.36823038555468));
#63187=CARTESIAN_POINT('Ctrl Pts',(19.6031809657068,5.24058429296718,-3.61944125134371));
#63188=CARTESIAN_POINT('Ctrl Pts',(19.6367042690261,5.77459010963087,-2.68667215673497));
#63189=CARTESIAN_POINT('Ctrl Pts',(19.6702275723453,6.05362468373747,-1.68301407119577));
#63190=CARTESIAN_POINT('Ctrl Pts',(19.7037508756646,6.33265925784406,-0.67935598565657));
#63191=CARTESIAN_POINT('Ctrl Pts',(19.7372741789839,6.35672258939355,0.395191090813077));
#63192=CARTESIAN_POINT('Ctrl Pts',(19.7707974823031,6.12289660028605,1.41033527152274));
#63193=CARTESIAN_POINT('Ctrl Pts',(19.8043207856224,5.88907061117856,2.4254794522324));
#63194=CARTESIAN_POINT('Ctrl Pts',(19.8378440889417,5.39735530141408,3.38122073718207));
#63195=CARTESIAN_POINT('Ctrl Pts',(19.8713673922609,4.70737114989471,4.16167770349345));
#63196=CARTESIAN_POINT('Ctrl Pts',(19.9048906955802,4.01738699837534,4.94213466980482));
#63197=CARTESIAN_POINT('Ctrl Pts',(19.9384139988995,3.12913400510108,5.5473073174779));
#63198=CARTESIAN_POINT('Ctrl Pts',(19.9719373022187,2.15031235628287,5.90381780552069));
#63199=CARTESIAN_POINT('Ctrl Pts',(20.005460605538,1.17149070746465,6.26032829356348));
#63200=CARTESIAN_POINT('Ctrl Pts',(20.0389839088573,0.10210040310249,6.36817662197599));
#63201=CARTESIAN_POINT('Ctrl Pts',(20.0725072121765,-0.928195388057467,
6.21428669637018));
#63202=CARTESIAN_POINT('Ctrl Pts',(20.1060305154958,-1.95849117921742,6.06039677076437));
#63203=CARTESIAN_POINT('Ctrl Pts',(20.1395538188151,-2.94969245717518,5.64476859114024));
#63204=CARTESIAN_POINT('Ctrl Pts',(20.1730771221343,-3.78161652151487,5.01779665574661));
#63205=CARTESIAN_POINT('Ctrl Pts',(20.2066004254536,-4.61354058585457,4.39082472035299));
#63206=CARTESIAN_POINT('Ctrl Pts',(20.2401237287729,-5.2861874365762,3.55250902918988));
#63207=CARTESIAN_POINT('Ctrl Pts',(20.2736470320921,-5.71799891828659,2.604495121429));
#63208=CARTESIAN_POINT('Ctrl Pts',(20.3024440728266,-6.08893172016407,1.79013637943426));
#63209=CARTESIAN_POINT('Ctrl Pts',(20.331241113561,-6.28215022177013,0.894830466416716));
#63210=CARTESIAN_POINT('Ctrl Pts',(20.3600381542954,-6.28297657866995,-0.000130087838368273));
#63211=CARTESIAN_POINT('Origin',(37.,0.,0.));
#63212=CARTESIAN_POINT('',(21.8162984310705,-6.28226794133467,0.000102037604138849));
#63213=CARTESIAN_POINT('',(21.6300381542954,-6.28215947560979,1.245194739236E-5));
#63214=CARTESIAN_POINT('',(37.,-6.28269,-7.69407619853508E-16));
#63215=CARTESIAN_POINT('Ctrl Pts',(21.8162984310705,-6.28226794133467,0.000102037604138849));
#63216=CARTESIAN_POINT('Ctrl Pts',(21.8033756153977,-6.28250126256899,0.401850367395142));
#63217=CARTESIAN_POINT('Ctrl Pts',(21.7904527997249,-6.24455488198961,0.803555180733288));
#63218=CARTESIAN_POINT('Ctrl Pts',(21.7775299840521,-6.16800368420105,1.19776333277082));
#63219=CARTESIAN_POINT('Ctrl Pts',(21.7440066807328,-5.96942087625138,2.22038563013157));
#63220=CARTESIAN_POINT('Ctrl Pts',(21.7104833774135,-5.51104903483399,3.19255954995002));
#63221=CARTESIAN_POINT('Ctrl Pts',(21.6769600740943,-4.8484655484309,3.99640942288543));
#63222=CARTESIAN_POINT('Ctrl Pts',(21.643436770775,-4.18588206202782,4.80025929582083));
#63223=CARTESIAN_POINT('Ctrl Pts',(21.6099134674557,-3.31908693063903,5.4357851218732));
#63224=CARTESIAN_POINT('Ctrl Pts',(21.5763901641365,-2.35317869086444,5.82592966817379));
#63225=CARTESIAN_POINT('Ctrl Pts',(21.5428668608172,-1.38727045108985,6.21607421447439));
#63226=CARTESIAN_POINT('Ctrl Pts',(21.5093435574979,-0.322249102929453,
6.36083748102322));
#63227=CARTESIAN_POINT('Ctrl Pts',(21.4758202541787,0.712751973552881,6.24266698405807));
#63228=CARTESIAN_POINT('Ctrl Pts',(21.4422969508594,1.74775305003522,6.12449648709291));
#63229=CARTESIAN_POINT('Ctrl Pts',(21.4087736475401,2.75273385483948,5.74339222661377));
#63230=CARTESIAN_POINT('Ctrl Pts',(21.3752503442209,3.60584089794109,5.14556293017366));
#63231=CARTESIAN_POINT('Ctrl Pts',(21.3417270409016,4.4589479410427,4.54773363373354));
#63232=CARTESIAN_POINT('Ctrl Pts',(21.3082037375823,5.16018122244165,3.73317930133244));
#63233=CARTESIAN_POINT('Ctrl Pts',(21.2746804342631,5.62451650858963,2.80066429517295));
#63234=CARTESIAN_POINT('Ctrl Pts',(21.2411571309438,6.0888517947376,1.86814928901346));
#63235=CARTESIAN_POINT('Ctrl Pts',(21.2076338276245,6.31628908563461,0.817673609095557));
#63236=CARTESIAN_POINT('Ctrl Pts',(21.1741105243053,6.27925170765075,-0.223393020520311));
#63237=CARTESIAN_POINT('Ctrl Pts',(21.140587220986,6.24221432966688,-1.26445965013619));
#63238=CARTESIAN_POINT('Ctrl Pts',(21.1070639176667,5.94070228280213,-2.29611722945003));
#63239=CARTESIAN_POINT('Ctrl Pts',(21.0735406143475,5.41127377296556,-3.1932777210302));
#63240=CARTESIAN_POINT('Ctrl Pts',(21.0400173110282,4.881845263129,-4.09043821261036));
#63241=CARTESIAN_POINT('Ctrl Pts',(21.0064940077089,4.12450029032062,-4.85310161645685));
#63242=CARTESIAN_POINT('Ctrl Pts',(20.9729707043897,3.23106660651773,-5.38879532307552));
#63243=CARTESIAN_POINT('Ctrl Pts',(20.9394474010704,2.33763292271485,-5.92448902969418));
#63244=CARTESIAN_POINT('Ctrl Pts',(20.9059240977511,1.30811052791746,-6.23321303908502));
#63245=CARTESIAN_POINT('Ctrl Pts',(20.8724007944319,0.267328569380539,-6.27753469806501));
#63246=CARTESIAN_POINT('Ctrl Pts',(20.8388774911126,-0.773453389156391,
-6.32185635704499));
#63247=CARTESIAN_POINT('Ctrl Pts',(20.8053541877933,-1.82549491143286,-6.10177566561411));
#63248=CARTESIAN_POINT('Ctrl Pts',(20.771830884474,-2.76123641570027,-5.64397731273306));
#63249=CARTESIAN_POINT('Ctrl Pts',(20.7383075811548,-3.69697791996767,-5.186178959852));
#63250=CARTESIAN_POINT('Ctrl Pts',(20.7047842778355,-4.51641940622602,-4.49066294552077));
#63251=CARTESIAN_POINT('Ctrl Pts',(20.6712609745163,-5.1202039469391,-3.64176028740937));
#63252=CARTESIAN_POINT('Ctrl Pts',(20.637737671197,-5.72398848765219,-2.79285762929797));
#63253=CARTESIAN_POINT('Ctrl Pts',(20.6042143678777,-6.11211608282,-1.7905683274064));
#63254=CARTESIAN_POINT('Ctrl Pts',(20.5706910645585,-6.23752642863648,-0.756419527617094));
#63255=CARTESIAN_POINT('Ctrl Pts',(20.5625601867291,-6.26794396209543,-0.505592887164689));
#63256=CARTESIAN_POINT('Ctrl Pts',(20.5544293088998,-6.28290646576581,-0.252892028364329));
#63257=CARTESIAN_POINT('Ctrl Pts',(20.5462984310705,-6.28265148386535,-0.000161171021448303));
#63258=CARTESIAN_POINT('Ctrl Pts',(20.3600381542954,-6.28297657866995,-0.000130087838368273));
#63259=CARTESIAN_POINT('Ctrl Pts',(20.3647644168803,-6.28311220301182,-0.147013881263527));
#63260=CARTESIAN_POINT('Ctrl Pts',(20.3694906794651,-6.27806547058088,-0.293888371957929));
#63261=CARTESIAN_POINT('Ctrl Pts',(20.3742169420499,-6.26777149220422,-0.440394174383335));
#63262=CARTESIAN_POINT('Ctrl Pts',(20.4077402453692,-6.19475647171228,-1.47955743807614));
#63263=CARTESIAN_POINT('Ctrl Pts',(20.4412635486885,-5.85775031802924,-2.50017184110311));
#63264=CARTESIAN_POINT('Ctrl Pts',(20.4747868520078,-5.29761487851413,-3.37848829441954));
#63265=CARTESIAN_POINT('Ctrl Pts',(20.508310155327,-4.73747943899902,-4.25680474773598));
#63266=CARTESIAN_POINT('Ctrl Pts',(20.5418334586463,-3.95421471365185,-4.99282325134187));
#63267=CARTESIAN_POINT('Ctrl Pts',(20.5753567619656,-3.04279121519469,-5.49730189480007));
#63268=CARTESIAN_POINT('Ctrl Pts',(20.6088800652848,-2.13136771673754,-6.00178053825826));
#63269=CARTESIAN_POINT('Ctrl Pts',(20.6424033686041,-1.0917854451704,-6.27471932156876));
#63270=CARTESIAN_POINT('Ctrl Pts',(20.6759266719233,-0.050093302497819,
-6.28302452638716));
#63271=CARTESIAN_POINT('Ctrl Pts',(20.7094499752426,0.991598840174758,-6.29132973120555));
#63272=CARTESIAN_POINT('Ctrl Pts',(20.7429732785619,2.03540085395279,-6.03500135753185));
#63273=CARTESIAN_POINT('Ctrl Pts',(20.7764965818812,2.95475219343646,-5.54511911461026));
#63274=CARTESIAN_POINT('Ctrl Pts',(20.8100198852004,3.87410353292014,-5.05523687168867));
#63275=CARTESIAN_POINT('Ctrl Pts',(20.8435431885197,4.66900419810947,-4.33180075951921));
#63276=CARTESIAN_POINT('Ctrl Pts',(20.8770664918389,5.2430728257406,-3.46252709314663));
#63277=CARTESIAN_POINT('Ctrl Pts',(20.9105897951582,5.81714145337173,-2.59325342677405));
#63278=CARTESIAN_POINT('Ctrl Pts',(20.9441130984775,6.17037804344467,-1.57814220619837));
#63279=CARTESIAN_POINT('Ctrl Pts',(20.9776364017968,6.25995281132153,-0.54027523110904));
#63280=CARTESIAN_POINT('Ctrl Pts',(21.011159705116,6.34952757919838,0.497591743980281));
#63281=CARTESIAN_POINT('Ctrl Pts',(21.0446830084353,6.17544052487916,1.55821447358325));
#63282=CARTESIAN_POINT('Ctrl Pts',(21.0782063117546,5.75879962883674,2.51299290881145));
#63283=CARTESIAN_POINT('Ctrl Pts',(21.1117296150738,5.3421587327943,3.46777134403967));
#63284=CARTESIAN_POINT('Ctrl Pts',(21.1452529183931,4.68296399502866,4.31670548489312));
#63285=CARTESIAN_POINT('Ctrl Pts',(21.1787762217123,3.86114249373319,4.95686243189617));
#63286=CARTESIAN_POINT('Ctrl Pts',(21.2122995250316,3.03932099243774,5.59701937889922));
#63287=CARTESIAN_POINT('Ctrl Pts',(21.2458228283509,2.05487272761245,6.02839913205186));
#63288=CARTESIAN_POINT('Ctrl Pts',(21.2793461316702,1.02716162766404,6.19869708210485));
#63289=CARTESIAN_POINT('Ctrl Pts',(21.3128694349894,-0.000549472284362418,
6.36899503215785));
#63290=CARTESIAN_POINT('Ctrl Pts',(21.3463927383087,-1.07152340735589,6.27821117911118));
#63291=CARTESIAN_POINT('Ctrl Pts',(21.379916041628,-2.05590504889449,5.93735302599625));
#63292=CARTESIAN_POINT('Ctrl Pts',(21.4134393449472,-3.04028669043309,5.59649487288131));
#63293=CARTESIAN_POINT('Ctrl Pts',(21.4469626482665,-3.93807603843877,5.00556241969809));
#63294=CARTESIAN_POINT('Ctrl Pts',(21.4804859515858,-4.64041652088273,4.23620597208803));
#63295=CARTESIAN_POINT('Ctrl Pts',(21.514009254905,-5.34275700332668,3.46684952447795));
#63296=CARTESIAN_POINT('Ctrl Pts',(21.5475325582243,-5.84964862020891,2.51906908244102));
#63297=CARTESIAN_POINT('Ctrl Pts',(21.5810558615436,-6.09963098115819,1.50778261661611));
#63298=CARTESIAN_POINT('Ctrl Pts',(21.5973832924608,-6.22138418936879,1.01523837802827));
#63299=CARTESIAN_POINT('Ctrl Pts',(21.6137107233781,-6.28219467558877,0.507629559776358));
#63300=CARTESIAN_POINT('Ctrl Pts',(21.6300381542954,-6.28215947560979,1.245194739236E-5));
#63301=CARTESIAN_POINT('Origin',(37.,0.,0.));
#63302=CARTESIAN_POINT('',(23.0862984310705,-6.28322123118156,1.47945420200454E-5));
#63303=CARTESIAN_POINT('',(22.9000381542954,-6.2830493926505,0.000112281392144475));
#63304=CARTESIAN_POINT('',(37.,-6.28269,-7.69407619853508E-16));
#63305=CARTESIAN_POINT('Ctrl Pts',(23.0862984310705,-6.28322123118156,1.47945420200454E-5));
#63306=CARTESIAN_POINT('Ctrl Pts',(23.0858452252148,-6.28322315649896,0.0140980318367827));
#63307=CARTESIAN_POINT('Ctrl Pts',(23.0853920193592,-6.28317679231295,0.0281812564013002));
#63308=CARTESIAN_POINT('Ctrl Pts',(23.0849388135035,-6.2830820614407,0.042264155619573));
#63309=CARTESIAN_POINT('Ctrl Pts',(23.0514155101842,-6.27607488859701,1.08396583758096));
#63310=CARTESIAN_POINT('Ctrl Pts',(23.0178922068649,-6.00443171689342,2.12388740320311));
#63311=CARTESIAN_POINT('Ctrl Pts',(22.9843689035457,-5.50108916397988,3.03593881025149));
#63312=CARTESIAN_POINT('Ctrl Pts',(22.9508456002264,-4.99774661106633,3.94799021729987));
#63313=CARTESIAN_POINT('Ctrl Pts',(22.9173222969072,-4.26270467694284,4.73217146577448));
#63314=CARTESIAN_POINT('Ctrl Pts',(22.8837989935879,-3.38508687974927,5.29340091682063));
#63315=CARTESIAN_POINT('Ctrl Pts',(22.8502756902686,-2.5074690825557,5.85463036786677));
#63316=CARTESIAN_POINT('Ctrl Pts',(22.8167523869493,-1.48727542229206,6.19290802148445));
#63317=CARTESIAN_POINT('Ctrl Pts',(22.7832290836301,-0.448203941159331,
6.26721785777208));
#63318=CARTESIAN_POINT('Ctrl Pts',(22.7497057803108,0.590867539973411,6.34152769405972));
#63319=CARTESIAN_POINT('Ctrl Pts',(22.7161824769916,1.64881684197523,6.15186971301729));
#63320=CARTESIAN_POINT('Ctrl Pts',(22.6826591736723,2.59736806733497,5.72123986321468));
#63321=CARTESIAN_POINT('Ctrl Pts',(22.649135870353,3.54591929269469,5.29061001341208));
#63322=CARTESIAN_POINT('Ctrl Pts',(22.6156125670338,4.38507244141232,4.61900829484931));
#63323=CARTESIAN_POINT('Ctrl Pts',(22.5820892637145,5.01308055538941,3.7878661268351));
#63324=CARTESIAN_POINT('Ctrl Pts',(22.5485659603952,5.64108866936651,2.95672395882087));
#63325=CARTESIAN_POINT('Ctrl Pts',(22.515042657076,6.05795174860305,1.96604134135519));
#63326=CARTESIAN_POINT('Ctrl Pts',(22.4815193537567,6.21312532416547,0.935938115401774));
#63327=CARTESIAN_POINT('Ctrl Pts',(22.4479960504374,6.36829889972788,-0.0941651105516532));
#63328=CARTESIAN_POINT('Ctrl Pts',(22.4144727471182,6.26178297161615,-1.16368894499283));
#63329=CARTESIAN_POINT('Ctrl Pts',(22.3809494437989,5.90649255026785,-2.14295408333414));
#63330=CARTESIAN_POINT('Ctrl Pts',(22.3474261404796,5.55120212891955,-3.12221922167544));
#63331=CARTESIAN_POINT('Ctrl Pts',(22.3139028371603,4.94713721433467,-4.0112256639169));
#63332=CARTESIAN_POINT('Ctrl Pts',(22.2803795338411,4.16754041740843,-4.70218176157783));
#63333=CARTESIAN_POINT('Ctrl Pts',(22.2468562305218,3.3879436204822,-5.39313785923877));
#63334=CARTESIAN_POINT('Ctrl Pts',(22.2133329272025,2.43281494121461,-5.88604361231919));
#63335=CARTESIAN_POINT('Ctrl Pts',(22.1798096238833,1.41796332086578,-6.1211344104118));
#63336=CARTESIAN_POINT('Ctrl Pts',(22.146286320564,0.403111700516944,-6.35622520850441));
#63337=CARTESIAN_POINT('Ctrl Pts',(22.1127630172448,-0.671462860913124,
-6.33350105160919));
#63338=CARTESIAN_POINT('Ctrl Pts',(22.0792397139255,-1.67546866036334,-6.05571723396893));
#63339=CARTESIAN_POINT('Ctrl Pts',(22.0457164106062,-2.67947445981354,-5.77793341632867));
#63340=CARTESIAN_POINT('Ctrl Pts',(22.0121931072869,-3.61291149728388,-5.24508993794336));
#63341=CARTESIAN_POINT('Ctrl Pts',(21.9786698039677,-4.36260093374578,-4.5217938412237));
#63342=CARTESIAN_POINT('Ctrl Pts',(21.9451465006484,-5.11229037020769,-3.79849774450404));
#63343=CARTESIAN_POINT('Ctrl Pts',(21.9116231973291,-5.67823220566115,-2.88474902945002));
#63344=CARTESIAN_POINT('Ctrl Pts',(21.8780998940099,-5.99180623614691,-1.89133933447148));
#63345=CARTESIAN_POINT('Ctrl Pts',(21.8574994063634,-6.18450138554061,-1.28087669735034));
#63346=CARTESIAN_POINT('Ctrl Pts',(21.8368989187169,-6.28189599985327,-0.640332037631833));
#63347=CARTESIAN_POINT('Ctrl Pts',(21.8162984310705,-6.28226794133467,0.000102037604138849));
#63348=CARTESIAN_POINT('Ctrl Pts',(21.6300381542954,-6.28215947560979,1.245194739236E-5));
#63349=CARTESIAN_POINT('Ctrl Pts',(21.6472340266974,-6.28212240337534,-0.534604356999154));
#63350=CARTESIAN_POINT('Ctrl Pts',(21.6644298990994,-6.21459485201875,-1.06923036080506));
#63351=CARTESIAN_POINT('Ctrl Pts',(21.6816257715014,-6.07969017924126,-1.58627672545295));
#63352=CARTESIAN_POINT('Ctrl Pts',(21.7151490748206,-5.81669391135876,-2.59425711208423));
#63353=CARTESIAN_POINT('Ctrl Pts',(21.7486723781399,-5.29762827057744,-3.5354253957339));
#63354=CARTESIAN_POINT('Ctrl Pts',(21.7821956814592,-4.58542974242937,-4.29566532710693));
#63355=CARTESIAN_POINT('Ctrl Pts',(21.8157189847784,-3.87323121428129,-5.05590525847996));
#63356=CARTESIAN_POINT('Ctrl Pts',(21.8492422880977,-2.96789979876645,-5.63521683757636));
#63357=CARTESIAN_POINT('Ctrl Pts',(21.882765591417,-1.97920654034809,-5.96335878477205));
#63358=CARTESIAN_POINT('Ctrl Pts',(21.9162888947362,-0.990513281929732,
-6.29150073196775));
#63359=CARTESIAN_POINT('Ctrl Pts',(21.9498121980555,0.0815418193921472,
-6.36847304726274));
#63360=CARTESIAN_POINT('Ctrl Pts',(21.9833355013748,1.10697254401,-6.18494287055884));
#63361=CARTESIAN_POINT('Ctrl Pts',(22.016858804694,2.13240326862785,-6.00141269385496));
#63362=CARTESIAN_POINT('Ctrl Pts',(22.0503821080133,3.11120961654167,-5.55738002515219));
#63363=CARTESIAN_POINT('Ctrl Pts',(22.0839054113326,3.92471173935929,-4.90668363441203));
#63364=CARTESIAN_POINT('Ctrl Pts',(22.1174287146519,4.73821386217691,-4.25598724367186));
#63365=CARTESIAN_POINT('Ctrl Pts',(22.1509520179711,5.38641175989832,-3.39862713089432));
#63366=CARTESIAN_POINT('Ctrl Pts',(22.1844753212904,5.79071171641843,-2.43855784073391));
#63367=CARTESIAN_POINT('Ctrl Pts',(22.2179986246096,6.19501167293854,-1.47848855057352));
#63368=CARTESIAN_POINT('Ctrl Pts',(22.2515219279289,6.35541368825735,-0.415710083030268));
#63369=CARTESIAN_POINT('Ctrl Pts',(22.2850452312482,6.25246908705679,0.620916130141472));
#63370=CARTESIAN_POINT('Ctrl Pts',(22.3185685345674,6.14952448585624,1.65754234331321));
#63371=CARTESIAN_POINT('Ctrl Pts',(22.3520918378867,5.78323326813632,2.66801630211346));
#63372=CARTESIAN_POINT('Ctrl Pts',(22.385615141206,5.19800808638858,3.52981847396006));
#63373=CARTESIAN_POINT('Ctrl Pts',(22.4191384445253,4.61278290464085,4.39162064580665));
#63374=CARTESIAN_POINT('Ctrl Pts',(22.4526617478445,3.80862375886531,5.10475103069959));
#63375=CARTESIAN_POINT('Ctrl Pts',(22.4861850511638,2.8830345993656,5.58274287641222));
#63376=CARTESIAN_POINT('Ctrl Pts',(22.519708354483,1.95744543986588,6.06073472212486));
#63377=CARTESIAN_POINT('Ctrl Pts',(22.5532316578023,0.910426266642013,6.30358802865718));
#63378=CARTESIAN_POINT('Ctrl Pts',(22.5867549611216,-0.131072296204699,
6.28185693711966));
#63379=CARTESIAN_POINT('Ctrl Pts',(22.6202782644409,-1.17257085905141,6.26012584558213));
#63380=CARTESIAN_POINT('Ctrl Pts',(22.6538015677601,-2.20854881152097,5.97381035597475));
#63381=CARTESIAN_POINT('Ctrl Pts',(22.6873248710794,-3.11339427277617,5.45762609817814));
#63382=CARTESIAN_POINT('Ctrl Pts',(22.7208481743987,-4.01823973403137,4.94144184038154));
#63383=CARTESIAN_POINT('Ctrl Pts',(22.7543714777179,-4.79195270407223,4.19538881439572));
#63384=CARTESIAN_POINT('Ctrl Pts',(22.7878947810372,-5.34072081829846,3.30992562850951));
#63385=CARTESIAN_POINT('Ctrl Pts',(22.8214180843564,-5.8894889325247,2.42446244262331));
#63386=CARTESIAN_POINT('Ctrl Pts',(22.8549413876757,-6.2133121909363,1.39958909683672));
#63387=CARTESIAN_POINT('Ctrl Pts',(22.888464690995,-6.27292716282903,0.359571043206212));
#63388=CARTESIAN_POINT('Ctrl Pts',(22.8923225120951,-6.27978758151336,0.239887026580249));
#63389=CARTESIAN_POINT('Ctrl Pts',(22.8961803331953,-6.28314905621492,0.120002446659774));
#63390=CARTESIAN_POINT('Ctrl Pts',(22.9000381542954,-6.2830493926505,0.000112281392144475));
#63391=CARTESIAN_POINT('Origin',(37.,0.,0.));
#63392=CARTESIAN_POINT('',(24.3562984310705,-6.28232352063531,-0.000120941246437023));
#63393=CARTESIAN_POINT('',(24.1700381542954,-6.28260548706583,-0.00016035527560624));
#63394=CARTESIAN_POINT('',(37.,-6.28269,-7.69407619853508E-16));
#63395=CARTESIAN_POINT('Ctrl Pts',(24.3562984310705,-6.28232352063531,-0.000120941246437023));
#63396=CARTESIAN_POINT('Ctrl Pts',(24.3347915317127,-6.28185779185402,0.668474984502739));
#63397=CARTESIAN_POINT('Ctrl Pts',(24.3132846323549,-6.17554954378264,1.33721551995562));
#63398=CARTESIAN_POINT('Ctrl Pts',(24.2917777329971,-5.96582038543131,1.9717742209544));
#63399=CARTESIAN_POINT('Ctrl Pts',(24.2582544296778,-5.6389106773723,2.96087559970648));
#63400=CARTESIAN_POINT('Ctrl Pts',(24.2247311263586,-5.06072765769983,3.86692817607369));
#63401=CARTESIAN_POINT('Ctrl Pts',(24.1912078230393,-4.30137576869091,4.58007346514953));
#63402=CARTESIAN_POINT('Ctrl Pts',(24.1576845197201,-3.54202387968198,5.29321875422537));
#63403=CARTESIAN_POINT('Ctrl Pts',(24.1241612164008,-2.60150312133661,5.81345675600984));
#63404=CARTESIAN_POINT('Ctrl Pts',(24.0906379130815,-1.59385123079055,6.07770883670447));
#63405=CARTESIAN_POINT('Ctrl Pts',(24.0571146097623,-0.586199340244509,
6.34196091739909));
#63406=CARTESIAN_POINT('Ctrl Pts',(24.023591306443,0.48858368250222,6.35022707700387));
#63407=CARTESIAN_POINT('Ctrl Pts',(23.9900680031237,1.50018085854362,6.10150504722461));
#63408=CARTESIAN_POINT('Ctrl Pts',(23.9565446998044,2.51177803458502,5.85278301744535));
#63409=CARTESIAN_POINT('Ctrl Pts',(23.9230213964852,3.46018936392109,5.34707279828205));
#63410=CARTESIAN_POINT('Ctrl Pts',(23.8894980931659,4.23042038107967,4.64569153614333));
#63411=CARTESIAN_POINT('Ctrl Pts',(23.8559747898466,5.00065139823827,3.9443102740046));
#63412=CARTESIAN_POINT('Ctrl Pts',(23.8224514865274,5.59270210321936,3.04725796889044));
#63413=CARTESIAN_POINT('Ctrl Pts',(23.7889281832081,5.93478660287112,2.06330182669177));
#63414=CARTESIAN_POINT('Ctrl Pts',(23.7554048798889,6.27687110252287,1.07934568449311));
#63415=CARTESIAN_POINT('Ctrl Pts',(23.7218815765696,6.36898939684528,0.00848570520994477));
#63416=CARTESIAN_POINT('Ctrl Pts',(23.6883582732503,6.1999721823008,-1.01943679958313));
#63417=CARTESIAN_POINT('Ctrl Pts',(23.654834969931,6.03095496775632,-2.04735930437621));
#63418=CARTESIAN_POINT('Ctrl Pts',(23.6213116666118,5.60080224434495,-3.0323443346792));
#63419=CARTESIAN_POINT('Ctrl Pts',(23.5877883632925,4.96166984463642,-3.85496287951956));
#63420=CARTESIAN_POINT('Ctrl Pts',(23.5542650599732,4.32253744492788,-4.67758142435991));
#63421=CARTESIAN_POINT('Ctrl Pts',(23.520741756654,3.47442536892218,-5.33783348373762));
#63422=CARTESIAN_POINT('Ctrl Pts',(23.4872184533347,2.52016684079541,-5.7556637796351));
#63423=CARTESIAN_POINT('Ctrl Pts',(23.4536951500154,1.56590831266863,-6.17349407553258));
#63424=CARTESIAN_POINT('Ctrl Pts',(23.4201718466962,0.505503332420783,-6.34890260794982));
#63425=CARTESIAN_POINT('Ctrl Pts',(23.3866485433769,-0.532474452506596,
-6.26062116782958));
#63426=CARTESIAN_POINT('Ctrl Pts',(23.3531252400576,-1.57045223743399,-6.17233972770935));
#63427=CARTESIAN_POINT('Ctrl Pts',(23.3196019367384,-2.58600282704091,-5.82036831505163));
#63428=CARTESIAN_POINT('Ctrl Pts',(23.2860786334191,-3.45599114944506,-5.24738331214763));
#63429=CARTESIAN_POINT('Ctrl Pts',(23.2525553300998,-4.32597947184921,-4.67439830924364));
#63430=CARTESIAN_POINT('Ctrl Pts',(23.2190320267806,-5.05040552705059,-3.88039971609336));
#63431=CARTESIAN_POINT('Ctrl Pts',(23.1855087234613,-5.54143296765939,-2.9616595203679));
#63432=CARTESIAN_POINT('Ctrl Pts',(23.1524386259977,-6.02582214505017,-2.05533989168984));
#63433=CARTESIAN_POINT('Ctrl Pts',(23.1193685285341,-6.28308074218897,-1.02762865739354));
#63434=CARTESIAN_POINT('Ctrl Pts',(23.0862984310705,-6.28322123118156,1.47945420200454E-5));
#63435=CARTESIAN_POINT('Ctrl Pts',(22.9000381542954,-6.2830493926505,0.000112281392144475));
#63436=CARTESIAN_POINT('Ctrl Pts',(22.9297036365145,-6.28228300986044,-0.921806976571348));
#63437=CARTESIAN_POINT('Ctrl Pts',(22.9593691187337,-6.07685444261615,-1.84405650430791));
#63438=CARTESIAN_POINT('Ctrl Pts',(22.9890346009528,-5.68395407028917,-2.67797921054549));
#63439=CARTESIAN_POINT('Ctrl Pts',(23.022557904272,-5.2399593204827,-3.62034864919228));
#63440=CARTESIAN_POINT('Ctrl Pts',(23.0560812075913,-4.55656313549588,-4.4499247650114));
#63441=CARTESIAN_POINT('Ctrl Pts',(23.0896045109106,-3.71662700861485,-5.06612181102126));
#63442=CARTESIAN_POINT('Ctrl Pts',(23.1231278142299,-2.87669088173383,-5.68231885703111));
#63443=CARTESIAN_POINT('Ctrl Pts',(23.1566511175491,-1.88021481295859,-6.08513683323169));
#63444=CARTESIAN_POINT('Ctrl Pts',(23.1901744208684,-0.848021096730545,
-6.22573423338731));
#63445=CARTESIAN_POINT('Ctrl Pts',(23.2236977241877,0.184172619497497,-6.36633163354292));
#63446=CARTESIAN_POINT('Ctrl Pts',(23.2572210275069,1.25208398317834,-6.24470845765358));
#63447=CARTESIAN_POINT('Ctrl Pts',(23.2907443308262,2.22622920111004,-5.8756114634475));
#63448=CARTESIAN_POINT('Ctrl Pts',(23.3242676341455,3.20037441904174,-5.50651446924142));
#63449=CARTESIAN_POINT('Ctrl Pts',(23.3577909374647,4.0807534912243,-4.88994365671861));
#63450=CARTESIAN_POINT('Ctrl Pts',(23.391314240784,4.76062083408337,-4.10065797151653));
#63451=CARTESIAN_POINT('Ctrl Pts',(23.4248375441033,5.44048817694244,-3.31137228631445));
#63452=CARTESIAN_POINT('Ctrl Pts',(23.4583608474225,5.91984379047802,-2.34937172843309));
#63453=CARTESIAN_POINT('Ctrl Pts',(23.4918841507418,6.14056601287044,-1.33129845145675));
#63454=CARTESIAN_POINT('Ctrl Pts',(23.5254074540611,6.36128823526285,-0.313225174480436));
#63455=CARTESIAN_POINT('Ctrl Pts',(23.5589307573803,6.32337706651211,0.760920821590882));
#63456=CARTESIAN_POINT('Ctrl Pts',(23.5924540606996,6.03142921951174,1.76089979706136));
#63457=CARTESIAN_POINT('Ctrl Pts',(23.6259773640189,5.73948137251136,2.76087877253185));
#63458=CARTESIAN_POINT('Ctrl Pts',(23.6595006673381,5.19349684726135,3.68669072740151));
#63459=CARTESIAN_POINT('Ctrl Pts',(23.6930239706574,4.4596760324487,4.42608136062515));
#63460=CARTESIAN_POINT('Ctrl Pts',(23.7265472739767,3.72585521763604,5.16547199384878));
#63461=CARTESIAN_POINT('Ctrl Pts',(23.7600705772959,2.80419811326075,5.71844130542639));
#63462=CARTESIAN_POINT('Ctrl Pts',(23.7935938806152,1.80645524653388,6.01794200433511));
#63463=CARTESIAN_POINT('Ctrl Pts',(23.8271171839345,0.808712379806998,6.31744270324383));
#63464=CARTESIAN_POINT('Ctrl Pts',(23.8606404872537,-0.265116249271454,
6.36347478948366));
#63465=CARTESIAN_POINT('Ctrl Pts',(23.894163790573,-1.28482938161696,6.15045689241088));
#63466=CARTESIAN_POINT('Ctrl Pts',(23.9276870938923,-2.30454251396245,5.9374389953381));
#63467=CARTESIAN_POINT('Ctrl Pts',(23.9612103972115,-3.27014014957498,5.46537111495272));
#63468=CARTESIAN_POINT('Ctrl Pts',(23.9947337005308,-4.06454399074362,4.79149127856668));
#63469=CARTESIAN_POINT('Ctrl Pts',(24.0282570038501,-4.85894783191226,4.11761144218065));
#63470=CARTESIAN_POINT('Ctrl Pts',(24.0617803071694,-5.482157878637,3.24191964979396));
#63471=CARTESIAN_POINT('Ctrl Pts',(24.0953036104886,-5.858610180991,2.27059315432319));
#63472=CARTESIAN_POINT('Ctrl Pts',(24.1202151250909,-6.1383557937021,1.54879035508707));
#63473=CARTESIAN_POINT('Ctrl Pts',(24.1451266396931,-6.28183856374847,0.774176826311881));
#63474=CARTESIAN_POINT('Ctrl Pts',(24.1700381542954,-6.28260548706583,-0.00016035527560624));
#63475=CARTESIAN_POINT('Origin',(37.,0.,0.));
#63476=CARTESIAN_POINT('',(25.6262984310704,-6.28256558997173,0.000158582405482416));
#63477=CARTESIAN_POINT('',(25.4400381542954,-6.28229618588959,0.000112427966882737));
#63478=CARTESIAN_POINT('',(37.,-6.28269,-7.69407619853508E-16));
#63479=CARTESIAN_POINT('Ctrl Pts',(25.6262984310704,-6.28256558997173,0.000158582405482416));
#63480=CARTESIAN_POINT('Ctrl Pts',(25.6172611415298,-6.28283770681108,0.281074340762559));
#63481=CARTESIAN_POINT('Ctrl Pts',(25.6082238519892,-6.2643418990228,0.561954538374488));
#63482=CARTESIAN_POINT('Ctrl Pts',(25.5991865624485,-6.22678609035292,0.84026271762793));
#63483=CARTESIAN_POINT('Ctrl Pts',(25.5656632591293,-6.0874749883041,1.8726308261621));
#63484=CARTESIAN_POINT('Ctrl Pts',(25.53213995581,-5.6858990072367,2.86960806101203));
#63485=CARTESIAN_POINT('Ctrl Pts',(25.4986166524908,-5.0707490620111,3.71031136156545));
#63486=CARTESIAN_POINT('Ctrl Pts',(25.4650933491715,-4.45559911678551,4.55101466211884));
#63487=CARTESIAN_POINT('Ctrl Pts',(25.4315700458522,-3.62687520740172,5.23544402837575));
#63488=CARTESIAN_POINT('Ctrl Pts',(25.3980467425329,-2.68505975117786,5.68061269426572));
#63489=CARTESIAN_POINT('Ctrl Pts',(25.3645234392137,-1.74324429495397,6.1257813601557));
#63490=CARTESIAN_POINT('Ctrl Pts',(25.3310001358944,-0.688337291889995,
6.33168932567874));
#63491=CARTESIAN_POINT('Ctrl Pts',(25.2974768325751,0.351754237939646,6.27337033864091));
#63492=CARTESIAN_POINT('Ctrl Pts',(25.2639535292559,1.39184576776926,6.21505135160309));
#63493=CARTESIAN_POINT('Ctrl Pts',(25.2304302259366,2.41712182436454,5.8925054120044));
#63494=CARTESIAN_POINT('Ctrl Pts',(25.1969069226173,3.30326812715684,5.3448410761928));
#63495=CARTESIAN_POINT('Ctrl Pts',(25.163383619298,4.18941442994916,4.79717674038119));
#63496=CARTESIAN_POINT('Ctrl Pts',(25.1298603159788,4.9364309789385,4.02439400835665));
#63497=CARTESIAN_POINT('Ctrl Pts',(25.0963370126595,5.45374233908651,3.12019245376039));
#63498=CARTESIAN_POINT('Ctrl Pts',(25.0628137093403,5.97105369923453,2.21599089916413));
#63499=CARTESIAN_POINT('Ctrl Pts',(25.029290406021,6.25865987054123,1.18037052199615));
#63500=CARTESIAN_POINT('Ctrl Pts',(24.9957671027017,6.28168872852549,0.138899847242213));
#63501=CARTESIAN_POINT('Ctrl Pts',(24.9622437993825,6.30471758650975,-0.90257082751171));
#63502=CARTESIAN_POINT('Ctrl Pts',(24.9287204960632,6.06316913117159,-1.94989179985159));
#63503=CARTESIAN_POINT('Ctrl Pts',(24.8951971927439,5.58633100875483,-2.87607585266319));
#63504=CARTESIAN_POINT('Ctrl Pts',(24.8616738894247,5.10949288633808,-3.80225990547479));
#63505=CARTESIAN_POINT('Ctrl Pts',(24.8281505861054,4.39736509684273,-4.60730703875809));
#63506=CARTESIAN_POINT('Ctrl Pts',(24.7946272827861,3.53629282823508,-5.19360563410635));
#63507=CARTESIAN_POINT('Ctrl Pts',(24.7611039794669,2.67522055962742,-5.77990422945461));
#63508=CARTESIAN_POINT('Ctrl Pts',(24.7275806761476,1.66520381190747,-6.14745428686781));
#63509=CARTESIAN_POINT('Ctrl Pts',(24.6940573728283,0.628706681010569,-6.25169052008341));
#63510=CARTESIAN_POINT('Ctrl Pts',(24.6605340695091,-0.407790449886316,
-6.35592675329901));
#63511=CARTESIAN_POINT('Ctrl Pts',(24.6270107661898,-1.47076796396015,-6.19684916231701));
#63512=CARTESIAN_POINT('Ctrl Pts',(24.5934874628705,-2.43134029515023,-5.79374583657472));
#63513=CARTESIAN_POINT('Ctrl Pts',(24.5599641595512,-3.39191262634031,-5.39064251083242));
#63514=CARTESIAN_POINT('Ctrl Pts',(24.526440856232,-4.25007977464665,-4.74351345032983));
#63515=CARTESIAN_POINT('Ctrl Pts',(24.4929175529127,-4.90178934270455,-3.93082277511924));
#63516=CARTESIAN_POINT('Ctrl Pts',(24.4593942495934,-5.55349891076246,-3.11813209990865));
#63517=CARTESIAN_POINT('Ctrl Pts',(24.4258709462742,-5.99875089857193,-2.13987980999006));
#63518=CARTESIAN_POINT('Ctrl Pts',(24.3923476429549,-6.18355869425389,-1.11467857446229));
#63519=CARTESIAN_POINT('Ctrl Pts',(24.3803312389934,-6.24980291568388,-0.747195929014405));
#63520=CARTESIAN_POINT('Ctrl Pts',(24.368314835032,-6.28258373411747,-0.37368100665398));
#63521=CARTESIAN_POINT('Ctrl Pts',(24.3562984310705,-6.28232352063531,-0.000120941246437023));
#63522=CARTESIAN_POINT('Ctrl Pts',(24.1700381542954,-6.28260548706583,-0.00016035527560624));
#63523=CARTESIAN_POINT('Ctrl Pts',(24.1786499430124,-6.28287060870442,-0.267844930461688));
#63524=CARTESIAN_POINT('Ctrl Pts',(24.1872617317294,-6.26608045776481,-0.535496480747446));
#63525=CARTESIAN_POINT('Ctrl Pts',(24.1958735204464,-6.23196844560772,-0.800921855252021));
#63526=CARTESIAN_POINT('Ctrl Pts',(24.2293968237657,-6.09917984988718,-1.83414917080157));
#63527=CARTESIAN_POINT('Ctrl Pts',(24.2629201270849,-5.70390810046283,-2.83364260334581));
#63528=CARTESIAN_POINT('Ctrl Pts',(24.2964434304042,-5.09407972682174,-3.67821400438507));
#63529=CARTESIAN_POINT('Ctrl Pts',(24.3299667337235,-4.48425135318065,-4.52278540542433));
#63530=CARTESIAN_POINT('Ctrl Pts',(24.3634900370428,-3.65986635532282,-5.21243477495862));
#63531=CARTESIAN_POINT('Ctrl Pts',(24.397013340362,-2.72088105941141,-5.66354242376686));
#63532=CARTESIAN_POINT('Ctrl Pts',(24.4305366436813,-1.78189576349997,-6.11465007257511));
#63533=CARTESIAN_POINT('Ctrl Pts',(24.4640599470005,-0.72831016953494,-6.32721600065731));
#63534=CARTESIAN_POINT('Ctrl Pts',(24.4975832503198,0.312128922693782,-6.27546668072492));
#63535=CARTESIAN_POINT('Ctrl Pts',(24.5311065536391,1.35256801492247,-6.22371736079254));
#63536=CARTESIAN_POINT('Ctrl Pts',(24.5646298569584,2.37986060541485,-5.90765279284559));
#63537=CARTESIAN_POINT('Ctrl Pts',(24.5981531602776,3.26944790973518,-5.36559566970891));
#63538=CARTESIAN_POINT('Ctrl Pts',(24.6316764635969,4.15903521405553,-4.82353854657221));
#63539=CARTESIAN_POINT('Ctrl Pts',(24.6651997669162,4.91091723220384,-4.05548886824577));
#63540=CARTESIAN_POINT('Ctrl Pts',(24.6987230702354,5.43392859310039,-3.15457232764708));
#63541=CARTESIAN_POINT('Ctrl Pts',(24.7322463735547,5.95693995399695,-2.25365578704838));
#63542=CARTESIAN_POINT('Ctrl Pts',(24.7657696768739,6.25108065764178,-1.21987238417744));
#63543=CARTESIAN_POINT('Ctrl Pts',(24.7992929801932,6.2806862703203,-0.178567911677147));
#63544=CARTESIAN_POINT('Ctrl Pts',(24.8328162835125,6.31029188299883,0.862736560823136));
#63545=CARTESIAN_POINT('Ctrl Pts',(24.8663395868318,6.07536240471107,1.91156210295276));
#63546=CARTESIAN_POINT('Ctrl Pts',(24.899862890151,5.60438293358239,2.84073906915807));
#63547=CARTESIAN_POINT('Ctrl Pts',(24.9333861934703,5.13340346245372,3.76991603536338));
#63548=CARTESIAN_POINT('Ctrl Pts',(24.9669094967896,4.42637399848413,4.57944442564439));
#63549=CARTESIAN_POINT('Ctrl Pts',(25.0004328001088,3.56902155986432,5.17116927111213));
#63550=CARTESIAN_POINT('Ctrl Pts',(25.0339561034281,2.7116691212445,5.76289411657988));
#63551=CARTESIAN_POINT('Ctrl Pts',(25.0674794067474,1.70399370797445,6.13681541723436));
#63552=CARTESIAN_POINT('Ctrl Pts',(25.1010027100666,0.668175530195226,6.24759537631232));
#63553=CARTESIAN_POINT('Ctrl Pts',(25.1345260133859,-0.367642647583973,
6.35837533539027));
#63554=CARTESIAN_POINT('Ctrl Pts',(25.1680493167052,-1.43160358987234,6.2060139528917));
#63555=CARTESIAN_POINT('Ctrl Pts',(25.2015726200244,-2.39470249036147,5.80898498086604));
#63556=CARTESIAN_POINT('Ctrl Pts',(25.2350959233437,-3.35780139085063,5.41195600884038));
#63557=CARTESIAN_POINT('Ctrl Pts',(25.268619226663,-4.22003824954055,4.7702594472876));
#63558=CARTESIAN_POINT('Ctrl Pts',(25.3021425299822,-4.87686721843417,3.9617007281006));
#63559=CARTESIAN_POINT('Ctrl Pts',(25.3356658333015,-5.5336961873278,3.1531420089136));
#63560=CARTESIAN_POINT('Ctrl Pts',(25.3691891366208,-5.98511726642513,2.17772113209237));
#63561=CARTESIAN_POINT('Ctrl Pts',(25.40271243994,-6.17639584418372,1.15370745911635));
#63562=CARTESIAN_POINT('Ctrl Pts',(25.4151543447252,-6.2473873520683,0.773653008739074));
#63563=CARTESIAN_POINT('Ctrl Pts',(25.4275962495103,-6.28254517710532,0.386905077530623));
#63564=CARTESIAN_POINT('Ctrl Pts',(25.4400381542954,-6.28229618588959,0.000112427966882737));
#63565=CARTESIAN_POINT('Origin',(37.,0.,0.));
#63566=CARTESIAN_POINT('',(26.8962984310705,-6.28308193949819,-0.000102270523308912));
#63567=CARTESIAN_POINT('',(26.7100381542954,-6.28322420806427,-9.06020636693901E-7));
#63568=CARTESIAN_POINT('',(37.,-6.28269,-7.69407619853508E-16));
#63569=CARTESIAN_POINT('Ctrl Pts',(26.8962984310705,-6.28308193949819,-0.000102270523308912));
#63570=CARTESIAN_POINT('Ctrl Pts',(26.8662074480277,-6.28235777825568,0.935026311892883));
#63571=CARTESIAN_POINT('Ctrl Pts',(26.8361164649849,-6.07079837144568,1.87047159745313));
#63572=CARTESIAN_POINT('Ctrl Pts',(26.8060254819422,-5.66692843813987,2.71382175660999));
#63573=CARTESIAN_POINT('Ctrl Pts',(26.7725021786229,-5.2169911842954,3.65336843574593));
#63574=CARTESIAN_POINT('Ctrl Pts',(26.7389788753036,-4.52836959479689,4.47861214632833));
#63575=CARTESIAN_POINT('Ctrl Pts',(26.7054555719844,-3.68455874097844,5.08949244364578));
#63576=CARTESIAN_POINT('Ctrl Pts',(26.6719322686651,-2.84074788715999,5.70037274096323));
#63577=CARTESIAN_POINT('Ctrl Pts',(26.6384089653458,-1.84174776902159,6.09688962501574));
#63578=CARTESIAN_POINT('Ctrl Pts',(26.6048856620266,-0.808686720903557,
6.23096559427849));
#63579=CARTESIAN_POINT('Ctrl Pts',(26.5713623587073,0.224374327214448,6.36504156354124));
#63580=CARTESIAN_POINT('Ctrl Pts',(26.537839055388,1.29149630531209,6.23667661801425));
#63581=CARTESIAN_POINT('Ctrl Pts',(26.5043157520688,2.26329113284964,5.86143495209256));
#63582=CARTESIAN_POINT('Ctrl Pts',(26.4707924487495,3.23508596038721,5.48619328617085));
#63583=CARTESIAN_POINT('Ctrl Pts',(26.4372691454302,4.11155363736469,4.86407489985442));
#63584=CARTESIAN_POINT('Ctrl Pts',(26.403745842111,4.78642283519279,4.07051137971547));
#63585=CARTESIAN_POINT('Ctrl Pts',(26.3702225387917,5.4612920330209,3.27694785957651));
#63586=CARTESIAN_POINT('Ctrl Pts',(26.3366992354724,5.93456275169962,2.31193920561507));
#63587=CARTESIAN_POINT('Ctrl Pts',(26.3031759321531,6.1488511202917,1.29249230177033));
#63588=CARTESIAN_POINT('Ctrl Pts',(26.2696526288339,6.36313948888378,0.273045397925603));
#63589=CARTESIAN_POINT('Ctrl Pts',(26.2361293255146,6.31844550738921,-0.800839755802381));
#63590=CARTESIAN_POINT('Ctrl Pts',(26.2026060221954,6.02018830182727,-1.79895504673967));
#63591=CARTESIAN_POINT('Ctrl Pts',(26.1690827188761,5.72193109626534,-2.79707033767695));
#63592=CARTESIAN_POINT('Ctrl Pts',(26.1355594155568,5.17011066663604,-3.71941576582354));
#63593=CARTESIAN_POINT('Ctrl Pts',(26.1020361122376,4.43163500252052,-4.45415734500737));
#63594=CARTESIAN_POINT('Ctrl Pts',(26.0685128089183,3.69315933840497,-5.18889892419122));
#63595=CARTESIAN_POINT('Ctrl Pts',(26.034989505599,2.76802843980317,-5.7360366544123));
#63596=CARTESIAN_POINT('Ctrl Pts',(26.0014662022797,1.76841402998099,-6.02923032137723));
#63597=CARTESIAN_POINT('Ctrl Pts',(25.9679428989605,0.768799620158812,-6.32242398834215));
#63598=CARTESIAN_POINT('Ctrl Pts',(25.9344195956412,-0.30529830088375,-6.36167359205092));
#63599=CARTESIAN_POINT('Ctrl Pts',(25.9008962923219,-1.32364582252742,-6.14222013494744));
#63600=CARTESIAN_POINT('Ctrl Pts',(25.8673729890027,-2.34199334417108,-5.92276667784397));
#63601=CARTESIAN_POINT('Ctrl Pts',(25.8338496856834,-3.30459046641586,-5.44461015992825));
#63602=CARTESIAN_POINT('Ctrl Pts',(25.8003263823641,-4.09472270250518,-4.76572685319215));
#63603=CARTESIAN_POINT('Ctrl Pts',(25.7668030790449,-4.88485493859451,-4.08684354645604));
#63604=CARTESIAN_POINT('Ctrl Pts',(25.7332797757256,-5.50252228852838,-3.20723345089954));
#63605=CARTESIAN_POINT('Ctrl Pts',(25.6997564724063,-5.87283285198019,-2.23354891201208));
#63606=CARTESIAN_POINT('Ctrl Pts',(25.6752704586277,-6.14331423839656,-1.52235250012592));
#63607=CARTESIAN_POINT('Ctrl Pts',(25.6507844448491,-6.28182830512015,-0.760966431774124));
#63608=CARTESIAN_POINT('Ctrl Pts',(25.6262984310704,-6.28256558997173,0.000158582405482416));
#63609=CARTESIAN_POINT('Ctrl Pts',(25.4400381542954,-6.28229618588959,0.000112427966882737));
#63610=CARTESIAN_POINT('Ctrl Pts',(25.4611195528296,-6.28187429847437,-0.655263910009739));
#63611=CARTESIAN_POINT('Ctrl Pts',(25.4822009513637,-6.17980133808627,-1.31076863198916));
#63612=CARTESIAN_POINT('Ctrl Pts',(25.5032823498978,-5.97815379453737,-1.93405887555916));
#63613=CARTESIAN_POINT('Ctrl Pts',(25.5368056532171,-5.65749709071257,-2.92520506812781));
#63614=CARTESIAN_POINT('Ctrl Pts',(25.5703289565364,-5.08504760664311,-3.83489098413436));
#63615=CARTESIAN_POINT('Ctrl Pts',(25.6038522598556,-4.33021459588196,-4.55281759780484));
#63616=CARTESIAN_POINT('Ctrl Pts',(25.6373755631749,-3.57538158512081,-5.27074421147534));
#63617=CARTESIAN_POINT('Ctrl Pts',(25.6708988664942,-2.63816504766797,-5.79691152280978));
#63618=CARTESIAN_POINT('Ctrl Pts',(25.7044221698134,-1.63220208529813,-6.06752197177885));
#63619=CARTESIAN_POINT('Ctrl Pts',(25.7379454731327,-0.626239122928279,
-6.33813242074792));
#63620=CARTESIAN_POINT('Ctrl Pts',(25.771468776452,0.448470264358575,-6.35318600735159));
#63621=CARTESIAN_POINT('Ctrl Pts',(25.8049920797712,1.4616180259242,-6.11085749069344));
#63622=CARTESIAN_POINT('Ctrl Pts',(25.8385153830905,2.47476578748983,-5.86852897403529));
#63623=CARTESIAN_POINT('Ctrl Pts',(25.8720386864098,3.42635192333425,-5.36881835411532));
#63624=CARTESIAN_POINT('Ctrl Pts',(25.905561989729,4.20099702406263,-4.67231532851622));
#63625=CARTESIAN_POINT('Ctrl Pts',(25.9390852930483,4.97564212479099,-3.97581230291713));
#63626=CARTESIAN_POINT('Ctrl Pts',(25.9726085963676,5.57334619040331,-3.08251687163894));
#63627=CARTESIAN_POINT('Ctrl Pts',(26.0061318996868,5.92163786020453,-2.10074072123691));
#63628=CARTESIAN_POINT('Ctrl Pts',(26.0396552030061,6.26992953000576,-1.11896457083487));
#63629=CARTESIAN_POINT('Ctrl Pts',(26.0731785063254,6.36880880399585,-0.048707701308994));
#63630=CARTESIAN_POINT('Ctrl Pts',(26.1067018096447,6.20628661276258,0.980261702564567));
#63631=CARTESIAN_POINT('Ctrl Pts',(26.1402251129639,6.0437644215293,2.00923110643813));
#63632=CARTESIAN_POINT('Ctrl Pts',(26.1737484162832,5.61984076507263,2.9969130446594));
#63633=CARTESIAN_POINT('Ctrl Pts',(26.2072717196024,4.98591620427515,3.82355150733151));
#63634=CARTESIAN_POINT('Ctrl Pts',(26.2407950229217,4.35199164347768,4.65018997000362));
#63635=CARTESIAN_POINT('Ctrl Pts',(26.274318326241,3.50806617833942,5.31578495712655));
#63636=CARTESIAN_POINT('Ctrl Pts',(26.3078416295603,2.5564654082707,5.73963336299332));
#63637=CARTESIAN_POINT('Ctrl Pts',(26.3413649328795,1.604864638202,6.16348176886008));
#63638=CARTESIAN_POINT('Ctrl Pts',(26.3748882361988,0.545588563202851,6.34558359347067));
#63639=CARTESIAN_POINT('Ctrl Pts',(26.408411539518,-0.492926048560667,6.26385906897027));
#63640=CARTESIAN_POINT('Ctrl Pts',(26.4419348428373,-1.53144066032422,6.18213454446987));
#63641=CARTESIAN_POINT('Ctrl Pts',(26.4754581461566,-2.54919380885212,5.83658367085848));
#63642=CARTESIAN_POINT('Ctrl Pts',(26.5089814494759,-3.42278336294098,5.26910434283143));
#63643=CARTESIAN_POINT('Ctrl Pts',(26.5425047527951,-4.29637291702982,4.7016250148044));
#63644=CARTESIAN_POINT('Ctrl Pts',(26.5760280561144,-5.0257988766796,3.91221723236171));
#63645=CARTESIAN_POINT('Ctrl Pts',(26.6095513594336,-5.52261865823816,2.99659634935212));
#63646=CARTESIAN_POINT('Ctrl Pts',(26.6430469577209,-6.01902784756412,2.08173217297243));
#63647=CARTESIAN_POINT('Ctrl Pts',(26.6765425560082,-6.2832151704884,1.04086342518149));
#63648=CARTESIAN_POINT('Ctrl Pts',(26.7100381542954,-6.28322420274766,-9.06011619686462E-7));
#63649=CARTESIAN_POINT('Origin',(37.,0.,0.));
#63650=CARTESIAN_POINT('',(28.1662984310705,-6.28216368284996,-2.4584581325704E-5));
#63651=CARTESIAN_POINT('',(27.9800381542954,-6.2822927855414,-0.000111271035758665));
#63652=CARTESIAN_POINT('',(37.,-6.28269,-7.69407619853508E-16));
#63653=CARTESIAN_POINT('Ctrl Pts',(28.1662984310705,-6.28216368284996,-2.4584581325704E-5));
#63654=CARTESIAN_POINT('Ctrl Pts',(28.1486770578448,-6.28208861679347,0.547819922382556));
#63655=CARTESIAN_POINT('Ctrl Pts',(28.1310556846192,-6.21113725184404,1.09568350878778));
#63656=CARTESIAN_POINT('Ctrl Pts',(28.1134343113936,-6.06955109855608,1.62464024068863));
#63657=CARTESIAN_POINT('Ctrl Pts',(28.0799110080743,-5.80019436331722,2.63093962151618));
#63658=CARTESIAN_POINT('Ctrl Pts',(28.046387704755,-5.27519530128862,3.56881107339447));
#63659=CARTESIAN_POINT('Ctrl Pts',(28.0128644014358,-4.55820982277412,4.32453808645659));
#63660=CARTESIAN_POINT('Ctrl Pts',(27.9793410981165,-3.84122434425962,5.0802650995187));
#63661=CARTESIAN_POINT('Ctrl Pts',(27.9458177947972,-2.93225244925926,5.65384767376462));
#63662=CARTESIAN_POINT('Ctrl Pts',(27.912294491478,-1.94150658880723,5.97573916894523));
#63663=CARTESIAN_POINT('Ctrl Pts',(27.8787711881587,-0.950760728355178,
6.29763066412585));
#63664=CARTESIAN_POINT('Ctrl Pts',(27.8452478848394,0.121759097548558,6.36783108024112));
#63665=CARTESIAN_POINT('Ctrl Pts',(27.8117245815202,1.14601032164098,6.17782864705233));
#63666=CARTESIAN_POINT('Ctrl Pts',(27.7782012782009,2.17026154573339,5.98782621386355));
#63667=CARTESIAN_POINT('Ctrl Pts',(27.7446779748816,3.14624416801453,5.53762093137072));
#63668=CARTESIAN_POINT('Ctrl Pts',(27.7111546715624,3.95562071560972,4.8817999963013));
#63669=CARTESIAN_POINT('Ctrl Pts',(27.6776313682431,4.76499726320491,4.22597906123187));
#63670=CARTESIAN_POINT('Ctrl Pts',(27.6441080649238,5.40776773611416,3.36454247358585));
#63671=CARTESIAN_POINT('Ctrl Pts',(27.6105847616046,5.80599649115486,2.40193904884065));
#63672=CARTESIAN_POINT('Ctrl Pts',(27.5770614582853,6.20422524619555,1.43933562409545));
#63673=CARTESIAN_POINT('Ctrl Pts',(27.543538154966,6.35791228336769,0.375565362251069));
#63674=CARTESIAN_POINT('Ctrl Pts',(27.5100148516468,6.24842311556325,-0.660390050305834));
#63675=CARTESIAN_POINT('Ctrl Pts',(27.4764915483275,6.13893394775881,-1.69634546286274));
#63676=CARTESIAN_POINT('Ctrl Pts',(27.4429682450082,5.76626857497779,-2.70448602613216));
#63677=CARTESIAN_POINT('Ctrl Pts',(27.409444941689,5.17561251326937,-3.56257513073585));
#63678=CARTESIAN_POINT('Ctrl Pts',(27.3759216383697,4.58495645156096,-4.42066423533953));
#63679=CARTESIAN_POINT('Ctrl Pts',(27.3423983350504,3.77630970092515,-5.12870188127748));
#63680=CARTESIAN_POINT('Ctrl Pts',(27.3088750317312,2.84772033182337,-5.60083880872927));
#63681=CARTESIAN_POINT('Ctrl Pts',(27.2753517284119,1.91913096272157,-6.07297573618107));
#63682=CARTESIAN_POINT('Ctrl Pts',(27.2418284250926,0.87059897515379,-6.3092119451467));
#63683=CARTESIAN_POINT('Ctrl Pts',(27.2083051217734,-0.170741578690559,
-6.28090389696852));
#63684=CARTESIAN_POINT('Ctrl Pts',(27.1747818184541,-1.21208213253486,-6.25259584879034));
#63685=CARTESIAN_POINT('Ctrl Pts',(27.1412585151348,-2.24623125265574,-5.95974354346838));
#63686=CARTESIAN_POINT('Ctrl Pts',(27.1077352118156,-3.14779880335115,-5.4378551969751));
#63687=CARTESIAN_POINT('Ctrl Pts',(27.0742119084963,-4.04936635404659,-4.9159668504818));
#63688=CARTESIAN_POINT('Ctrl Pts',(27.040688605177,-4.81835233531656,-4.16504246281716));
#63689=CARTESIAN_POINT('Ctrl Pts',(27.0071653018578,-5.36151752791466,-3.2761312927769));
#63690=CARTESIAN_POINT('Ctrl Pts',(26.9736419985385,-5.90468272051275,-2.38722012273665));
#63691=CARTESIAN_POINT('Ctrl Pts',(26.9401186952192,-6.22202712443898,-1.36032217032077));
#63692=CARTESIAN_POINT('Ctrl Pts',(26.9065953919,-6.27507286730687,-0.319948370268094));
#63693=CARTESIAN_POINT('Ctrl Pts',(26.9031630716235,-6.28050401402572,-0.213428554632629));
#63694=CARTESIAN_POINT('Ctrl Pts',(26.899730751347,-6.28316454076491,-0.106767472853189));
#63695=CARTESIAN_POINT('Ctrl Pts',(26.8962984310705,-6.28308193949819,-0.000102270523308912));
#63696=CARTESIAN_POINT('Ctrl Pts',(26.7100381542954,-6.28322420274766,-9.06011619686462E-7));
#63697=CARTESIAN_POINT('Ctrl Pts',(26.7435891626467,-6.28323324994852,-1.04258708610992));
#63698=CARTESIAN_POINT('Ctrl Pts',(26.777140170998,-6.01813621291833,-2.08516881317694));
#63699=CARTESIAN_POINT('Ctrl Pts',(26.8106911793493,-5.52015237330997,-3.00113716792668));
#63700=CARTESIAN_POINT('Ctrl Pts',(26.8442144826685,-5.02257974811507,-3.9163491539757));
#63701=CARTESIAN_POINT('Ctrl Pts',(26.8777377859878,-4.29250482183851,-4.70515678554019));
#63702=CARTESIAN_POINT('Ctrl Pts',(26.911261089307,-3.41844886505665,-5.27191747680705));
#63703=CARTESIAN_POINT('Ctrl Pts',(26.9447843926263,-2.54439290827479,-5.8386781680739));
#63704=CARTESIAN_POINT('Ctrl Pts',(26.9783076959456,-1.52635592098762,-6.18339191904313));
#63705=CARTESIAN_POINT('Ctrl Pts',(27.0118309992649,-0.487774449725965,
-6.26426233577947));
#63706=CARTESIAN_POINT('Ctrl Pts',(27.0453543025841,0.550807021535724,-6.34513275251581));
#63707=CARTESIAN_POINT('Ctrl Pts',(27.0788776059034,1.60993297677191,-6.16215983501923));
#63708=CARTESIAN_POINT('Ctrl Pts',(27.1124009092227,2.56118484977315,-5.73752897078204));
#63709=CARTESIAN_POINT('Ctrl Pts',(27.1459242125419,3.51243672277437,-5.31289810654485));
#63710=CARTESIAN_POINT('Ctrl Pts',(27.1794475158612,4.35581451354066,-4.64660929556708));
#63711=CARTESIAN_POINT('Ctrl Pts',(27.2129708191805,4.98905902794354,-3.81944976939948));
#63712=CARTESIAN_POINT('Ctrl Pts',(27.2464941224997,5.62230354234643,-2.99229024323187));
#63713=CARTESIAN_POINT('Ctrl Pts',(27.280017425819,6.04541478038589,-2.00426000187443));
#63714=CARTESIAN_POINT('Ctrl Pts',(27.3135407291383,6.20709068656277,-0.975157286829399));
#63715=CARTESIAN_POINT('Ctrl Pts',(27.3470640324575,6.36876659273964,0.0539454282156333));
#63716=CARTESIAN_POINT('Ctrl Pts',(27.3805873357768,6.26900716705394,1.1241206169483));
#63717=CARTESIAN_POINT('Ctrl Pts',(27.4141106390961,5.91990819693216,2.10560999835346));
#63718=CARTESIAN_POINT('Ctrl Pts',(27.4476339424153,5.57080922681039,3.08709937975862));
#63719=CARTESIAN_POINT('Ctrl Pts',(27.4811572457346,4.97237071225256,3.97990295383629));
#63720=CARTESIAN_POINT('Ctrl Pts',(27.5146805490539,4.19715306557227,4.67576867150504));
#63721=CARTESIAN_POINT('Ctrl Pts',(27.5482038523731,3.42193541889198,5.37163438917379));
#63722=CARTESIAN_POINT('Ctrl Pts',(27.5817271556924,2.46993864008926,5.8705622504336));
#63723=CARTESIAN_POINT('Ctrl Pts',(27.6152504590117,1.45659192884083,6.11205746685242));
#63724=CARTESIAN_POINT('Ctrl Pts',(27.6487737623309,0.443245217592412,6.35355268327125));
#63725=CARTESIAN_POINT('Ctrl Pts',(27.6822970656502,-0.631451426101716,
6.33761525484909));
#63726=CARTESIAN_POINT('Ctrl Pts',(27.7158203689695,-1.63719149675844,6.06617758792244));
#63727=CARTESIAN_POINT('Ctrl Pts',(27.7493436722887,-2.64293156741516,5.79473992099578));
#63728=CARTESIAN_POINT('Ctrl Pts',(27.782866975608,-3.57971506503448,5.26780201556465));
#63729=CARTESIAN_POINT('Ctrl Pts',(27.8163902789273,-4.33395739373514,4.54925486586091));
#63730=CARTESIAN_POINT('Ctrl Pts',(27.8499135822465,-5.0881997224358,3.83070771615717));
#63731=CARTESIAN_POINT('Ctrl Pts',(27.8834368855658,-5.6599008822178,2.92055132218081));
#63732=CARTESIAN_POINT('Ctrl Pts',(27.9169601888851,-5.97974235352591,1.92914175495713));
#63733=CARTESIAN_POINT('Ctrl Pts',(27.9379861773552,-6.18034857135421,1.30732456913029));
#63734=CARTESIAN_POINT('Ctrl Pts',(27.9590121658253,-6.28187663832541,0.653543498152181));
#63735=CARTESIAN_POINT('Ctrl Pts',(27.9800381542954,-6.2822927855414,-0.000111271035758665));
#63736=CARTESIAN_POINT('Origin',(37.,0.,0.));
#63737=CARTESIAN_POINT('',(29.4362984310705,-6.2829384025201,0.000137440727676699));
#63738=CARTESIAN_POINT('',(29.2500381542954,-6.2826107429555,0.000160513984483283));
#63739=CARTESIAN_POINT('',(37.,-6.28269,-7.69407619853508E-16));
#63740=CARTESIAN_POINT('Ctrl Pts',(29.4362984310705,-6.2829384025201,0.000137440727676699));
#63741=CARTESIAN_POINT('Ctrl Pts',(29.431146667662,-6.28309165294254,0.160247852387589));
#63742=CARTESIAN_POINT('Ctrl Pts',(29.4259949042535,-6.27709430813338,0.320346810608086));
#63743=CARTESIAN_POINT('Ctrl Pts',(29.420843140845,-6.26486526914223,0.479968341813839));
#63744=CARTESIAN_POINT('Ctrl Pts',(29.3873198375257,-6.18528906369617,1.51864977622924));
#63745=CARTESIAN_POINT('Ctrl Pts',(29.3537965342065,-5.84184412917577,2.53711551071983));
#63746=CARTESIAN_POINT('Ctrl Pts',(29.3202732308872,-5.27617301606801,3.41187701334088));
#63747=CARTESIAN_POINT('Ctrl Pts',(29.2867499275679,-4.71050190296023,4.28663851596196));
#63748=CARTESIAN_POINT('Ctrl Pts',(29.2532266242487,-3.92260461126508,5.0176957867135));
#63749=CARTESIAN_POINT('Ctrl Pts',(29.2197033209294,-3.00801334847831,5.51640844617441));
#63750=CARTESIAN_POINT('Ctrl Pts',(29.1861800176101,-2.09342208569153,6.01512110563532));
#63751=CARTESIAN_POINT('Ctrl Pts',(29.1526567142909,-1.05213685181313,6.28148915380559));
#63752=CARTESIAN_POINT('Ctrl Pts',(29.1191334109716,-0.0104130332667599,
6.28321557949322));
#63753=CARTESIAN_POINT('Ctrl Pts',(29.0856101076523,1.03131078527958,6.28494200518084));
#63754=CARTESIAN_POINT('Ctrl Pts',(29.0520868043331,2.07347318849388,6.02202680838582));
#63755=CARTESIAN_POINT('Ctrl Pts',(29.0185635010138,2.98971243354806,5.52634834355709));
#63756=CARTESIAN_POINT('Ctrl Pts',(28.9850401976945,3.90595167860227,5.03066987872835));
#63757=CARTESIAN_POINT('Ctrl Pts',(28.9515168943753,4.69626776549635,4.30222814586588));
#63758=CARTESIAN_POINT('Ctrl Pts',(28.917993591056,5.26483520885776,3.42934639154749));
#63759=CARTESIAN_POINT('Ctrl Pts',(28.8844702877367,5.83340265221916,2.55646463722912));
#63760=CARTESIAN_POINT('Ctrl Pts',(28.8509469844174,6.1802214520479,1.53914286145485));
#63761=CARTESIAN_POINT('Ctrl Pts',(28.8174236810982,6.26323997814055,0.500730891667414));
#63762=CARTESIAN_POINT('Ctrl Pts',(28.7839003777789,6.3462585042332,-0.537681078120038));
#63763=CARTESIAN_POINT('Ctrl Pts',(28.7503770744597,6.16547675658973,-1.5971832419207));
#63764=CARTESIAN_POINT('Ctrl Pts',(28.7168537711404,5.74281444430087,-2.54931141839858));
#63765=CARTESIAN_POINT('Ctrl Pts',(28.6833304678211,5.32015213201201,-3.50143959487647));
#63766=CARTESIAN_POINT('Ctrl Pts',(28.6498071645018,4.65560925507778,-4.34619378403158));
#63767=CARTESIAN_POINT('Ctrl Pts',(28.6162838611826,3.82976135129761,-4.98114790402325));
#63768=CARTESIAN_POINT('Ctrl Pts',(28.5827605578633,3.00391344751746,-5.6161020240149));
#63769=CARTESIAN_POINT('Ctrl Pts',(28.5492372545441,2.01676051689141,-6.04125607484308));
#63770=CARTESIAN_POINT('Ctrl Pts',(28.5157139512248,0.987994427373088,-6.20506031083726));
#63771=CARTESIAN_POINT('Ctrl Pts',(28.4821906479055,-0.0407716621452466,
-6.36886454683144));
#63772=CARTESIAN_POINT('Ctrl Pts',(28.4486673445863,-1.11115091055585,-6.27131896799162));
#63773=CARTESIAN_POINT('Ctrl Pts',(28.415144041267,-2.09336029469551,-5.92425093376711));
#63774=CARTESIAN_POINT('Ctrl Pts',(28.3816207379477,-3.07556967883516,-5.5771828995426));
#63775=CARTESIAN_POINT('Ctrl Pts',(28.3480974346284,-3.96960919870387,-4.9805924099334));
#63776=CARTESIAN_POINT('Ctrl Pts',(28.3145741313092,-4.66707694732499,-4.20681580502353));
#63777=CARTESIAN_POINT('Ctrl Pts',(28.2810508279899,-5.3645446959461,-3.43303920011367));
#63778=CARTESIAN_POINT('Ctrl Pts',(28.2475275246706,-5.86544067331962,-2.48207647990313));
#63779=CARTESIAN_POINT('Ctrl Pts',(28.2140042213514,-6.10903145778184,-1.46923146490945));
#63780=CARTESIAN_POINT('Ctrl Pts',(28.1981022912577,-6.22457984479734,-0.988783864900291));
#63781=CARTESIAN_POINT('Ctrl Pts',(28.1822003611641,-6.28223142417565,-0.494411993574757));
#63782=CARTESIAN_POINT('Ctrl Pts',(28.1662984310705,-6.28216368284996,-2.4584581325704E-5));
#63783=CARTESIAN_POINT('Ctrl Pts',(27.9800381542954,-6.2822927855414,-0.000111271035758665));
#63784=CARTESIAN_POINT('Ctrl Pts',(27.9925354691446,-6.28254013290341,-0.388627105371091));
#63785=CARTESIAN_POINT('Ctrl Pts',(28.0050327839937,-6.24706653565671,-0.777098319653106));
#63786=CARTESIAN_POINT('Ctrl Pts',(28.0175300988429,-6.17544494012033,-1.15878657086317));
#63787=CARTESIAN_POINT('Ctrl Pts',(28.0510534021621,-5.9833242725724,-2.18264258898881));
#63788=CARTESIAN_POINT('Ctrl Pts',(28.0845767054814,-5.53110115464228,-3.1576918847691));
#63789=CARTESIAN_POINT('Ctrl Pts',(28.1181000088007,-4.8736074447357,-3.96571015076587));
#63790=CARTESIAN_POINT('Ctrl Pts',(28.15162331212,-4.21611373482911,-4.77372841676265));
#63791=CARTESIAN_POINT('Ctrl Pts',(28.1851466154392,-3.35334943294606,-5.41471565297589));
#63792=CARTESIAN_POINT('Ctrl Pts',(28.2186699187585,-2.38992433934372,-5.81095243290488));
#63793=CARTESIAN_POINT('Ctrl Pts',(28.2521932220777,-1.42649924574139,-6.20718921283386));
#63794=CARTESIAN_POINT('Ctrl Pts',(28.285716525397,-0.362413360419771,-6.35867553647858));
#63795=CARTESIAN_POINT('Ctrl Pts',(28.3192398287163,0.673313361023692,-6.24704375229898));
#63796=CARTESIAN_POINT('Ctrl Pts',(28.3527631320355,1.70904008246716,-6.13541196811938));
#63797=CARTESIAN_POINT('Ctrl Pts',(28.3862864353548,2.71640764003249,-5.76066207611546));
#63798=CARTESIAN_POINT('Ctrl Pts',(28.4198097386741,3.57327315095031,-5.168232339395));
#63799=CARTESIAN_POINT('Ctrl Pts',(28.4533330419934,4.43013866186816,-4.57580260267451));
#63800=CARTESIAN_POINT('Ctrl Pts',(28.4868563453126,5.13650212613849,-3.76569302123748));
#63801=CARTESIAN_POINT('Ctrl Pts',(28.5203796486319,5.60671727774752,-2.83612903315032));
#63802=CARTESIAN_POINT('Ctrl Pts',(28.5539029519511,6.07693242935653,-1.90656504506317));
#63803=CARTESIAN_POINT('Ctrl Pts',(28.5874262552704,6.31099926830424,-0.857546650325907));
#63804=CARTESIAN_POINT('Ctrl Pts',(28.6209495585897,6.28053729111394,0.183733122212116));
#63805=CARTESIAN_POINT('Ctrl Pts',(28.654472861909,6.25007531392364,1.22501289475014));
#63806=CARTESIAN_POINT('Ctrl Pts',(28.6879961652282,5.95508452059534,2.25855404508894));
#63807=CARTESIAN_POINT('Ctrl Pts',(28.7215194685475,5.43133241785183,3.15904015360085));
#63808=CARTESIAN_POINT('Ctrl Pts',(28.7550427718668,4.90758031510832,4.05952626211275));
#63809=CARTESIAN_POINT('Ctrl Pts',(28.788566075186,4.15506690294963,4.82695732879775));
#63810=CARTESIAN_POINT('Ctrl Pts',(28.8220893785053,3.2650341087074,5.36828266713368));
#63811=CARTESIAN_POINT('Ctrl Pts',(28.8556126818245,2.37500131446517,5.90960800546961));
#63812=CARTESIAN_POINT('Ctrl Pts',(28.8891359851438,1.34744913813939,6.22482761545645));
#63813=CARTESIAN_POINT('Ctrl Pts',(28.9226592884631,0.306967838836412,6.27572125505832));
#63814=CARTESIAN_POINT('Ctrl Pts',(28.9561825917824,-0.73351346046657,6.32661489466019));
#63815=CARTESIAN_POINT('Ctrl Pts',(28.9897058951016,-1.78692388274679,6.1131825638771));
#63816=CARTESIAN_POINT('Ctrl Pts',(29.0232291984209,-2.72553786770569,5.66130284095216));
#63817=CARTESIAN_POINT('Ctrl Pts',(29.0567525017402,-3.6641518526646,5.20942311802722));
#63818=CARTESIAN_POINT('Ctrl Pts',(29.0902758050594,-4.48796940030219,4.51909600296044));
#63819=CARTESIAN_POINT('Ctrl Pts',(29.1237991083787,-5.09710298755033,3.67402336132696));
#63820=CARTESIAN_POINT('Ctrl Pts',(29.157322411698,-5.70623657479846,2.82895071969347));
#63821=CARTESIAN_POINT('Ctrl Pts',(29.1908457150172,-6.10068620165712,1.82913255149328));
#63822=CARTESIAN_POINT('Ctrl Pts',(29.2243690183365,-6.23262502064645,0.795796379284606));
#63823=CARTESIAN_POINT('Ctrl Pts',(29.2329253969895,-6.26630065468368,0.532051023374284));
#63824=CARTESIAN_POINT('Ctrl Pts',(29.2414817756425,-6.28287481385524,0.266122110498242));
#63825=CARTESIAN_POINT('Ctrl Pts',(29.2500381542954,-6.2826107429555,0.000160513984483283));
#63826=CARTESIAN_POINT('Origin',(37.,0.,0.));
#63827=CARTESIAN_POINT('',(30.7062984310705,-6.28273062840727,-0.000159623917656282));
#63828=CARTESIAN_POINT('',(30.5200381542954,-6.2830449876847,-0.000113525223425687));
#63829=CARTESIAN_POINT('',(37.,-6.28269,-7.69407619853508E-16));
#63830=CARTESIAN_POINT('Ctrl Pts',(30.7062984310705,-6.28273062840727,-0.000159623917656282));
#63831=CARTESIAN_POINT('Ctrl Pts',(30.6800929741599,-6.28189621740857,0.814351134667963));
#63832=CARTESIAN_POINT('Ctrl Pts',(30.6538875172492,-6.12272898283887,1.62917848446481));
#63833=CARTESIAN_POINT('Ctrl Pts',(30.6276820603386,-5.81392593643026,2.38268161015097));
#63834=CARTESIAN_POINT('Ctrl Pts',(30.5941587570194,-5.4188899625879,3.34659969486711));
#63835=CARTESIAN_POINT('Ctrl Pts',(30.5606354537001,-4.77897829200318,4.21016204306709));
#63836=CARTESIAN_POINT('Ctrl Pts',(30.5271121503808,-3.97177993930735,4.86866209172127));
#63837=CARTESIAN_POINT('Ctrl Pts',(30.4935888470616,-3.1645815866115,5.52716214037547));
#63838=CARTESIAN_POINT('Ctrl Pts',(30.4600655437423,-2.19009655180453,5.98059988948387));
#63839=CARTESIAN_POINT('Ctrl Pts',(30.426542240423,-1.16648072592444,6.17399620713318));
#63840=CARTESIAN_POINT('Ctrl Pts',(30.3930189371038,-0.142864900044355,
6.36739252478249));
#63841=CARTESIAN_POINT('Ctrl Pts',(30.3594956337845,0.929881716908839,6.3007474109727));
#63842=CARTESIAN_POINT('Ctrl Pts',(30.3259723304652,1.92168905935509,5.98214155706826));
#63843=CARTESIAN_POINT('Ctrl Pts',(30.2924490271459,2.91349640180132,5.66353570316382));
#63844=CARTESIAN_POINT('Ctrl Pts',(30.2589257238267,3.8243644697406,5.09296910916473));
#63845=CARTESIAN_POINT('Ctrl Pts',(30.2254024205074,4.543850901986,4.33962272901333));
#63846=CARTESIAN_POINT('Ctrl Pts',(30.1918791171881,5.26333733423141,3.58627634886191));
#63847=CARTESIAN_POINT('Ctrl Pts',(30.1583558138689,5.79144213078293,2.65015018255818));
#63848=CARTESIAN_POINT('Ctrl Pts',(30.1248325105496,6.06413281236254,1.64474912484432));
#63849=CARTESIAN_POINT('Ctrl Pts',(30.0913092072304,6.33682349394214,0.639348067130484));
#63850=CARTESIAN_POINT('Ctrl Pts',(30.0577859039111,6.35410006054985,-0.435327881993504));
#63851=CARTESIAN_POINT('Ctrl Pts',(30.0242626005918,6.11386773592056,-1.44897472625222));
#63852=CARTESIAN_POINT('Ctrl Pts',(29.9907392972725,5.87363541129127,-2.46262157051093));
#63853=CARTESIAN_POINT('Ctrl Pts',(29.9572159939533,5.375894195425,-3.41523930990441));
#63854=CARTESIAN_POINT('Ctrl Pts',(29.923692690634,4.68099499651056,-4.19132345355154));
#63855=CARTESIAN_POINT('Ctrl Pts',(29.8901693873147,3.98609579759611,-4.96740759719869));
#63856=CARTESIAN_POINT('Ctrl Pts',(29.8566460839955,3.09403861563348,-5.56695814509948));
#63857=CARTESIAN_POINT('Ctrl Pts',(29.8231227806762,2.11298499998145,-5.91727985137609));
#63858=CARTESIAN_POINT('Ctrl Pts',(29.7895994773569,1.13193138432942,-6.26760155765271));
#63859=CARTESIAN_POINT('Ctrl Pts',(29.7560761740377,0.0618813349879865,
-6.36869442230514));
#63860=CARTESIAN_POINT('Ctrl Pts',(29.7225528707184,-0.967422040125088,
-6.20830097900612));
#63861=CARTESIAN_POINT('Ctrl Pts',(29.6890295673991,-1.99672541523813,-6.04790753570709));
#63862=CARTESIAN_POINT('Ctrl Pts',(29.6555062640799,-2.98528211612282,-5.62602778445662));
#63863=CARTESIAN_POINT('Ctrl Pts',(29.6219829607606,-3.81323006828586,-4.99381446351071));
#63864=CARTESIAN_POINT('Ctrl Pts',(29.5884596574413,-4.64117802044892,-4.36160114256479));
#63865=CARTESIAN_POINT('Ctrl Pts',(29.5549363541221,-5.30851722389033,-3.51905425192342));
#63866=CARTESIAN_POINT('Ctrl Pts',(29.5214130508028,-5.73433308742517,-2.56833223943262));
#63867=CARTESIAN_POINT('Ctrl Pts',(29.493041510892,-6.09471081189538,-1.76371441091639));
#63868=CARTESIAN_POINT('Ctrl Pts',(29.4646699709812,-6.28209442927599,-0.881614801049781));
#63869=CARTESIAN_POINT('Ctrl Pts',(29.4362984310705,-6.2829384025201,0.000137440727676699));
#63870=CARTESIAN_POINT('Ctrl Pts',(29.2500381542954,-6.2826107429555,0.000160513984483283));
#63871=CARTESIAN_POINT('Ctrl Pts',(29.2750050789617,-6.28184020222472,-0.775897140030194));
#63872=CARTESIAN_POINT('Ctrl Pts',(29.299972003628,-6.13770353553637,-1.55223307308622));
#63873=CARTESIAN_POINT('Ctrl Pts',(29.3249389282943,-5.85674085145818,-2.27541053968984));
#63874=CARTESIAN_POINT('Ctrl Pts',(29.3584622316136,-5.47948985216053,-3.24642711023853));
#63875=CARTESIAN_POINT('Ctrl Pts',(29.3919855349328,-4.85555984244519,-4.12160607511872));
#63876=CARTESIAN_POINT('Ctrl Pts',(29.4255088382521,-4.06060206744173,-4.79483236152825));
#63877=CARTESIAN_POINT('Ctrl Pts',(29.4590321415714,-3.2656442924383,-5.46805864793777));
#63878=CARTESIAN_POINT('Ctrl Pts',(29.4925554448906,-2.29965875214676,-5.93933225587664));
#63879=CARTESIAN_POINT('Ctrl Pts',(29.5260787482099,-1.27977077755342,-6.1515114632252));
#63880=CARTESIAN_POINT('Ctrl Pts',(29.5596020515292,-0.259882802960086,
-6.36369067057376));
#63881=CARTESIAN_POINT('Ctrl Pts',(29.5931253548484,0.813907605935034,-6.31677547733201));
#63882=CARTESIAN_POINT('Ctrl Pts',(29.6266486581677,1.81140382422821,-6.01645433048753));
#63883=CARTESIAN_POINT('Ctrl Pts',(29.660171961487,2.80890004252139,-5.71613318364305));
#63884=CARTESIAN_POINT('Ctrl Pts',(29.6936952648062,3.73010207021262,-5.16240608319584));
#63885=CARTESIAN_POINT('Ctrl Pts',(29.7272185681255,4.46331455794289,-4.42241220174304));
#63886=CARTESIAN_POINT('Ctrl Pts',(29.7607418714448,5.19652704567314,-3.68241832029027));
#63887=CARTESIAN_POINT('Ctrl Pts',(29.7942651747641,5.74174999344244,-2.75615765783192));
#63888=CARTESIAN_POINT('Ctrl Pts',(29.8277884780833,6.03287535350555,-1.75593892101519));
#63889=CARTESIAN_POINT('Ctrl Pts',(29.8613117814026,6.32400071356866,-0.755720184198445));
#63890=CARTESIAN_POINT('Ctrl Pts',(29.8948350847218,6.36102848592557,0.318456626976721));
#63891=CARTESIAN_POINT('Ctrl Pts',(29.9283583880411,6.13946906911527,1.33634803649634));
#63892=CARTESIAN_POINT('Ctrl Pts',(29.9618816913604,5.91790965230497,2.35423944601598));
#63893=CARTESIAN_POINT('Ctrl Pts',(29.9954049946797,5.43776304632746,3.3158454538801));
#63894=CARTESIAN_POINT('Ctrl Pts',(30.0289282979989,4.75724682049554,4.10457174552421));
#63895=CARTESIAN_POINT('Ctrl Pts',(30.0624516013182,4.07673059466362,4.89329803716833));
#63896=CARTESIAN_POINT('Ctrl Pts',(30.0959749046374,3.1958447489773,5.50914461259242));
#63897=CARTESIAN_POINT('Ctrl Pts',(30.1294982079567,2.22139631308013,5.87744033959552));
#63898=CARTESIAN_POINT('Ctrl Pts',(30.163021511276,1.24694787718298,6.24573606659861));
#63899=CARTESIAN_POINT('Ctrl Pts',(30.1965448145952,0.178936851075004,6.36648094518072));
#63900=CARTESIAN_POINT('Ctrl Pts',(30.2300681179145,-0.85314088801549,6.2250347107841));
#63901=CARTESIAN_POINT('Ctrl Pts',(30.2635914212338,-1.88521862710601,6.08358847638747));
#63902=CARTESIAN_POINT('Ctrl Pts',(30.2971147245531,-2.88136307917904,5.67995112901209));
#63903=CARTESIAN_POINT('Ctrl Pts',(30.3306380278723,-3.72079215817558,5.06306352329593));
#63904=CARTESIAN_POINT('Ctrl Pts',(30.3641613311916,-4.56022123717211,4.44617591757977));
#63905=CARTESIAN_POINT('Ctrl Pts',(30.3976846345109,-5.24293494309215,3.61603805352283));
#63906=CARTESIAN_POINT('Ctrl Pts',(30.4312079378301,-5.68615453294266,2.67330378983877));
#63907=CARTESIAN_POINT('Ctrl Pts',(30.4608180099852,-6.0776363601075,1.84061647066497));
#63908=CARTESIAN_POINT('Ctrl Pts',(30.4904280821403,-6.28227375269624,0.920085612915368));
#63909=CARTESIAN_POINT('Ctrl Pts',(30.5200381542954,-6.2830449876847,-0.000113525223425687));
#63910=CARTESIAN_POINT('Origin',(37.,0.,0.));
#63911=CARTESIAN_POINT('',(31.9762984310705,-6.28222702961327,8.28361765500829E-5));
#63912=CARTESIAN_POINT('',(31.7900381542954,-6.28215913048763,-1.08654762067814E-5));
#63913=CARTESIAN_POINT('',(37.,-6.28269,-7.69407619853508E-16));
#63914=CARTESIAN_POINT('Ctrl Pts',(31.9762984310705,-6.28222702961327,8.28361765500829E-5));
#63915=CARTESIAN_POINT('Ctrl Pts',(31.962562583977,-6.28242667605806,0.427114891079368));
#63916=CARTESIAN_POINT('Ctrl Pts',(31.9488267368835,-6.23951894558398,0.854107376943399));
#63917=CARTESIAN_POINT('Ctrl Pts',(31.9350908897901,-6.15310136954611,1.27210454984562));
#63918=CARTESIAN_POINT('Ctrl Pts',(31.9015675864708,-5.94219318209182,2.29225612247456));
#63919=CARTESIAN_POINT('Ctrl Pts',(31.8680442831515,-5.47212362906995,3.2588281532623));
#63920=CARTESIAN_POINT('Ctrl Pts',(31.8345209798322,-4.79988844145972,4.05462419950228));
#63921=CARTESIAN_POINT('Ctrl Pts',(31.800997676513,-4.12765325384953,4.85042024574221));
#63922=CARTESIAN_POINT('Ctrl Pts',(31.7674743731937,-3.253252431651,5.4754403074344));
#63923=CARTESIAN_POINT('Ctrl Pts',(31.7339510698744,-2.28270669820105,5.85390097111628));
#63924=CARTESIAN_POINT('Ctrl Pts',(31.7004277665552,-1.31216096475108,6.23236163479817));
#63925=CARTESIAN_POINT('Ctrl Pts',(31.6669044632359,-0.245470320049679,
6.36426290046972));
#63926=CARTESIAN_POINT('Ctrl Pts',(31.6333811599166,0.788029454352046,6.23361179644046));
#63927=CARTESIAN_POINT('Ctrl Pts',(31.5998578565974,1.82152922875377,6.10296069241121));
#63928=CARTESIAN_POINT('Ctrl Pts',(31.5663345532781,2.82183813285582,5.70975721868114));
#63929=CARTESIAN_POINT('Ctrl Pts',(31.5328112499588,3.66766914258312,5.10167712719961));
#63930=CARTESIAN_POINT('Ctrl Pts',(31.4992879466396,4.5135001523104,4.49359703571811));
#63931=CARTESIAN_POINT('Ctrl Pts',(31.4657646433203,5.20485326766293,3.67064032648515));
#63932=CARTESIAN_POINT('Ctrl Pts',(31.432241340001,5.65790222097252,2.73259014628289));
#63933=CARTESIAN_POINT('Ctrl Pts',(31.3987180366818,6.11095117428214,1.79453996608057));
#63934=CARTESIAN_POINT('Ctrl Pts',(31.3651947333625,6.32569596554878,0.741396314908916));
#63935=CARTESIAN_POINT('Ctrl Pts',(31.3316714300432,6.27609888126061,-0.299147592815625));
#63936=CARTESIAN_POINT('Ctrl Pts',(31.298148126724,6.22650179697245,-1.33969150054011));
#63937=CARTESIAN_POINT('Ctrl Pts',(31.2646248234047,5.9125628371295,-2.36763566481748));
#63938=CARTESIAN_POINT('Ctrl Pts',(31.2311015200854,5.37234696548889,-3.25834229817102));
#63939=CARTESIAN_POINT('Ctrl Pts',(31.1975782167662,4.83213109384825,-4.14904893152461));
#63940=CARTESIAN_POINT('Ctrl Pts',(31.1640549134469,4.06563831040993,-4.90251803395436));
#63941=CARTESIAN_POINT('Ctrl Pts',(31.1305316101276,3.16580553525635,-5.42739180109455));
#63942=CARTESIAN_POINT('Ctrl Pts',(31.0970083068084,2.26597276010281,-5.95226556823471));
#63943=CARTESIAN_POINT('Ctrl Pts',(31.0634850034891,1.23279999323403,-6.24854400008536));
#63944=CARTESIAN_POINT('Ctrl Pts',(31.0299617001698,0.191558987940454,-6.28030346430707));
#63945=CARTESIAN_POINT('Ctrl Pts',(30.9964383968505,-0.849682017353119,
-6.31206292852878));
#63946=CARTESIAN_POINT('Ctrl Pts',(30.9629150935313,-1.89899126107148,-6.07930342512155));
#63947=CARTESIAN_POINT('Ctrl Pts',(30.929391790212,-2.82914044905153,-5.6102469436905));
#63948=CARTESIAN_POINT('Ctrl Pts',(30.8958684868928,-3.75928963703158,-5.14119046225945));
#63949=CARTESIAN_POINT('Ctrl Pts',(30.8623451835735,-4.57027876927331,-4.43583700280456));
#63950=CARTESIAN_POINT('Ctrl Pts',(30.8288218802542,-5.16377576255377,-3.5797103686905));
#63951=CARTESIAN_POINT('Ctrl Pts',(30.795298576935,-5.75727275583425,-2.72358373457642));
#63952=CARTESIAN_POINT('Ctrl Pts',(30.7617752736157,-6.13327761015345,-1.71668392580315));
#63953=CARTESIAN_POINT('Ctrl Pts',(30.7282519702964,-6.24619989876305,-0.681097110800348));
#63954=CARTESIAN_POINT('Ctrl Pts',(30.7209341238878,-6.27084985513186,-0.455037489442588));
#63955=CARTESIAN_POINT('Ctrl Pts',(30.7136162774791,-6.28296363680513,-0.227610900567938));
#63956=CARTESIAN_POINT('Ctrl Pts',(30.7062984310705,-6.28273062840727,-0.000159623917656282));
#63957=CARTESIAN_POINT('Ctrl Pts',(30.5200381542954,-6.2830449876847,-0.000113525223425687));
#63958=CARTESIAN_POINT('Ctrl Pts',(30.5239513854596,-6.28314691316384,-0.121725925414179));
#63959=CARTESIAN_POINT('Ctrl Pts',(30.5278646166237,-6.27968812365058,-0.243332531808624));
#63960=CARTESIAN_POINT('Ctrl Pts',(30.5317778477879,-6.27262932827603,-0.364729811397658));
#63961=CARTESIAN_POINT('Ctrl Pts',(30.5653011511072,-6.21215905997791,-1.40469848563893));
#63962=CARTESIAN_POINT('Ctrl Pts',(30.5988244544264,-5.88749304960068,-2.42930517081028));
#63963=CARTESIAN_POINT('Ctrl Pts',(30.6323477577457,-5.33799691116167,-3.31431674734011));
#63964=CARTESIAN_POINT('Ctrl Pts',(30.665871061065,-4.78850077272267,-4.19932832386993));
#63965=CARTESIAN_POINT('Ctrl Pts',(30.6993943643842,-4.01417450622188,-4.94474479175823));
#63966=CARTESIAN_POINT('Ctrl Pts',(30.7329176677035,-3.10890483819142,-5.46018472511148));
#63967=CARTESIAN_POINT('Ctrl Pts',(30.7664409710228,-2.20363517016098,-5.97562465846471));
#63968=CARTESIAN_POINT('Ctrl Pts',(30.7999642743421,-1.16742210060086,-6.2610880572829));
#63969=CARTESIAN_POINT('Ctrl Pts',(30.8334875776613,-0.125906018194264,
-6.28196260732688));
#63970=CARTESIAN_POINT('Ctrl Pts',(30.8670108809806,0.915610064212363,-6.30283715737087));
#63971=CARTESIAN_POINT('Ctrl Pts',(30.9005341842998,1.96242915946547,-6.05912285864064));
#63972=CARTESIAN_POINT('Ctrl Pts',(30.9340574876191,2.88762490283157,-5.5803699649591));
#63973=CARTESIAN_POINT('Ctrl Pts',(30.9675807909384,3.81282064619766,-5.10161707127757));
#63974=CARTESIAN_POINT('Ctrl Pts',(31.0011040942577,4.61639303767675,-4.38782558264473));
#63975=CARTESIAN_POINT('Ctrl Pts',(31.0346273975769,5.20090927067106,-3.52554240983122));
#63976=CARTESIAN_POINT('Ctrl Pts',(31.0681507008962,5.78542550366535,-2.66325923701774));
#63977=CARTESIAN_POINT('Ctrl Pts',(31.1016740042154,6.15088557817489,-1.6524843800236));
#63978=CARTESIAN_POINT('Ctrl Pts',(31.1351973075347,6.25297761746464,-0.61577385520735));
#63979=CARTESIAN_POINT('Ctrl Pts',(31.168720610854,6.35506965675439,0.42093666960893));
#63980=CARTESIAN_POINT('Ctrl Pts',(31.2022439141733,6.19379366082435,1.48358286224732));
#63981=CARTESIAN_POINT('Ctrl Pts',(31.2357672174925,5.78870427476552,2.44331932922858));
#63982=CARTESIAN_POINT('Ctrl Pts',(31.2692905208118,5.3836148887067,3.40305579620984));
#63983=CARTESIAN_POINT('Ctrl Pts',(31.3028138241311,4.73471211251909,4.25988253753397));
#63984=CARTESIAN_POINT('Ctrl Pts',(31.3363371274503,3.92067512851839,4.90990967960593));
#63985=CARTESIAN_POINT('Ctrl Pts',(31.3698604307696,3.10663814451772,5.55993682167786));
#63986=CARTESIAN_POINT('Ctrl Pts',(31.4033837340889,2.12746695270396,6.00316436449764));
#63987=CARTESIAN_POINT('Ctrl Pts',(31.4369070374081,1.10188563863521,6.18585115926985));
#63988=CARTESIAN_POINT('Ctrl Pts',(31.4704303407274,0.076304324566436,6.36853795404207));
#63989=CARTESIAN_POINT('Ctrl Pts',(31.5039536440467,-0.995687111757333,
6.29068400076671));
#63990=CARTESIAN_POINT('Ctrl Pts',(31.5374769473659,-1.98411017008232,5.96172905776895));
#63991=CARTESIAN_POINT('Ctrl Pts',(31.5710002506852,-2.97253322840731,5.63277411477118));
#63992=CARTESIAN_POINT('Ctrl Pts',(31.6045235540045,-3.87738790873352,5.05271818205102));
#63993=CARTESIAN_POINT('Ctrl Pts',(31.6380468573237,-4.58896097053383,4.29189279178638));
#63994=CARTESIAN_POINT('Ctrl Pts',(31.671570160643,-5.30053403233411,3.53106740152177));
#63995=CARTESIAN_POINT('Ctrl Pts',(31.7050934639623,-5.81882547560849,2.58947255371271));
#63996=CARTESIAN_POINT('Ctrl Pts',(31.7386167672815,-6.08099268594003,1.5812762183801));
#63997=CARTESIAN_POINT('Ctrl Pts',(31.7557572296195,-6.21503875986478,1.0657855117973));
#63998=CARTESIAN_POINT('Ctrl Pts',(31.7728976919575,-6.28212688791591,0.532883337562788));
#63999=CARTESIAN_POINT('Ctrl Pts',(31.7900381542954,-6.28215913048763,-1.08654762067814E-5));
#64000=CARTESIAN_POINT('Origin',(37.,0.,0.));
#64001=CARTESIAN_POINT('',(33.2462984310705,-6.28320205698061,4.08552788717063E-5));
#64002=CARTESIAN_POINT('',(33.0600381542954,-6.28298144306473,0.000129065751391986));
#64003=CARTESIAN_POINT('',(37.,-6.28269,-7.69407619853508E-16));
#64004=CARTESIAN_POINT('Ctrl Pts',(33.2462984310705,-6.28320205698061,4.08552788717063E-5));
#64005=CARTESIAN_POINT('Ctrl Pts',(33.2450321937941,-6.28321600959046,0.0393891522380337));
#64006=CARTESIAN_POINT('Ctrl Pts',(33.2437659565178,-6.28285406172601,0.0787371917293483));
#64007=CARTESIAN_POINT('Ctrl Pts',(33.2424997192415,-6.28211461241435,0.118078135732937));
#64008=CARTESIAN_POINT('Ctrl Pts',(33.2089764159222,-6.26253788376541,1.15961941977684));
#64009=CARTESIAN_POINT('Ctrl Pts',(33.1754531126029,-5.97836590406743,2.19618739214224));
#64010=CARTESIAN_POINT('Ctrl Pts',(33.1419298092837,-5.4640544035471,3.10209863233354));
#64011=CARTESIAN_POINT('Ctrl Pts',(33.1084065059644,-4.94974290302676,4.00800987252487));
#64012=CARTESIAN_POINT('Ctrl Pts',(33.0748832026451,-4.20529188168404,4.7832643805421));
#64013=CARTESIAN_POINT('Ctrl Pts',(33.0413598993259,-3.32096570543438,5.3338628809688));
#64014=CARTESIAN_POINT('Ctrl Pts',(33.0078365960066,-2.43663952918469,5.88446138139552));
#64015=CARTESIAN_POINT('Ctrl Pts',(32.9743132926873,-1.41243819802804,6.21040387423169));
#64016=CARTESIAN_POINT('Ctrl Pts',(32.940789989368,-0.37254568253624,6.27216997251124));
#64017=CARTESIAN_POINT('Ctrl Pts',(32.9072666860488,0.667346832955501,6.3339360707908));
#64018=CARTESIAN_POINT('Ctrl Pts',(32.8737433827295,1.72293053278239,6.13152577451377));
#64019=CARTESIAN_POINT('Ctrl Pts',(32.8402200794102,2.66621634767878,5.68948124498346));
#64020=CARTESIAN_POINT('Ctrl Pts',(32.806696776091,3.60950216257517,5.24743671545314));
#64021=CARTESIAN_POINT('Ctrl Pts',(32.7731734727717,4.44049009254105,4.56575795266955));
#64022=CARTESIAN_POINT('Ctrl Pts',(32.7396501694525,5.05842320873721,3.72709821321586));
#64023=CARTESIAN_POINT('Ctrl Pts',(32.7061268661332,5.67635632493336,2.88843847376217));
#64024=CARTESIAN_POINT('Ctrl Pts',(32.6726035628139,6.08123462735978,1.89279775763838));
#64025=CARTESIAN_POINT('Ctrl Pts',(32.6390802594947,6.22396679611268,0.86089707313647));
#64026=CARTESIAN_POINT('Ctrl Pts',(32.6055569561754,6.36669896486559,-0.171003611365471));
#64027=CARTESIAN_POINT('Ctrl Pts',(32.5720336528561,6.24728499994497,-1.23916426424554));
#64028=CARTESIAN_POINT('Ctrl Pts',(32.5385103495368,5.88020379319996,-2.21407086609369));
#64029=CARTESIAN_POINT('Ctrl Pts',(32.5049870462176,5.51312258645496,-3.18897746794185));
#64030=CARTESIAN_POINT('Ctrl Pts',(32.4714637428983,4.89837413788557,-4.07063001875808));
#64031=CARTESIAN_POINT('Ctrl Pts',(32.4379404395791,4.11049643228429,-4.75212852623183));
#64032=CARTESIAN_POINT('Ctrl Pts',(32.4044171362598,3.322618726683,-5.43362703370557));
#64033=CARTESIAN_POINT('Ctrl Pts',(32.3708938329405,2.36161176404983,-5.91497149783683));
#64034=CARTESIAN_POINT('Ctrl Pts',(32.3373705296213,1.34399722497286,-6.13779910952724));
#64035=CARTESIAN_POINT('Ctrl Pts',(32.303847226302,0.326382685895892,-6.36062672121764));
#64036=CARTESIAN_POINT('Ctrl Pts',(32.2703239229827,-0.747839429624867,
-6.32493748046721));
#64037=CARTESIAN_POINT('Ctrl Pts',(32.2368006196634,-1.74842015244313,-6.03505869235576));
#64038=CARTESIAN_POINT('Ctrl Pts',(32.2032773163442,-2.74900087526137,-5.74517990424432));
#64039=CARTESIAN_POINT('Ctrl Pts',(32.1697540130249,-3.67594020537711,-5.20111156877187));
#64040=CARTESIAN_POINT('Ctrl Pts',(32.1362307097056,-4.41684714798181,-4.46882173743965));
#64041=CARTESIAN_POINT('Ctrl Pts',(32.1027074063864,-5.1577540905865,-3.73653190610742));
#64042=CARTESIAN_POINT('Ctrl Pts',(32.0691841030671,-5.71262864568015,-2.81602057891541));
#64043=CARTESIAN_POINT('Ctrl Pts',(32.0356607997479,-6.01419251228362,-1.81889935808437));
#64044=CARTESIAN_POINT('Ctrl Pts',(32.0158733435221,-6.1921935211003,-1.23033884777023));
#64045=CARTESIAN_POINT('Ctrl Pts',(31.9960858872963,-6.28193942483286,-0.615086948103771));
#64046=CARTESIAN_POINT('Ctrl Pts',(31.9762984310705,-6.28222702961327,8.28361765500829E-5));
#64047=CARTESIAN_POINT('Ctrl Pts',(31.7900381542954,-6.28215913048763,-1.08654762067814E-5));
#64048=CARTESIAN_POINT('Ctrl Pts',(31.8064209952767,-6.28218994791338,-0.509350743019272));
#64049=CARTESIAN_POINT('Ctrl Pts',(31.822803836258,-6.22096171370733,-1.01868333845915));
#64050=CARTESIAN_POINT('Ctrl Pts',(31.8391866772393,-6.09838890969872,-1.51279847677552));
#64051=CARTESIAN_POINT('Ctrl Pts',(31.8727099805586,-5.84757494573717,-2.5238790137423));
#64052=CARTESIAN_POINT('Ctrl Pts',(31.9062332838779,-5.33990404042537,-3.47124226481969));
#64053=CARTESIAN_POINT('Ctrl Pts',(31.9397565871971,-4.63693107252356,-4.24002084357331));
#64054=CARTESIAN_POINT('Ctrl Pts',(31.9732798905164,-3.93395810462173,-5.00879942232696));
#64055=CARTESIAN_POINT('Ctrl Pts',(32.0068031938357,-3.03568307412986,-5.59899332875682));
#64056=CARTESIAN_POINT('Ctrl Pts',(32.040326497155,-2.05102144186464,-5.93904180573619));
#64057=CARTESIAN_POINT('Ctrl Pts',(32.0738498004742,-1.06635980959946,-6.27909028271555));
#64058=CARTESIAN_POINT('Ctrl Pts',(32.1073731037935,0.00468842443907186,
-6.36899333024443));
#64059=CARTESIAN_POINT('Ctrl Pts',(32.1408964071127,1.0322591228683,-6.19785024250553));
#64060=CARTESIAN_POINT('Ctrl Pts',(32.174419710432,2.05982982129758,-6.02670715476662));
#64061=CARTESIAN_POINT('Ctrl Pts',(32.2079430137513,3.04392298411755,-5.59451793175988));
#64062=CARTESIAN_POINT('Ctrl Pts',(32.2414663170705,3.86521773890408,-4.95368533075446));
#64063=CARTESIAN_POINT('Ctrl Pts',(32.2749896203898,4.68651249369057,-4.31285272974907));
#64064=CARTESIAN_POINT('Ctrl Pts',(32.3085129237091,5.34500884044363,-3.46337675074502));
#64065=CARTESIAN_POINT('Ctrl Pts',(32.3420362270284,5.76086438054576,-2.5082559905699));
#64066=CARTESIAN_POINT('Ctrl Pts',(32.3755595303476,6.17671992064788,-1.55313523039478));
#64067=CARTESIAN_POINT('Ctrl Pts',(32.4090828336669,6.34993465409905,-0.492369689048594));
#64068=CARTESIAN_POINT('Ctrl Pts',(32.4426061369861,6.25950636902242,0.545423268149143));
#64069=CARTESIAN_POINT('Ctrl Pts',(32.4761294403054,6.16907808394578,1.58321622534691));
#64070=CARTESIAN_POINT('Ctrl Pts',(32.5096527436247,5.81500678034133,2.59803659839622));
#64071=CARTESIAN_POINT('Ctrl Pts',(32.543176046944,5.24022345137374,3.46683785385809));
#64072=CARTESIAN_POINT('Ctrl Pts',(32.5766993502632,4.66544012240614,4.33563910931996));
#64073=CARTESIAN_POINT('Ctrl Pts',(32.6102226535825,3.86994476807541,5.05842124719439));
#64074=CARTESIAN_POINT('Ctrl Pts',(32.6437459569018,2.95019085770154,5.54754724435989));
#64075=CARTESIAN_POINT('Ctrl Pts',(32.677269260221,2.03043694732766,6.03667324152539));
#64076=CARTESIAN_POINT('Ctrl Pts',(32.7107925635403,0.98642448091063,6.29214309798196));
#64077=CARTESIAN_POINT('Ctrl Pts',(32.7443158668595,-0.0552604793544102,
6.28298120359215));
#64078=CARTESIAN_POINT('Ctrl Pts',(32.7778391701788,-1.09694543961945,6.27381930920233));
#64079=CARTESIAN_POINT('Ctrl Pts',(32.8113624734981,-2.1363028937325,6.00002566396611));
#64080=CARTESIAN_POINT('Ctrl Pts',(32.8448857768174,-3.04731119773671,5.49479762952369));
#64081=CARTESIAN_POINT('Ctrl Pts',(32.8784090801366,-3.9583195017409,4.98956959508127));
#64082=CARTESIAN_POINT('Ctrl Pts',(32.9119323834559,-4.74097865563625,4.25290717143266));
#64083=CARTESIAN_POINT('Ctrl Pts',(32.9454556867752,-5.30039157388068,3.37413036037516));
#64084=CARTESIAN_POINT('Ctrl Pts',(32.9789789900944,-5.8598044921251,2.49535354931767));
#64085=CARTESIAN_POINT('Ctrl Pts',(33.0125022934137,-6.19597117471861,1.47446235085129));
#64086=CARTESIAN_POINT('Ctrl Pts',(33.0460255967329,-6.26813155608769,0.435239383383873));
#64087=CARTESIAN_POINT('Ctrl Pts',(33.0506964492538,-6.27818577109184,0.290442876575982));
#64088=CARTESIAN_POINT('Ctrl Pts',(33.0553673017746,-6.28311476046551,0.145290490185292));
#64089=CARTESIAN_POINT('Ctrl Pts',(33.0600381542954,-6.28298144306473,0.000129065751391986));
#64090=CARTESIAN_POINT('Origin',(37.,0.,0.));
#64091=CARTESIAN_POINT('',(34.5162984310705,-6.28238146749754,-0.000135238015052663));
#64092=CARTESIAN_POINT('',(34.3300381542954,-6.28268367435609,-0.00016098647794763));
#64093=CARTESIAN_POINT('',(37.,-6.28269,-7.69407619853508E-16));
#64094=CARTESIAN_POINT('Ctrl Pts',(34.5162984310705,-6.28238146749754,-0.000135238015052663));
#64095=CARTESIAN_POINT('Ctrl Pts',(34.493978500292,-6.28183396867322,0.693717463406439));
#64096=CARTESIAN_POINT('Ctrl Pts',(34.4716585695136,-6.16718126832808,1.38774665406166));
#64097=CARTESIAN_POINT('Ctrl Pts',(34.4493386387351,-5.94159291191415,2.04361936738219));
#64098=CARTESIAN_POINT('Ctrl Pts',(34.4158153354158,-5.6027716596253,3.02870395952131));
#64099=CARTESIAN_POINT('Ctrl Pts',(34.3822920320965,-5.01369752830549,3.92771371652569));
#64100=CARTESIAN_POINT('Ctrl Pts',(34.3487687287773,-4.24579550283129,4.6316440923052));
#64101=CARTESIAN_POINT('Ctrl Pts',(34.315245425458,-3.47789347735709,5.33557446808473));
#64102=CARTESIAN_POINT('Ctrl Pts',(34.2817221221387,-2.53116355772858,5.84442546263936));
#64103=CARTESIAN_POINT('Ctrl Pts',(34.2481988188195,-1.52039633921443,6.09649911189622));
#64104=CARTESIAN_POINT('Ctrl Pts',(34.2146755155002,-0.509629120700321,
6.34857276115307));
#64105=CARTESIAN_POINT('Ctrl Pts',(34.181152212181,0.565175396699438,6.34386906511209));
#64106=CARTESIAN_POINT('Ctrl Pts',(34.1476289088617,1.57369762786122,6.08295834489372));
#64107=CARTESIAN_POINT('Ctrl Pts',(34.1141056055424,2.58221985902306,5.82204762467532));
#64108=CARTESIAN_POINT('Ctrl Pts',(34.0805823022231,3.52445980394702,5.3049298802795));
#64109=CARTESIAN_POINT('Ctrl Pts',(34.0470589989039,4.28617127486464,4.59430541563938));
#64110=CARTESIAN_POINT('Ctrl Pts',(34.0135356955846,5.04788274578218,3.88368095099931));
#64111=CARTESIAN_POINT('Ctrl Pts',(33.9800123922653,5.62906574269343,2.97954976611496));
#64112=CARTESIAN_POINT('Ctrl Pts',(33.9464890889461,5.95925207737237,1.99153737800253));
#64113=CARTESIAN_POINT('Ctrl Pts',(33.9129657856268,6.28943841205133,1.00352498989004));
#64114=CARTESIAN_POINT('Ctrl Pts',(33.8794424823075,6.36862808449797,-0.0683686014504739));
#64115=CARTESIAN_POINT('Ctrl Pts',(33.8459191789883,6.18721938101251,-1.09417675942749));
#64116=CARTESIAN_POINT('Ctrl Pts',(33.812395875669,6.00581067752706,-2.11998491740448));
#64117=CARTESIAN_POINT('Ctrl Pts',(33.7788725723497,5.56380359810951,-3.0997076420179));
#64118=CARTESIAN_POINT('Ctrl Pts',(33.7453492690305,4.91479131089306,-3.91455397459509));
#64119=CARTESIAN_POINT('Ctrl Pts',(33.7118259657112,4.26577902367657,-4.72940030717232));
#64120=CARTESIAN_POINT('Ctrl Pts',(33.6783026623919,3.40976152866115,-5.3793702477133));
#64121=CARTESIAN_POINT('Ctrl Pts',(33.6447793590727,2.45053057867523,-5.78565522068381));
#64122=CARTESIAN_POINT('Ctrl Pts',(33.6112560557534,1.49129962868933,-6.1919401936543));
#64123=CARTESIAN_POINT('Ctrl Pts',(33.5777327524341,0.428855223732931,-6.35454019905433));
#64124=CARTESIAN_POINT('Ctrl Pts',(33.5442094491149,-0.607981709384303,
-6.25374005621454));
#64125=CARTESIAN_POINT('Ctrl Pts',(33.5106861457956,-1.64481864250154,-6.15293991337474));
#64126=CARTESIAN_POINT('Ctrl Pts',(33.4771628424763,-2.65604810377963,-5.7887396222951));
#64127=CARTESIAN_POINT('Ctrl Pts',(33.4436395391571,-3.51905895628623,-5.20529831151201));
#64128=CARTESIAN_POINT('Ctrl Pts',(33.4101162358378,-4.38206980879284,-4.62185700072892));
#64129=CARTESIAN_POINT('Ctrl Pts',(33.3765929325185,-5.09686205252798,-3.81917467024236));
#64130=CARTESIAN_POINT('Ctrl Pts',(33.3430696291993,-5.57676743559559,-2.89457620713786));
#64131=CARTESIAN_POINT('Ctrl Pts',(33.3108125631563,-6.03854590320481,-2.00490154102544));
#64132=CARTESIAN_POINT('Ctrl Pts',(33.2785554971134,-6.28284661786531,-1.00234679939667));
#64133=CARTESIAN_POINT('Ctrl Pts',(33.2462984310705,-6.28320205698061,4.08552788717063E-5));
#64134=CARTESIAN_POINT('Ctrl Pts',(33.0600381542954,-6.28298144306473,0.000129065751391986));
#64135=CARTESIAN_POINT('Ctrl Pts',(33.0888906050939,-6.28215792450375,-0.896551537551931));
#64136=CARTESIAN_POINT('Ctrl Pts',(33.1177430558923,-6.08817246169332,-1.79357700458562));
#64137=CARTESIAN_POINT('Ctrl Pts',(33.1465955066908,-5.71585503173087,-2.60919676941154));
#64138=CARTESIAN_POINT('Ctrl Pts',(33.18011881001,-5.2832640458603,-3.55685521827101));
#64139=CARTESIAN_POINT('Ctrl Pts',(33.2136421133293,-4.60992799397454,-4.39461737952143));
#64140=CARTESIAN_POINT('Ctrl Pts',(33.2471654166485,-3.77748858255121,-5.02090495169605));
#64141=CARTESIAN_POINT('Ctrl Pts',(33.2806887199678,-2.94504917112791,-5.64719252387065));
#64142=CARTESIAN_POINT('Ctrl Pts',(33.3142120232871,-1.95350640016708,-6.06200550696946));
#64143=CARTESIAN_POINT('Ctrl Pts',(33.3477353266064,-0.923084403873464,
-6.2150480053332));
#64144=CARTESIAN_POINT('Ctrl Pts',(33.3812586299256,0.107337592420149,-6.36809050369695));
#64145=CARTESIAN_POINT('Ctrl Pts',(33.4147819332449,1.17663881404652,-6.25936251732563));
#64146=CARTESIAN_POINT('Ctrl Pts',(33.4483052365642,2.15516694812606,-5.90204726776868));
#64147=CARTESIAN_POINT('Ctrl Pts',(33.4818285398834,3.13369508220566,-5.5447320182117));
#64148=CARTESIAN_POINT('Ctrl Pts',(33.5153518432027,4.02145012873839,-4.93882950546908));
#64149=CARTESIAN_POINT('Ctrl Pts',(33.548875146522,4.71079217043467,-4.15780514842171));
#64150=CARTESIAN_POINT('Ctrl Pts',(33.5823984498412,5.40013421213092,-3.37678079137438));
#64151=CARTESIAN_POINT('Ctrl Pts',(33.6159217531605,5.89106324899072,-2.42063459002235));
#64152=CARTESIAN_POINT('Ctrl Pts',(33.6494450564798,6.12405434659775,-1.40529885974049));
#64153=CARTESIAN_POINT('Ctrl Pts',(33.682968359799,6.35704544420478,-0.389963129458594));
#64154=CARTESIAN_POINT('Ctrl Pts',(33.7164916631183,6.332098602559,0.684562129753203));
#64155=CARTESIAN_POINT('Ctrl Pts',(33.7500149664376,6.05223861547249,1.6879911927064));
#64156=CARTESIAN_POINT('Ctrl Pts',(33.7835382697568,5.77237862838598,2.69142025565957));
#64157=CARTESIAN_POINT('Ctrl Pts',(33.8170615730761,5.23760549585876,3.62375312235421));
#64158=CARTESIAN_POINT('Ctrl Pts',(33.8505848763954,4.51276023003573,4.37194483399306));
#64159=CARTESIAN_POINT('Ctrl Pts',(33.8841081797146,3.78791496421269,5.1201365456319));
#64160=CARTESIAN_POINT('Ctrl Pts',(33.9176314830339,2.87299756509385,5.68418710221493));
#64161=CARTESIAN_POINT('Ctrl Pts',(33.9511547863532,1.87894137352877,5.99570561653193));
#64162=CARTESIAN_POINT('Ctrl Pts',(33.9846780896725,0.884885181963638,6.30722413084894));
#64163=CARTESIAN_POINT('Ctrl Pts',(34.0182013929917,-0.188309802047724,
6.36621060289987));
#64164=CARTESIAN_POINT('Ctrl Pts',(34.051724696311,-1.21051914861245,6.16551294833717));
#64165=CARTESIAN_POINT('Ctrl Pts',(34.0852479996302,-2.23272849517715,5.96481529377447));
#64166=CARTESIAN_POINT('Ctrl Pts',(34.1187713029495,-3.2039522042952,5.50443351259817));
#64167=CARTESIAN_POINT('Ctrl Pts',(34.1522946062688,-4.00642981926466,4.84018869762095));
#64168=CARTESIAN_POINT('Ctrl Pts',(34.185817909588,-4.80890743423408,4.17594388264377));
#64169=CARTESIAN_POINT('Ctrl Pts',(34.2193412129073,-5.44263895505492,3.30783603386572));
#64170=CARTESIAN_POINT('Ctrl Pts',(34.2528645162266,-5.8307847075948,2.34112285430504));
#64171=CARTESIAN_POINT('Ctrl Pts',(34.2785890622495,-6.12863343627561,1.5993028301337));
#64172=CARTESIAN_POINT('Ctrl Pts',(34.3043136082725,-6.28186993566055,0.799419438509327));
#64173=CARTESIAN_POINT('Ctrl Pts',(34.3300381542954,-6.28268367435609,-0.00016098647794763));
#64174=CARTESIAN_POINT('Origin',(37.,0.,0.));
#64175=CARTESIAN_POINT('',(35.7862984310705,-6.28249223374509,0.000152535273694049));
#64176=CARTESIAN_POINT('',(35.6000381542954,-6.28225017164793,9.44259478526101E-5));
#64177=CARTESIAN_POINT('',(37.,-6.28269,-7.69407619853508E-16));
#64178=CARTESIAN_POINT('Ctrl Pts',(35.7862984310705,-6.28249223374509,0.000152535273694049));
#64179=CARTESIAN_POINT('Ctrl Pts',(35.7764481101091,-6.28277209891908,0.306350889573917));
#64180=CARTESIAN_POINT('Ctrl Pts',(35.7665977891478,-6.26078533904793,0.612509400593861));
#64181=CARTESIAN_POINT('Ctrl Pts',(35.7567474681865,-6.21619340497281,0.915339282244856));
#64182=CARTESIAN_POINT('Ctrl Pts',(35.7232241648672,-6.06443500669699,1.94595117972385));
#64183=CARTESIAN_POINT('Ctrl Pts',(35.689700861548,-5.65085788080548,2.93801006724945));
#64184=CARTESIAN_POINT('Ctrl Pts',(35.6561775582287,-5.0256080758031,3.77122923170559));
#64185=CARTESIAN_POINT('Ctrl Pts',(35.6226542549094,-4.40035827080072,4.60444839616172));
#64186=CARTESIAN_POINT('Ctrl Pts',(35.5891309515902,-3.56343578668749,5.27882783754836));
#64187=CARTESIAN_POINT('Ctrl Pts',(35.5556076482709,-2.61631711443867,5.71259933885997));
#64188=CARTESIAN_POINT('Ctrl Pts',(35.5220843449516,-1.66919844218988,6.14637084017157));
#64189=CARTESIAN_POINT('Ctrl Pts',(35.4885610416324,-0.611883581805538,
6.33953440140814));
#64190=CARTESIAN_POINT('Ctrl Pts',(35.4550377383131,0.427428494976258,6.26866902391013));
#64191=CARTESIAN_POINT('Ctrl Pts',(35.4215144349938,1.46674057175808,6.19780364641211));
#64192=CARTESIAN_POINT('Ctrl Pts',(35.3879911316745,2.48804986493734,5.8629093301795));
#64193=CARTESIAN_POINT('Ctrl Pts',(35.3544678283553,3.36752306230223,5.30459186691217));
#64194=CARTESIAN_POINT('Ctrl Pts',(35.320944525036,4.24699625966712,4.74627440364483));
#64195=CARTESIAN_POINT('Ctrl Pts',(35.2874212217168,4.98463336121762,3.96453379334279));
#64196=CARTESIAN_POINT('Ctrl Pts',(35.2538979183975,5.49099618588033,3.05415574853278));
#64197=CARTESIAN_POINT('Ctrl Pts',(35.2203746150782,5.99735901054301,2.14377770372282));
#64198=CARTESIAN_POINT('Ctrl Pts',(35.186851311759,6.27244755831792,1.10476222440484));
#64199=CARTESIAN_POINT('Ctrl Pts',(35.1533280084397,6.2829074611894,0.0630894902391272));
#64200=CARTESIAN_POINT('Ctrl Pts',(35.1198047051204,6.29336736406087,-0.978583243926678));
#64201=CARTESIAN_POINT('Ctrl Pts',(35.0862814018011,6.03919862202889,-2.0229132329403));
#64202=CARTESIAN_POINT('Ctrl Pts',(35.0527580984819,5.55121908566695,-2.94327591512843));
#64203=CARTESIAN_POINT('Ctrl Pts',(35.0192347951626,5.06323954930503,-3.86363859731651));
#64204=CARTESIAN_POINT('Ctrl Pts',(34.9857114918434,4.3414492186132,-4.6600339726791));
#64205=CARTESIAN_POINT('Ctrl Pts',(34.9521881885241,3.4733648605189,-5.2358994447335));
#64206=CARTESIAN_POINT('Ctrl Pts',(34.9186648852048,2.6052805024246,-5.81176491678791));
#64207=CARTESIAN_POINT('Ctrl Pts',(34.8851415818855,1.59090211692786,-6.1671004855341));
#64208=CARTESIAN_POINT('Ctrl Pts',(34.8516182785663,0.553222646667127,-6.25882186620315));
#64209=CARTESIAN_POINT('Ctrl Pts',(34.818094975247,-0.484456823593634,-6.3505432468722));
#64210=CARTESIAN_POINT('Ctrl Pts',(34.7845716719278,-1.54543737861837,-6.17865043946409));
#64211=CARTESIAN_POINT('Ctrl Pts',(34.7510483686085,-2.50107558277158,-5.76398537289191));
#64212=CARTESIAN_POINT('Ctrl Pts',(34.7175250652892,-3.45671378692479,-5.34932030631973));
#64213=CARTESIAN_POINT('Ctrl Pts',(34.68400176197,-4.30700964020647,-4.6918829805835));
#64214=CARTESIAN_POINT('Ctrl Pts',(34.6504784586507,-4.94886513638575,-3.87138738845827));
#64215=CARTESIAN_POINT('Ctrl Pts',(34.6169551553314,-5.590720632565,-3.05089179633308));
#64216=CARTESIAN_POINT('Ctrl Pts',(34.5834318520122,-6.02413577164186,-2.06733793781892));
#64217=CARTESIAN_POINT('Ctrl Pts',(34.5499085486929,-6.19655915455137,-1.03998129492494));
#64218=CARTESIAN_POINT('Ctrl Pts',(34.5387051761521,-6.25418245542611,-0.696642242296477));
#64219=CARTESIAN_POINT('Ctrl Pts',(34.5275018036113,-6.28265628166948,-0.348410973259297));
#64220=CARTESIAN_POINT('Ctrl Pts',(34.5162984310705,-6.28238146749754,-0.000135238015052663));
#64221=CARTESIAN_POINT('Ctrl Pts',(34.3300381542954,-6.28268367435609,-0.00016098647794763));
#64222=CARTESIAN_POINT('Ctrl Pts',(34.3378369115917,-6.28293037066643,-0.242565018323604));
#64223=CARTESIAN_POINT('Ctrl Pts',(34.345635668888,-6.26916812957207,-0.484941204979767));
#64224=CARTESIAN_POINT('Ctrl Pts',(34.3534344261844,-6.24117932363999,-0.725663265874277));
#64225=CARTESIAN_POINT('Ctrl Pts',(34.3869577295036,-6.12086820288638,-1.7604176961495));
#64226=CARTESIAN_POINT('Ctrl Pts',(34.4204810328229,-5.73768597712025,-2.76460804635658));
#64227=CARTESIAN_POINT('Ctrl Pts',(34.4540043361422,-5.13809332628862,-3.61647666875083));
#64228=CARTESIAN_POINT('Ctrl Pts',(34.4875276394615,-4.538500675457,-4.46834529114505));
#64229=CARTESIAN_POINT('Ctrl Pts',(34.5210509427807,-3.72249759955989,-5.16789218572647));
#64230=CARTESIAN_POINT('Ctrl Pts',(34.5545742461,-2.78902412033039,-5.63029759262208));
#64231=CARTESIAN_POINT('Ctrl Pts',(34.5880975494192,-1.85555064110086,-6.09270299951771));
#64232=CARTESIAN_POINT('Ctrl Pts',(34.6216208527385,-0.804606758538935,
-6.31796691872752));
#64233=CARTESIAN_POINT('Ctrl Pts',(34.6551441560578,0.236381033936069,-6.27877619700416));
#64234=CARTESIAN_POINT('Ctrl Pts',(34.688667459377,1.2773688264111,-6.23958547528079));
#64235=CARTESIAN_POINT('Ctrl Pts',(34.7221907626963,2.30840052879923,-5.93594011262423));
#64236=CARTESIAN_POINT('Ctrl Pts',(34.7557140660156,3.20446399095668,-5.40465697856327));
#64237=CARTESIAN_POINT('Ctrl Pts',(34.7892373693349,4.10052745311406,-4.87337384450235));
#64238=CARTESIAN_POINT('Ctrl Pts',(34.8227606726541,4.86162267504081,-4.11445293903707));
#64239=CARTESIAN_POINT('Ctrl Pts',(34.8562839759734,5.3954671886646,-3.21991309530465));
#64240=CARTESIAN_POINT('Ctrl Pts',(34.8898072792927,5.92931170228845,-2.32537325157215));
#64241=CARTESIAN_POINT('Ctrl Pts',(34.9233305826119,6.23590550760931,-1.29521446957246));
#64242=CARTESIAN_POINT('Ctrl Pts',(34.9568538859312,6.27807423769439,-0.254343058227982));
#64243=CARTESIAN_POINT('Ctrl Pts',(34.9903771892504,6.32024296777946,0.786528353116469));
#64244=CARTESIAN_POINT('Ctrl Pts',(35.0239004925697,6.0979866226288,1.83811239380565));
#64245=CARTESIAN_POINT('Ctrl Pts',(35.057423795889,5.63825368842958,2.77290495152301));
#64246=CARTESIAN_POINT('Ctrl Pts',(35.0909470992083,5.17852075423038,3.70769750924034));
#64247=CARTESIAN_POINT('Ctrl Pts',(35.1244704025275,4.48131123098262,4.52569858398577));
#64248=CARTESIAN_POINT('Ctrl Pts',(35.1579937058468,3.63116147329114,5.12772589752581));
#64249=CARTESIAN_POINT('Ctrl Pts',(35.191517009166,2.78101171559963,5.72975321106586));
#64250=CARTESIAN_POINT('Ctrl Pts',(35.2250403124853,1.77792172346437,6.1158067634005));
#64251=CARTESIAN_POINT('Ctrl Pts',(35.2585636158046,0.743515726687463,6.23907772747215));
#64252=CARTESIAN_POINT('Ctrl Pts',(35.2920869191239,-0.290890270089445,
6.3623486915438));
#64253=CARTESIAN_POINT('Ctrl Pts',(35.3256102224431,-1.35661227150802,6.22283706735246));
#64254=CARTESIAN_POINT('Ctrl Pts',(35.3591335257624,-2.32443194359826,5.83745857928351));
#64255=CARTESIAN_POINT('Ctrl Pts',(35.3926568290817,-3.29225161568848,5.45208009121458));
#64256=CARTESIAN_POINT('Ctrl Pts',(35.4261801324009,-4.1621689584504,4.82083473926805));
#64257=CARTESIAN_POINT('Ctrl Pts',(35.4597034357202,-4.82870686849902,4.02026075067041));
#64258=CARTESIAN_POINT('Ctrl Pts',(35.4932267390395,-5.49524477854764,3.21968676207277));
#64259=CARTESIAN_POINT('Ctrl Pts',(35.5267500423587,-5.95840325588298,2.249784136824));
#64260=CARTESIAN_POINT('Ctrl Pts',(35.560273345678,-6.16202453447816,1.22815315077553));
#64261=CARTESIAN_POINT('Ctrl Pts',(35.5735282818838,-6.24253530730445,0.824205681250167));
#64262=CARTESIAN_POINT('Ctrl Pts',(35.5867832180896,-6.28247082274164,0.412171156905869));
#64263=CARTESIAN_POINT('Ctrl Pts',(35.6000381542954,-6.28225017164793,9.44259478526101E-5));
#64264=CARTESIAN_POINT('Origin',(37.,0.,0.));
#64265=CARTESIAN_POINT('',(37.0562984310705,-6.28313695873549,-8.10514889743041E-5));
#64266=CARTESIAN_POINT('',(36.8700381542954,-6.28321544720413,2.5547018683295E-5));
#64267=CARTESIAN_POINT('',(37.,-6.28269,-7.69407619853508E-16));
#64268=CARTESIAN_POINT('Ctrl Pts',(37.0562984310705,-6.28313695873549,-8.10514889743041E-5));
#64269=CARTESIAN_POINT('Ctrl Pts',(37.025394416607,-6.28251941297775,0.960289475135647));
#64270=CARTESIAN_POINT('Ctrl Pts',(36.9944904021436,-6.05897203089142,1.92093764266805));
#64271=CARTESIAN_POINT('Ctrl Pts',(36.9635863876801,-5.63376854407137,2.78200619005063));
#64272=CARTESIAN_POINT('Ctrl Pts',(36.9300630843609,-5.17252667279488,3.7160551346214));
#64273=CARTESIAN_POINT('Ctrl Pts',(36.8965397810416,-4.47399712145521,4.53292926279806));
#64274=CARTESIAN_POINT('Ctrl Pts',(36.8630164777223,-3.62287629749518,5.13358293813353));
#64275=CARTESIAN_POINT('Ctrl Pts',(36.829493174403,-2.77175547353512,5.73423661346902));
#64276=CARTESIAN_POINT('Ctrl Pts',(36.7959698710837,-1.76804337695468,6.11866983596331));
#64277=CARTESIAN_POINT('Ctrl Pts',(36.7624465677645,-0.733439667452159,
6.24027024285453));
#64278=CARTESIAN_POINT('Ctrl Pts',(36.7289232644452,0.30116404205033,6.36187064974575));
#64279=CARTESIAN_POINT('Ctrl Pts',(36.695399961126,1.3666593644749,6.22063824103392));
#64280=CARTESIAN_POINT('Ctrl Pts',(36.6618766578067,2.33385545058203,5.83369738548689));
#64281=CARTESIAN_POINT('Ctrl Pts',(36.6283533544875,3.30105153668919,5.44675652993986));
#64282=CARTESIAN_POINT('Ctrl Pts',(36.5948300511682,4.16994838647891,4.81410722755762));
#64283=CARTESIAN_POINT('Ctrl Pts',(36.5613067478489,4.83519263089985,4.01245793395268));
#64284=CARTESIAN_POINT('Ctrl Pts',(36.5277834445296,5.5004368753208,3.21080864034775));
#64285=CARTESIAN_POINT('Ctrl Pts',(36.4942601412104,5.96202851437296,2.24015935552012));
#64286=CARTESIAN_POINT('Ctrl Pts',(36.4607368378911,6.16399976049693,1.21820088747378));
#64287=CARTESIAN_POINT('Ctrl Pts',(36.4272135345719,6.36597100662089,0.196242419427446));
#64288=CARTESIAN_POINT('Ctrl Pts',(36.3936902312526,6.30832185981666,-0.877025231837599));
#64289=CARTESIAN_POINT('Ctrl Pts',(36.3601669279333,5.99804225432123,-1.87146882555525));
#64290=CARTESIAN_POINT('Ctrl Pts',(36.326643624614,5.6877626488258,-2.86591241927291));
#64291=CARTESIAN_POINT('Ctrl Pts',(36.2931203212948,5.12485258463917,-3.78153195544317));
#64292=CARTESIAN_POINT('Ctrl Pts',(36.2595970179755,4.3775646647594,-4.50730895940117));
#64293=CARTESIAN_POINT('Ctrl Pts',(36.2260737146563,3.63027674487965,-5.23308596335915));
#64294=CARTESIAN_POINT('Ctrl Pts',(36.192550411337,2.69861096930678,-5.76902043510487));
#64295=CARTESIAN_POINT('Ctrl Pts',(36.1590271080177,1.69553141232668,-6.05013055061307));
#64296=CARTESIAN_POINT('Ctrl Pts',(36.1255038046984,0.692451855346581,-6.33124066612126));
#64297=CARTESIAN_POINT('Ctrl Pts',(36.0919805013792,-0.382041483040742,
-6.35752642539192));
#64298=CARTESIAN_POINT('Ctrl Pts',(36.0584571980599,-1.39766674803318,-6.12580069142724));
#64299=CARTESIAN_POINT('Ctrl Pts',(36.0249338947406,-2.41329201302567,-5.89407495746255));
#64300=CARTESIAN_POINT('Ctrl Pts',(35.9914105914214,-3.37004920462326,-5.40433773026249));
#64301=CARTESIAN_POINT('Ctrl Pts',(35.9578872881021,-4.15193192514676,-4.71596943783516));
#64302=CARTESIAN_POINT('Ctrl Pts',(35.9243639847828,-4.9338146456702,-4.02760114540786));
#64303=CARTESIAN_POINT('Ctrl Pts',(35.8908406814636,-5.54082289511957,-3.14060178775331));
#64304=CARTESIAN_POINT('Ctrl Pts',(35.8573173781443,-5.89935718451418,-2.16251965520987));
#64305=CARTESIAN_POINT('Ctrl Pts',(35.8336443957864,-6.15254153889369,-1.47183231906614));
#64306=CARTESIAN_POINT('Ctrl Pts',(35.8099714134284,-6.28181964212573,-0.735724830331349));
#64307=CARTESIAN_POINT('Ctrl Pts',(35.7862984310705,-6.28249223374509,0.000152535273694049));
#64308=CARTESIAN_POINT('Ctrl Pts',(35.6000381542954,-6.28225017164793,9.44259478526101E-5));
#64309=CARTESIAN_POINT('Ctrl Pts',(35.6203065214089,-6.28191276999605,-0.630019693976204));
#64310=CARTESIAN_POINT('Ctrl Pts',(35.6405748885223,-6.18768209352705,-1.26023250153714));
#64311=CARTESIAN_POINT('Ctrl Pts',(35.6608432556358,-6.00105655529379,-1.86178053095313));
#64312=CARTESIAN_POINT('Ctrl Pts',(35.6943665589551,-5.69238321765922,-2.85672387978495));
#64313=CARTESIAN_POINT('Ctrl Pts',(35.7278898622743,-5.13095246253506,-3.77325123060037));
#64314=CARTESIAN_POINT('Ctrl Pts',(35.7614131655936,-4.38483752733227,-4.50023403659957));
#64315=CARTESIAN_POINT('Ctrl Pts',(35.7949364689129,-3.63872259212945,-5.22721684259882));
#64316=CARTESIAN_POINT('Ctrl Pts',(35.8284597722321,-2.70792347684797,-5.7646551037818));
#64317=CARTESIAN_POINT('Ctrl Pts',(35.8619830755514,-1.70529917358644,-6.04738466230123));
#64318=CARTESIAN_POINT('Ctrl Pts',(35.8955063788707,-0.702674870324941,
-6.33011422082064));
#64319=CARTESIAN_POINT('Ctrl Pts',(35.9290296821899,0.371774620916599,-6.35813507667651));
#64320=CARTESIAN_POINT('Ctrl Pts',(35.9625529855092,1.38777276178361,-6.12804971315688));
#64321=CARTESIAN_POINT('Ctrl Pts',(35.9960762888285,2.40377090265057,-5.89796434963727));
#64322=CARTESIAN_POINT('Ctrl Pts',(36.0295995921477,3.36131769314301,-5.4097727667422));
#64323=CARTESIAN_POINT('Ctrl Pts',(36.063122895467,4.14431099705559,-4.72266798377303));
#64324=CARTESIAN_POINT('Ctrl Pts',(36.0966461987863,4.92730430096823,-4.03556320080382));
#64325=CARTESIAN_POINT('Ctrl Pts',(36.1301695021055,5.53574411830099,-3.14954521776048));
#64326=CARTESIAN_POINT('Ctrl Pts',(36.1636928054248,5.8958573830835,-2.17204333373218));
#64327=CARTESIAN_POINT('Ctrl Pts',(36.1972161087441,6.25597064786602,-1.19454144970389));
#64328=CARTESIAN_POINT('Ctrl Pts',(36.2307394120633,6.36775736009829,-0.125555664690637));
#64329=CARTESIAN_POINT('Ctrl Pts',(36.2642627153826,6.21766342903676,0.905299954981527));
#64330=CARTESIAN_POINT('Ctrl Pts',(36.2977860187019,6.06756949797523,1.93615557465366));
#64331=CARTESIAN_POINT('Ctrl Pts',(36.3313093220211,5.65559492361991,2.92888102898471));
#64332=CARTESIAN_POINT('Ctrl Pts',(36.3648326253404,5.03169144579161,3.76310878392031));
#64333=CARTESIAN_POINT('Ctrl Pts',(36.3983559286597,4.4077879679633,4.59733653885593));
#64334=CARTESIAN_POINT('Ctrl Pts',(36.431879231979,3.57195558666201,5.27306659439609));
#64335=CARTESIAN_POINT('Ctrl Pts',(36.4654025352982,2.62553861836627,5.70836697215044));
#64336=CARTESIAN_POINT('Ctrl Pts',(36.4989258386175,1.67912165007053,6.1436673499048));
#64337=CARTESIAN_POINT('Ctrl Pts',(36.5324491419367,0.622120094780342,6.33853804987336));
#64338=CARTESIAN_POINT('Ctrl Pts',(36.565972445256,-0.417305063873974,6.26935108356007));
#64339=CARTESIAN_POINT('Ctrl Pts',(36.5994957485753,-1.45673022252826,6.20016411724678));
#64340=CARTESIAN_POINT('Ctrl Pts',(36.6330190518946,-2.47857898454668,5.86691948465166));
#64341=CARTESIAN_POINT('Ctrl Pts',(36.6665423552138,-3.35895262735287,5.3100229540436));
#64342=CARTESIAN_POINT('Ctrl Pts',(36.7000656585331,-4.23932627015908,4.75312642343553));
#64343=CARTESIAN_POINT('Ctrl Pts',(36.7335889618523,-4.97822479375304,3.9725779948145));
#64344=CARTESIAN_POINT('Ctrl Pts',(36.7671122651716,-5.48605707018151,3.06301882919158));
#64345=CARTESIAN_POINT('Ctrl Pts',(36.8006355684909,-5.99388934660998,2.15345966356866));
#64346=CARTESIAN_POINT('Ctrl Pts',(36.8341588718101,-6.27065537587296,1.11488976094384));
#64347=CARTESIAN_POINT('Ctrl Pts',(36.8676821751294,-6.28279739604637,0.0732352749950272));
#64348=CARTESIAN_POINT('Ctrl Pts',(36.8684675015181,-6.28308183844643,0.0488331822806146));
#64349=CARTESIAN_POINT('Ctrl Pts',(36.8692528279068,-6.28322105764272,0.0244293967754612));
#64350=CARTESIAN_POINT('Ctrl Pts',(36.8700381542954,-6.28321544720413,2.5547018683295E-5));
#64351=CARTESIAN_POINT('Origin',(37.,0.,0.));
#64352=CARTESIAN_POINT('',(38.3262984310705,-6.28217936372029,-4.73315304236333E-5));
#64353=CARTESIAN_POINT('',(38.1400381542954,-6.2823463260306,-0.000127106979284774));
#64354=CARTESIAN_POINT('',(37.,-6.28269,-7.69407619853508E-16));
#64355=CARTESIAN_POINT('Ctrl Pts',(38.3262984310705,-6.28217936372029,-4.73315304236333E-5));
#64356=CARTESIAN_POINT('Ctrl Pts',(38.3078640264242,-6.282027712414,0.573070045152017));
#64357=CARTESIAN_POINT('Ctrl Pts',(38.2894296217778,-6.20429023609247,1.1462277488213));
#64358=CARTESIAN_POINT('Ctrl Pts',(38.2709952171315,-6.04950488904637,1.69776236471778));
#64359=CARTESIAN_POINT('Ctrl Pts',(38.2374719138122,-5.76802489346411,2.7007381903285));
#64360=CARTESIAN_POINT('Ctrl Pts',(38.203948610493,-5.23174689377087,3.63220626945104));
#64361=CARTESIAN_POINT('Ctrl Pts',(38.1704253071737,-4.50569436660769,4.37922649840903));
#64362=CARTESIAN_POINT('Ctrl Pts',(38.1369020038545,-3.77964183944451,5.12624672736702));
#64363=CARTESIAN_POINT('Ctrl Pts',(38.1033787005352,-2.86381478481141,5.68881910616045));
#64364=CARTESIAN_POINT('Ctrl Pts',(38.0698553972159,-1.86925683889755,5.99873197599983));
#64365=CARTESIAN_POINT('Ctrl Pts',(38.0363320938967,-0.874698892983714,
6.30864484583921));
#64366=CARTESIAN_POINT('Ctrl Pts',(38.0028087905774,0.198589944210873,6.36589820672455));
#64367=CARTESIAN_POINT('Ctrl Pts',(37.9692854872581,1.22047386313528,6.16355011329118));
#64368=CARTESIAN_POINT('Ctrl Pts',(37.9357621839389,2.24235778205969,5.96120201985782));
#64369=CARTESIAN_POINT('Ctrl Pts',(37.9022388806196,3.21283678271391,5.49925247210574));
#64370=CARTESIAN_POINT('Ctrl Pts',(37.8687155773003,4.01424070397671,4.83371265387017));
#64371=CARTESIAN_POINT('Ctrl Pts',(37.8351922739811,4.81564462523956,4.16817283563458));
#64372=CARTESIAN_POINT('Ctrl Pts',(37.8016689706618,5.44797346711096,3.29904274691547));
#64373=CARTESIAN_POINT('Ctrl Pts',(37.7681456673425,5.83455762967741,2.331704036884));
#64374=CARTESIAN_POINT('Ctrl Pts',(37.7346223640233,6.22114179224384,1.36436532685259));
#64375=CARTESIAN_POINT('Ctrl Pts',(37.701099060704,6.36198127550534,0.298817995508832));
#64376=CARTESIAN_POINT('Ctrl Pts',(37.6675757573847,6.23999935273579,-0.735740801848701));
#64377=CARTESIAN_POINT('Ctrl Pts',(37.6340524540655,6.11801742996624,-1.77029959920626));
#64378=CARTESIAN_POINT('Ctrl Pts',(37.6005291507462,5.73321410116562,-2.7738698625776));
#64379=CARTESIAN_POINT('Ctrl Pts',(37.5670058474269,5.13224660432614,-3.62476912947996));
#64380=CARTESIAN_POINT('Ctrl Pts',(37.5334825441077,4.53127910748666,-4.47566839638232));
#64381=CARTESIAN_POINT('Ctrl Pts',(37.4999592407884,3.71414744260832,-5.1738966668157));
#64382=CARTESIAN_POINT('Ctrl Pts',(37.4664359374691,2.77992847235244,-5.63479406351752));
#64383=CARTESIAN_POINT('Ctrl Pts',(37.4329126341498,1.84570950209658,-6.09569146021933));
#64384=CARTESIAN_POINT('Ctrl Pts',(37.3993893308306,0.794403226463186,-6.31925798318959));
#64385=CARTESIAN_POINT('Ctrl Pts',(37.3658660275113,-0.2465199211245,-6.27838628774439));
#64386=CARTESIAN_POINT('Ctrl Pts',(37.3323427241921,-1.28744306871219,-6.2375145922992));
#64387=CARTESIAN_POINT('Ctrl Pts',(37.2988194208728,-2.31798308825416,-5.93220467843854));
#64388=CARTESIAN_POINT('Ctrl Pts',(37.2652961175535,-3.21318744594017,-5.39947524180827));
#64389=CARTESIAN_POINT('Ctrl Pts',(37.2317728142342,-4.10839180362623,-4.86674580517798));
#64390=CARTESIAN_POINT('Ctrl Pts',(37.198249510915,-4.8682604994563,-4.10659684577804));
#64391=CARTESIAN_POINT('Ctrl Pts',(37.1647262075957,-5.40065978111937,-3.21119609775669));
#64392=CARTESIAN_POINT('Ctrl Pts',(37.1312029042765,-5.9330590627824,-2.31579534973541));
#64393=CARTESIAN_POINT('Ctrl Pts',(37.0976796009572,-6.23798893027845,-1.28514281309276));
#64394=CARTESIAN_POINT('Ctrl Pts',(37.0641562976379,-6.27847676841984,-0.244204664288998));
#64395=CARTESIAN_POINT('Ctrl Pts',(37.0615370087821,-6.28164021989209,-0.162872652738991));
#64396=CARTESIAN_POINT('Ctrl Pts',(37.0589177199263,-6.28318929920806,-0.0814778493327739));
#64397=CARTESIAN_POINT('Ctrl Pts',(37.0562984310705,-6.28313695873549,-8.10514889743041E-5));
#64398=CARTESIAN_POINT('Ctrl Pts',(36.8700381542954,-6.28321544720413,2.5547018683295E-5));
#64399=CARTESIAN_POINT('Ctrl Pts',(36.902776131226,-6.28298156430956,-1.01730009221029));
#64400=CARTESIAN_POINT('Ctrl Pts',(36.9355141081566,-6.03106071247253,-2.0347373888128));
#64401=CARTESIAN_POINT('Ctrl Pts',(36.9682520850872,-5.55596476178223,-2.93430777034463));
#64402=CARTESIAN_POINT('Ctrl Pts',(37.0017753884065,-5.06947209626076,-3.85545726046282));
#64403=CARTESIAN_POINT('Ctrl Pts',(37.0352986917257,-4.34896875413393,-4.65301717142637));
#64404=CARTESIAN_POINT('Ctrl Pts',(37.068821995045,-3.48181545551966,-5.23028370731217));
#64405=CARTESIAN_POINT('Ctrl Pts',(37.1023452983643,-2.6146621569054,-5.80755024319796));
#64406=CARTESIAN_POINT('Ctrl Pts',(37.1358686016836,-1.60085890180369,-6.164523404006));
#64407=CARTESIAN_POINT('Ctrl Pts',(37.1693919050028,-0.563328898540168,
-6.25792034763468));
#64408=CARTESIAN_POINT('Ctrl Pts',(37.2029152083221,0.474201104723353,-6.35131729126336));
#64409=CARTESIAN_POINT('Ctrl Pts',(37.2364385116413,1.5354578561487,-6.18113801771268));
#64410=CARTESIAN_POINT('Ctrl Pts',(37.2699618149606,2.49176443140565,-5.76801669065306));
#64411=CARTESIAN_POINT('Ctrl Pts',(37.3034851182799,3.44807100666263,-5.35489536359344));
#64412=CARTESIAN_POINT('Ctrl Pts',(37.3370084215992,4.29942740575116,-4.69883198302491));
#64413=CARTESIAN_POINT('Ctrl Pts',(37.3705317249184,4.94260703171787,-3.87937395146224));
#64414=CARTESIAN_POINT('Ctrl Pts',(37.4040550282377,5.58578665768455,-3.05991591989961));
#64415=CARTESIAN_POINT('Ctrl Pts',(37.4375783315569,6.02078951052939,-2.07706323734282));
#64416=CARTESIAN_POINT('Ctrl Pts',(37.4711016348762,6.19487168157636,-1.04998636851815));
#64417=CARTESIAN_POINT('Ctrl Pts',(37.5046249381955,6.36895385262334,-0.022909499693449));
#64418=CARTESIAN_POINT('Ctrl Pts',(37.5381482415148,6.28211534187248,1.04839155539914));
#64419=CARTESIAN_POINT('Ctrl Pts',(37.571671544834,5.94488528137579,2.03402200493313));
#64420=CARTESIAN_POINT('Ctrl Pts',(37.6051948481533,5.60765522087911,3.01965245446706));
#64421=CARTESIAN_POINT('Ctrl Pts',(37.6387181514726,5.02003361063657,3.91961229844241));
#64422=CARTESIAN_POINT('Ctrl Pts',(37.6722414547918,4.25326931796938,4.62478179313262));
#64423=CARTESIAN_POINT('Ctrl Pts',(37.7057647581111,3.48650502530215,5.32995128782288));
#64424=CARTESIAN_POINT('Ctrl Pts',(37.7392880614304,2.54059805021029,5.84033043322802));
#64425=CARTESIAN_POINT('Ctrl Pts',(37.7728113647496,1.53023920629164,6.09403597764229));
#64426=CARTESIAN_POINT('Ctrl Pts',(37.8063346680689,0.519880362372982,6.34774152205655));
#64427=CARTESIAN_POINT('Ctrl Pts',(37.8398579713882,-0.554930350372418,
6.34477346547987));
#64428=CARTESIAN_POINT('Ctrl Pts',(37.8733812747074,-1.5638725956381,6.08549168349467));
#64429=CARTESIAN_POINT('Ctrl Pts',(37.9069045780267,-2.57281484090379,5.82620990150948));
#64430=CARTESIAN_POINT('Ctrl Pts',(37.940427881346,-3.51588861868977,5.31061439411577));
#64431=CARTESIAN_POINT('Ctrl Pts',(37.9739511846652,-4.27874663935198,4.60122089466533));
#64432=CARTESIAN_POINT('Ctrl Pts',(38.0074744879845,-5.0416046600142,3.89182739521488));
#64433=CARTESIAN_POINT('Ctrl Pts',(38.0409977913038,-5.62424692355264,2.98863590370768));
#64434=CARTESIAN_POINT('Ctrl Pts',(38.074521094623,-5.95602830629082,2.00115799974245));
#64435=CARTESIAN_POINT('Ctrl Pts',(38.0963601145138,-6.17216990033383,1.35785774436396));
#64436=CARTESIAN_POINT('Ctrl Pts',(38.1181991344046,-6.28184679862301,0.678786557982193));
#64437=CARTESIAN_POINT('Ctrl Pts',(38.1400381542954,-6.2823463260306,-0.000127106979284774));
#64438=CARTESIAN_POINT('Origin',(37.,0.,0.));
#64439=CARTESIAN_POINT('',(39.5962984310705,-6.28286224794853,0.000148810185861201));
#64440=CARTESIAN_POINT('',(39.4100381542954,-6.282535125309,0.000156527191468202));
#64441=CARTESIAN_POINT('',(37.,-6.28269,-7.69407619853508E-16));
#64442=CARTESIAN_POINT('Ctrl Pts',(39.5962984310705,-6.28286224794853,0.000148810185861201));
#64443=CARTESIAN_POINT('Ctrl Pts',(39.5903336362413,-6.28304804443731,0.18553371703489));
#64444=CARTESIAN_POINT('Ctrl Pts',(39.5843688414121,-6.27500548490837,0.370902559242192));
#64445=CARTESIAN_POINT('Ctrl Pts',(39.578404046583,-6.25861743229305,0.555530634479874));
#64446=CARTESIAN_POINT('Ctrl Pts',(39.5448807432637,-6.16651339948561,1.59317621068257));
#64447=CARTESIAN_POINT('Ctrl Pts',(39.5113574399444,-5.81080378911597,2.60742349239934));
#64448=CARTESIAN_POINT('Ctrl Pts',(39.4778341366252,-5.23461823833893,3.47529543326859));
#64449=CARTESIAN_POINT('Ctrl Pts',(39.4443108333059,-4.65843268756187,4.34316737413788));
#64450=CARTESIAN_POINT('Ctrl Pts',(39.4107875299866,-3.86177119637738,5.06466397415965));
#64451=CARTESIAN_POINT('Ctrl Pts',(39.3772642266674,-2.94122862769708,5.55230408112373));
#64452=CARTESIAN_POINT('Ctrl Pts',(39.3437409233481,-2.02068605901675,6.03994418808783));
#64453=CARTESIAN_POINT('Ctrl Pts',(39.3102176200289,-0.976262412840673,
6.29372780199423));
#64454=CARTESIAN_POINT('Ctrl Pts',(39.2766943167096,0.0654063932673694,
6.28288376888892));
#64455=CARTESIAN_POINT('Ctrl Pts',(39.2431710133903,1.10707519937532,6.27203973578361));
#64456=CARTESIAN_POINT('Ctrl Pts',(39.209647710071,2.14598916541525,5.99656805566658));
#64457=CARTESIAN_POINT('Ctrl Pts',(39.1761244067517,3.0561804201681,5.48986955118509));
#64458=CARTESIAN_POINT('Ctrl Pts',(39.1426011034325,3.96637167492101,4.98317104670358));
#64459=CARTESIAN_POINT('Ctrl Pts',(39.1090778001132,4.74784021838694,4.24524571785757));
#64460=CARTESIAN_POINT('Ctrl Pts',(39.075554496794,5.3058333260259,3.365566693156));
#64461=CARTESIAN_POINT('Ctrl Pts',(39.0420311934747,5.86382643366487,2.48588766845441));
#64462=CARTESIAN_POINT('Ctrl Pts',(39.0085078901554,6.19834410547685,1.46445494789734));
#64463=CARTESIAN_POINT('Ctrl Pts',(38.9749845868362,6.26882621773588,0.425116809212897));
#64464=CARTESIAN_POINT('Ctrl Pts',(38.9414612835169,6.3393083299949,-0.61422132947149));
#64465=CARTESIAN_POINT('Ctrl Pts',(38.9079379801976,6.14575488270097,-1.67146488628317));
#64466=CARTESIAN_POINT('Ctrl Pts',(38.8744146768784,5.7116341480303,-2.61842353501152));
#64467=CARTESIAN_POINT('Ctrl Pts',(38.8408913735591,5.27751341335964,-3.56538218373986));
#64468=CARTESIAN_POINT('Ctrl Pts',(38.8073680702398,4.60282539131222,-4.40205592438488));
#64469=CARTESIAN_POINT('Ctrl Pts',(38.7738447669205,3.76937571416591,-5.02699842600973));
#64470=CARTESIAN_POINT('Ctrl Pts',(38.7403214636013,2.93592603701955,-5.65194092763462));
#64471=CARTESIAN_POINT('Ctrl Pts',(38.706798160282,1.94371470477427,-6.06515219023933));
#64472=CARTESIAN_POINT('Ctrl Pts',(38.6732748569627,0.913046914402851,-6.21653052608507));
#64473=CARTESIAN_POINT('Ctrl Pts',(38.6397515536435,-0.117620875968512,
-6.36790886193081));
#64474=CARTESIAN_POINT('Ctrl Pts',(38.6062282503242,-1.18674512446603,-6.25745427101762));
#64475=CARTESIAN_POINT('Ctrl Pts',(38.572704947005,-2.16469497612578,-5.89855932495248));
#64476=CARTESIAN_POINT('Ctrl Pts',(38.5391816436857,-3.14264482778553,-5.53966437888735));
#64477=CARTESIAN_POINT('Ctrl Pts',(38.5056583403664,-4.02942028260758,-4.93232907767022));
#64478=CARTESIAN_POINT('Ctrl Pts',(38.4721350370471,-4.7175001983755,-4.15019256516793));
#64479=CARTESIAN_POINT('Ctrl Pts',(38.4386117337279,-5.40558011414346,-3.36805605266561));
#64480=CARTESIAN_POINT('Ctrl Pts',(38.4050884304086,-5.8949644908573,-2.41111832887814));
#64481=CARTESIAN_POINT('Ctrl Pts',(38.3715651270894,-6.12631568347861,-1.39540768093492));
#64482=CARTESIAN_POINT('Ctrl Pts',(38.3564762284164,-6.23044726830737,-0.938234504953467));
#64483=CARTESIAN_POINT('Ctrl Pts',(38.3413873297434,-6.28230349309892,-0.469154427224146));
#64484=CARTESIAN_POINT('Ctrl Pts',(38.3262984310705,-6.28217936372029,-4.73315304236333E-5));
#64485=CARTESIAN_POINT('Ctrl Pts',(38.1400381542954,-6.2823463260306,-0.000127106979284774));
#64486=CARTESIAN_POINT('Ctrl Pts',(38.1517224377239,-6.28261358252104,-0.363358594680692));
#64487=CARTESIAN_POINT('Ctrl Pts',(38.1634067211523,-6.25162936468712,-0.726544992666329));
#64488=CARTESIAN_POINT('Ctrl Pts',(38.1750910045808,-6.18897823607404,-1.08418398746365));
#64489=CARTESIAN_POINT('Ctrl Pts',(38.2086143079001,-6.00922628118114,-2.11028375428133));
#64490=CARTESIAN_POINT('Ctrl Pts',(38.2421376112194,-5.56880186945739,-3.09071897149348));
#64491=CARTESIAN_POINT('Ctrl Pts',(38.2756609145386,-4.92110627125931,-3.90661229100649));
#64492=CARTESIAN_POINT('Ctrl Pts',(38.3091842178579,-4.27341067306123,-4.7225056105195));
#64493=CARTESIAN_POINT('Ctrl Pts',(38.3427075211772,-3.41844388838883,-5.37385703233337));
#64494=CARTESIAN_POINT('Ctrl Pts',(38.3762308244964,-2.45987027189365,-5.78169047690418));
#64495=CARTESIAN_POINT('Ctrl Pts',(38.4097541278157,-1.50129665539843,-6.18952392147501));
#64496=CARTESIAN_POINT('Ctrl Pts',(38.443277431135,-0.439116207080419,-6.35383938880275));
#64497=CARTESIAN_POINT('Ctrl Pts',(38.4768007344543,0.597882150879494,-6.25471369919763));
#64498=CARTESIAN_POINT('Ctrl Pts',(38.5103240377735,1.63488050883938,-6.1555880095925));
#64499=CARTESIAN_POINT('Ctrl Pts',(38.5438473410928,2.64669677644117,-5.79302116305454));
#64500=CARTESIAN_POINT('Ctrl Pts',(38.577370644412,3.51064866673838,-5.2109742336725));
#64501=CARTESIAN_POINT('Ctrl Pts',(38.6108939477313,4.37460055703559,-4.62892730429046));
#64502=CARTESIAN_POINT('Ctrl Pts',(38.6444172510506,5.09068807002823,-3.82740029206434));
#64503=CARTESIAN_POINT('Ctrl Pts',(38.6779405543698,5.57208590298025,-2.90357800223784));
#64504=CARTESIAN_POINT('Ctrl Pts',(38.7114638576891,6.05348373593226,-1.97975571241136));
#64505=CARTESIAN_POINT('Ctrl Pts',(38.7449871610084,6.30019188884368,-0.933638144984511));
#64506=CARTESIAN_POINT('Ctrl Pts',(38.7785104643276,6.28229710436072,0.107933395256214));
#64507=CARTESIAN_POINT('Ctrl Pts',(38.8120337676469,6.26440231987777,1.14950493549694));
#64508=CARTESIAN_POINT('Ctrl Pts',(38.8455570709662,5.98190459800044,2.18653044855153));
#64509=CARTESIAN_POINT('Ctrl Pts',(38.8790803742854,5.46905666591529,3.09327103731279));
#64510=CARTESIAN_POINT('Ctrl Pts',(38.9126036776047,4.95620873383013,4.00001162607407));
#64511=CARTESIAN_POINT('Ctrl Pts',(38.946126980924,4.21301059153714,4.77646729054201));
#64512=CARTESIAN_POINT('Ctrl Pts',(38.9796502842433,3.3295746939062,5.32849311559751));
#64513=CARTESIAN_POINT('Ctrl Pts',(39.0131735875625,2.44613879627526,5.88051894065301));
#64514=CARTESIAN_POINT('Ctrl Pts',(39.0466968908818,1.42246514330638,6.20811492629609));
#64515=CARTESIAN_POINT('Ctrl Pts',(39.0802201942011,0.382673724818222,6.27156020026951));
#64516=CARTESIAN_POINT('Ctrl Pts',(39.1137434975203,-0.657117693669971,
6.33500547424293));
#64517=CARTESIAN_POINT('Ctrl Pts',(39.1472668008396,-1.71302687767745,6.13430003654668));
#64518=CARTESIAN_POINT('Ctrl Pts',(39.1807901041589,-2.65702529312174,5.69377933511495));
#64519=CARTESIAN_POINT('Ctrl Pts',(39.2143134074781,-3.60102370856599,5.25325863368324));
#64520=CARTESIAN_POINT('Ctrl Pts',(39.2478367107974,-4.43311135544706,4.57292266851607));
#64521=CARTESIAN_POINT('Ctrl Pts',(39.2813600141166,-5.0523979647231,3.7352618825636));
#64522=CARTESIAN_POINT('Ctrl Pts',(39.3148833174359,-5.67168457399914,2.89760109661113));
#64523=CARTESIAN_POINT('Ctrl Pts',(39.3484066207552,-6.07817014567012,1.90261548987344));
#64524=CARTESIAN_POINT('Ctrl Pts',(39.3819299240745,-6.22256847912821,0.870946638911246));
#64525=CARTESIAN_POINT('Ctrl Pts',(39.3912993341481,-6.26292629193788,0.582606064809031));
#64526=CARTESIAN_POINT('Ctrl Pts',(39.4006687442218,-6.28281132775394,0.29140000254511));
#64527=CARTESIAN_POINT('Ctrl Pts',(39.4100381542954,-6.282535125309,0.000156527191468202));
#64528=CARTESIAN_POINT('Origin',(37.,0.,0.));
#64529=CARTESIAN_POINT('',(40.8662984310705,-6.28281011036189,-0.000154357209955491));
#64530=CARTESIAN_POINT('',(40.6800381542954,-6.28310564591676,-9.39174517631389E-5));
#64531=CARTESIAN_POINT('',(37.,-6.28269,-7.69407619853508E-16));
#64532=CARTESIAN_POINT('Ctrl Pts',(40.8662984310705,-6.28281011036189,-0.000154357209955491));
#64533=CARTESIAN_POINT('Ctrl Pts',(40.8392799427392,-6.28195467965013,0.839596208053496));
#64534=CARTESIAN_POINT('Ctrl Pts',(40.8122614544079,-6.11248623477459,1.6796816398236));
#64535=CARTESIAN_POINT('Ctrl Pts',(40.7852429660766,-5.78475116091983,2.45266395086745));
#64536=CARTESIAN_POINT('Ctrl Pts',(40.7517196627573,-5.37811248615472,3.41174501253935));
#64537=CARTESIAN_POINT('Ctrl Pts',(40.718196359438,-4.72782692174914,4.26752276412259));
#64538=CARTESIAN_POINT('Ctrl Pts',(40.6846730561188,-3.91274131249501,4.91623452157674));
#64539=CARTESIAN_POINT('Ctrl Pts',(40.6511497527995,-3.09765570324088,5.56494627903089));
#64540=CARTESIAN_POINT('Ctrl Pts',(40.6176264494803,-2.11777004913822,6.00659204235594));
#64541=CARTESIAN_POINT('Ctrl Pts',(40.584103146161,-1.09189506399012,6.18762245283939));
#64542=CARTESIAN_POINT('Ctrl Pts',(40.5505798428417,-0.0660200788419529,
6.36865286332285));
#64543=CARTESIAN_POINT('Ctrl Pts',(40.5170565395225,1.00584423735164,6.28906792096469));
#64544=CARTESIAN_POINT('Ctrl Pts',(40.4835332362032,1.99373479759796,5.95851726577133));
#64545=CARTESIAN_POINT('Ctrl Pts',(40.4500099328839,2.98162535784423,5.627966610578));
#64546=CARTESIAN_POINT('Ctrl Pts',(40.4164866295647,3.88554216214322,5.0464502425495));
#64547=CARTESIAN_POINT('Ctrl Pts',(40.3829633262454,4.59588568703246,4.2844767710163));
#64548=CARTESIAN_POINT('Ctrl Pts',(40.3494400229261,5.30622921192172,3.52250329948308));
#64549=CARTESIAN_POINT('Ctrl Pts',(40.3159167196068,5.82299945740124,2.58007272444507));
#64550=CARTESIAN_POINT('Ctrl Pts',(40.2823934162875,6.08353825363188,1.57145434749016));
#64551=CARTESIAN_POINT('Ctrl Pts',(40.2488701129683,6.3440770498625,0.562835970535265));
#64552=CARTESIAN_POINT('Ctrl Pts',(40.215346809649,6.34838439684431,-0.5119702083366));
#64553=CARTESIAN_POINT('Ctrl Pts',(40.1818235063298,6.09593803060969,-1.52264440254924));
#64554=CARTESIAN_POINT('Ctrl Pts',(40.1483002030105,5.84349166437507,-2.53331859676188));
#64555=CARTESIAN_POINT('Ctrl Pts',(40.1147768996912,5.33429158492403,-3.47986080631527));
#64556=CARTESIAN_POINT('Ctrl Pts',(40.081253596372,4.63007808272299,-4.24750319570642));
#64557=CARTESIAN_POINT('Ctrl Pts',(40.0477302930527,3.9258645805219,-5.01514558509763));
#64558=CARTESIAN_POINT('Ctrl Pts',(40.0142069897334,3.02663765557088,-5.60388815432652));
#64559=CARTESIAN_POINT('Ctrl Pts',(39.9806836864142,2.04142818547992,-5.94234612027744));
#64560=CARTESIAN_POINT('Ctrl Pts',(39.9471603830949,1.05621871538901,-6.28080408622833));
#64561=CARTESIAN_POINT('Ctrl Pts',(39.9136370797757,-0.0149732998418345,
-6.36897744890122));
#64562=CARTESIAN_POINT('Ctrl Pts',(39.8801137764564,-1.04226628942212,-6.19617522602309));
#64563=CARTESIAN_POINT('Ctrl Pts',(39.8465904731371,-2.06955927900244,-6.02337300314495));
#64564=CARTESIAN_POINT('Ctrl Pts',(39.8130671698178,-3.05295324293226,-5.5895951947158));
#64565=CARTESIAN_POINT('Ctrl Pts',(39.7795438664985,-3.873212086352,-4.94743717330346));
#64566=CARTESIAN_POINT('Ctrl Pts',(39.7460205631793,-4.69347092977173,-4.30527915189112));
#64567=CARTESIAN_POINT('Ctrl Pts',(39.71249725986,-5.35059465268135,-3.4547409174956));
#64568=CARTESIAN_POINT('Ctrl Pts',(39.6789739565408,-5.76490728651354,-2.49894986495351));
#64569=CARTESIAN_POINT('Ctrl Pts',(39.6514154480507,-6.10550135411715,-1.71322252819967));
#64570=CARTESIAN_POINT('Ctrl Pts',(39.6238569395606,-6.28200383215044,-0.856365399548567));
#64571=CARTESIAN_POINT('Ctrl Pts',(39.5962984310705,-6.28286224794853,0.000148810185861201));
#64572=CARTESIAN_POINT('Ctrl Pts',(39.4100381542954,-6.282535125309,0.000156527191468202));
#64573=CARTESIAN_POINT('Ctrl Pts',(39.434192047541,-6.28182308855144,-0.7506552909351));
#64574=CARTESIAN_POINT('Ctrl Pts',(39.4583459407866,-6.1471227161439,-1.50171575041843));
#64575=CARTESIAN_POINT('Ctrl Pts',(39.4824998340322,-5.88377149391016,-2.20457241494147));
#64576=CARTESIAN_POINT('Ctrl Pts',(39.5160231373515,-5.5182650799889,-3.18007052264519));
#64577=CARTESIAN_POINT('Ctrl Pts',(39.5495464406708,-4.90494115690126,-4.06271464286602));
#64578=CARTESIAN_POINT('Ctrl Pts',(39.5830697439901,-4.11816498633818,-4.74548455592988));
#64579=CARTESIAN_POINT('Ctrl Pts',(39.6165930473094,-3.33138881577507,-5.42825446899375));
#64580=CARTESIAN_POINT('Ctrl Pts',(39.6501163506286,-2.37116039773654,-5.91115017490064));
#64581=CARTESIAN_POINT('Ctrl Pts',(39.6836396539478,-1.35390701461365,-6.13562077715455));
#64582=CARTESIAN_POINT('Ctrl Pts',(39.7171629572671,-0.336653631490792,
-6.36009137940847));
#64583=CARTESIAN_POINT('Ctrl Pts',(39.7506862605864,0.737624716716394,-6.32613687800943));
#64584=CARTESIAN_POINT('Ctrl Pts',(39.7842095639057,1.73867224267262,-6.03787424163757));
#64585=CARTESIAN_POINT('Ctrl Pts',(39.8177328672249,2.73971976862887,-5.7496116052657));
#64586=CARTESIAN_POINT('Ctrl Pts',(39.8512561705442,3.66753647233414,-5.20704083392101));
#64587=CARTESIAN_POINT('Ctrl Pts',(39.8847794738634,4.40962497780978,-4.47594840009877));
#64588=CARTESIAN_POINT('Ctrl Pts',(39.9183027771827,5.15171348328543,-3.74485596627654));
#64589=CARTESIAN_POINT('Ctrl Pts',(39.951826080502,5.70807379053144,-2.82524186997678));
#64590=CARTESIAN_POINT('Ctrl Pts',(39.9853493838213,6.0112474517597,-1.82860892456074));
#64591=CARTESIAN_POINT('Ctrl Pts',(40.0188726871405,6.31442111298794,-0.831975979144762));
#64592=CARTESIAN_POINT('Ctrl Pts',(40.0523959904598,6.36440812819845,0.241675815387561));
#64593=CARTESIAN_POINT('Ctrl Pts',(40.0859192937791,6.15514759331208,1.26216664106418));
#64594=CARTESIAN_POINT('Ctrl Pts',(40.1194425970983,5.94588705842569,2.28265746674088));
#64595=CARTESIAN_POINT('Ctrl Pts',(40.1529659004176,5.47737897344238,3.24998732356193));
#64596=CARTESIAN_POINT('Ctrl Pts',(40.1864892037369,4.80642974201378,4.04686788274043));
#64597=CARTESIAN_POINT('Ctrl Pts',(40.2200125070561,4.13548051058523,4.84374844191888));
#64598=CARTESIAN_POINT('Ctrl Pts',(40.2535358103754,3.26209013271142,5.47017970345478));
#64599=CARTESIAN_POINT('Ctrl Pts',(40.2870591136947,2.29215681578979,5.85020714651191));
#64600=CARTESIAN_POINT('Ctrl Pts',(40.3205824170139,1.32222349886816,6.23023458956905));
#64601=CARTESIAN_POINT('Ctrl Pts',(40.3541057203332,0.25574724289874,6.36385821414741));
#64602=CARTESIAN_POINT('Ctrl Pts',(40.3876290236525,-0.777962165108884,
6.2348762132804));
#64603=CARTESIAN_POINT('Ctrl Pts',(40.4211523269717,-1.81167157311654,6.10589421241339));
#64604=CARTESIAN_POINT('Ctrl Pts',(40.454675630291,-2.81261413316237,5.71430658610099));
#64605=CARTESIAN_POINT('Ctrl Pts',(40.4881989336103,-3.65942599066088,5.10759316548865));
#64606=CARTESIAN_POINT('Ctrl Pts',(40.5217222369295,-4.50623784815938,4.5008797448763));
#64607=CARTESIAN_POINT('Ctrl Pts',(40.5552455402488,-5.19891900311054,3.67904052996403));
#64608=CARTESIAN_POINT('Ctrl Pts',(40.588768843568,-5.65348216361643,2.74172317182855));
#64609=CARTESIAN_POINT('Ctrl Pts',(40.6191919471438,-6.06600780233705,1.89108793465174));
#64610=CARTESIAN_POINT('Ctrl Pts',(40.6496150507196,-6.28242077900449,0.945345537979423));
#64611=CARTESIAN_POINT('Ctrl Pts',(40.6800381542954,-6.28310564591676,-9.39174517631389E-5));
#64612=CARTESIAN_POINT('Origin',(37.,0.,0.));
#64613=CARTESIAN_POINT('',(42.1362984310705,-6.28219522128395,6.19374010119023E-5));
#64614=CARTESIAN_POINT('',(41.9500381542954,-6.28216889122489,-3.39632393438963E-5));
#64615=CARTESIAN_POINT('',(37.,-6.28269,-7.69407619853508E-16));
#64616=CARTESIAN_POINT('Ctrl Pts',(42.1362984310705,-6.28219522128395,6.19374010119023E-5));
#64617=CARTESIAN_POINT('Ctrl Pts',(42.1217495525563,-6.28235233139332,0.452376781104032));
#64618=CARTESIAN_POINT('Ctrl Pts',(42.1072006740422,-6.23417154886657,0.904658649178573));
#64619=CARTESIAN_POINT('Ctrl Pts',(42.092651795528,-6.13730307499778,1.34626053023583));
#64620=CARTESIAN_POINT('Ctrl Pts',(42.0591284922087,-5.91410021929876,2.36379282941863));
#64621=CARTESIAN_POINT('Ctrl Pts',(42.0256051888895,-5.43240140354768,3.32462222441192));
#64622=CARTESIAN_POINT('Ctrl Pts',(41.9920818855702,-4.7506124018243,4.11224856462754));
#64623=CARTESIAN_POINT('Ctrl Pts',(41.9585585822509,-4.06882340010089,4.89987490484318));
#64624=CARTESIAN_POINT('Ctrl Pts',(41.9250352789317,-3.18694421240517,5.51429819028114));
#64625=CARTESIAN_POINT('Ctrl Pts',(41.8915119756124,-2.21190231067177,5.88101986203864));
#64626=CARTESIAN_POINT('Ctrl Pts',(41.8579886722932,-1.23686040893839,6.24774153379614));
#64627=CARTESIAN_POINT('Ctrl Pts',(41.8244653689739,-0.168655793167334,
6.36676159187319));
#64628=CARTESIAN_POINT('Ctrl Pts',(41.7909420656546,0.86319218674972,6.22364890545589));
#64629=CARTESIAN_POINT('Ctrl Pts',(41.7574187623353,1.89504016666674,6.0805362190386));
#64630=CARTESIAN_POINT('Ctrl Pts',(41.7238954590161,2.89053151072977,5.67529078812696));
#64631=CARTESIAN_POINT('Ctrl Pts',(41.6903721556968,3.72896332194492,5.05704844679558));
#64632=CARTESIAN_POINT('Ctrl Pts',(41.6568488523775,4.56739513316007,4.4388061054642));
#64633=CARTESIAN_POINT('Ctrl Pts',(41.6233255490583,5.24876741152739,3.60756685371299));
#64634=CARTESIAN_POINT('Ctrl Pts',(41.589802245739,5.69046406156712,2.66411809303964));
#64635=CARTESIAN_POINT('Ctrl Pts',(41.5562789424197,6.13216071160688,1.72066933236623));
#64636=CARTESIAN_POINT('Ctrl Pts',(41.5227556391005,6.33418173331909,0.66501106277067));
#64637=CARTESIAN_POINT('Ctrl Pts',(41.4892323357812,6.27203216477392,-0.374858604929178));
#64638=CARTESIAN_POINT('Ctrl Pts',(41.4557090324619,6.20988259622875,-1.41472827262897));
#64639=CARTESIAN_POINT('Ctrl Pts',(41.4221857291426,5.88356243742621,-2.43880933843296));
#64640=CARTESIAN_POINT('Ctrl Pts',(41.3886624258234,5.33263786716822,-3.32293241389162));
#64641=CARTESIAN_POINT('Ctrl Pts',(41.3551391225041,4.78171329691024,-4.20705548935028));
#64642=CARTESIAN_POINT('Ctrl Pts',(41.3216158191849,4.00618431519681,-4.95122057446359));
#64643=CARTESIAN_POINT('Ctrl Pts',(41.2880925158656,3.10008347726189,-5.4651979729609));
#64644=CARTESIAN_POINT('Ctrl Pts',(41.2545692125463,2.19398263932697,-5.97917537145821));
#64645=CARTESIAN_POINT('Ctrl Pts',(41.2210459092271,1.15730994517057,-6.26296508333951));
#64646=CARTESIAN_POINT('Ctrl Pts',(41.1875226059078,0.115761512760339,-6.28215772818636));
#64647=CARTESIAN_POINT('Ctrl Pts',(41.1539993025885,-0.92578691964992,-6.30135037303321));
#64648=CARTESIAN_POINT('Ctrl Pts',(41.1204759992693,-1.972211090314,-6.05594595084558));
#64649=CARTESIAN_POINT('Ctrl Pts',(41.08695269595,-2.89663251893485,-5.57569964218817));
#64650=CARTESIAN_POINT('Ctrl Pts',(41.0534293926307,-3.82105394755572,-5.09545333353073));
#64651=CARTESIAN_POINT('Ctrl Pts',(41.0199060893115,-4.62347263413335,-4.38036513840349));
#64652=CARTESIAN_POINT('Ctrl Pts',(40.9863827859922,-5.20659565829271,-3.51713919268141));
#64653=CARTESIAN_POINT('Ctrl Pts',(40.9528594826729,-5.78971868245205,-2.65391324695935));
#64654=CARTESIAN_POINT('Ctrl Pts',(40.9193361793536,-6.15354604419313,-1.64254955064245));
#64655=CARTESIAN_POINT('Ctrl Pts',(40.8858128760344,-6.25396383250134,-0.60567551660371));
#64656=CARTESIAN_POINT('Ctrl Pts',(40.8793080610464,-6.27344875999268,-0.404481926192384));
#64657=CARTESIAN_POINT('Ctrl Pts',(40.8728032460584,-6.28301605891263,-0.202327846566644));
#64658=CARTESIAN_POINT('Ctrl Pts',(40.8662984310705,-6.28281011036189,-0.000154357209955491));
#64659=CARTESIAN_POINT('Ctrl Pts',(40.6800381542954,-6.28310564591676,-9.39174517631389E-5));
#64660=CARTESIAN_POINT('Ctrl Pts',(40.6831383540389,-6.2831754357796,-0.096436854650988));
#64661=CARTESIAN_POINT('Ctrl Pts',(40.6862385537824,-6.28100506553998,-0.192776646053021));
#64662=CARTESIAN_POINT('Ctrl Pts',(40.6893387535259,-6.27657377857455,-0.289012330845967));
#64663=CARTESIAN_POINT('Ctrl Pts',(40.7228620568452,-6.22865706696617,-1.3296349740264));
#64664=CARTESIAN_POINT('Ctrl Pts',(40.7563853601644,-5.91637847768878,-2.35808475902857));
#64665=CARTESIAN_POINT('Ctrl Pts',(40.7899086634837,-5.37760165528307,-3.24966259208051));
#64666=CARTESIAN_POINT('Ctrl Pts',(40.8234319668029,-4.83882483287737,-4.14124042513245));
#64667=CARTESIAN_POINT('Ctrl Pts',(40.8569552701222,-4.07354977734334,-4.89594630623416));
#64668=CARTESIAN_POINT('Ctrl Pts',(40.8904785734415,-3.17456575977914,-5.42227247213828));
#64669=CARTESIAN_POINT('Ctrl Pts',(40.9240018767608,-2.275581742215,-5.94859863804237));
#64670=CARTESIAN_POINT('Ctrl Pts',(40.95752518008,-1.24288876262071,-6.24654508874889));
#64671=CARTESIAN_POINT('Ctrl Pts',(40.9910484833993,-0.201700400286187,
-6.27998594535012));
#64672=CARTESIAN_POINT('Ctrl Pts',(41.0245717867186,0.839487962048451,-6.31342680195135));
#64673=CARTESIAN_POINT('Ctrl Pts',(41.0580950900378,1.88917170712332,-6.08236206444723));
#64674=CARTESIAN_POINT('Ctrl Pts',(41.0916183933571,2.820077132647,-5.61480823280655));
#64675=CARTESIAN_POINT('Ctrl Pts',(41.1251416966764,3.7509825581706,-5.1472544011659));
#64676=CARTESIAN_POINT('Ctrl Pts',(41.1586649999956,4.56310966414304,-4.44321147538874));
#64677=CARTESIAN_POINT('Ctrl Pts',(41.1921883033149,5.15798838851631,-3.58804435719538));
#64678=CARTESIAN_POINT('Ctrl Pts',(41.2257116066342,5.75286711288959,-2.73287723900201));
#64679=CARTESIAN_POINT('Ctrl Pts',(41.2592349099534,6.1304974556637,-1.72658592839243));
#64680=CARTESIAN_POINT('Ctrl Pts',(41.2927582132727,6.2450919003148,-0.691182813655839));
#64681=CARTESIAN_POINT('Ctrl Pts',(41.326281516592,6.3596863449659,0.344220301080751));
#64682=CARTESIAN_POINT('Ctrl Pts',(41.3598048199112,6.21124489149398,1.40873521994435));
#64683=CARTESIAN_POINT('Ctrl Pts',(41.3933281232305,5.8177660022412,2.37328996720524));
#64684=CARTESIAN_POINT('Ctrl Pts',(41.4268514265498,5.4242871129884,3.33784471446619));
#64685=CARTESIAN_POINT('Ctrl Pts',(41.460374729869,4.7857707879547,4.20243929012441));
#64686=CARTESIAN_POINT('Ctrl Pts',(41.4938980331883,3.97963685672385,4.86224197401525));
#64687=CARTESIAN_POINT('Ctrl Pts',(41.5274213365076,3.17350292549306,5.52204465790606));
#64688=CARTESIAN_POINT('Ctrl Pts',(41.5609446398268,2.19975138806514,5.9770554500295));
#64689=CARTESIAN_POINT('Ctrl Pts',(41.5944679431461,1.17644919923661,6.17210448768378));
#64690=CARTESIAN_POINT('Ctrl Pts',(41.6279912464654,0.153147010408017,6.36715352533808));
#64691=CARTESIAN_POINT('Ctrl Pts',(41.6615145497846,-0.919705829821191,
6.30224080852317));
#64692=CARTESIAN_POINT('Ctrl Pts',(41.6950378531039,-1.91202637634447,5.98523697621353));
#64693=CARTESIAN_POINT('Ctrl Pts',(41.7285611564232,-2.90434692286771,5.6682331439039));
#64694=CARTESIAN_POINT('Ctrl Pts',(41.7620844597424,-3.81613517568503,5.09913819609954));
#64695=CARTESIAN_POINT('Ctrl Pts',(41.7956077630617,-4.53683720158905,4.3469546502751));
#64696=CARTESIAN_POINT('Ctrl Pts',(41.829131066381,-5.25753922749303,3.5947711044507));
#64697=CARTESIAN_POINT('Ctrl Pts',(41.8626543697003,-5.78715502648374,2.65949896060625));
#64698=CARTESIAN_POINT('Ctrl Pts',(41.8961776730195,-6.06146891088779,1.65453956362833));
#64699=CARTESIAN_POINT('Ctrl Pts',(41.9141311667782,-6.20837843721501,1.11633090055299));
#64700=CARTESIAN_POINT('Ctrl Pts',(41.9320846605368,-6.28206312737231,0.558134773999001));
#64701=CARTESIAN_POINT('Ctrl Pts',(41.9500381542954,-6.28216889122489,-3.39632393438963E-5));
#64702=CARTESIAN_POINT('Origin',(37.,0.,0.));
#64703=CARTESIAN_POINT('',(43.4062984310705,-6.2831673517952,6.56348350827965E-5));
#64704=CARTESIAN_POINT('',(43.2200381542954,-6.28290773611714,0.000142516273084187));
#64705=CARTESIAN_POINT('',(37.,-6.28269,-7.69407619853508E-16));
#64706=CARTESIAN_POINT('Ctrl Pts',(43.4062984310705,-6.2831673517952,6.56348350827965E-5));
#64707=CARTESIAN_POINT('Ctrl Pts',(43.4042191623735,-6.28320215738342,0.0646799042948801));
#64708=CARTESIAN_POINT('Ctrl Pts',(43.4021398936764,-6.28222608018872,0.129293120214478));
#64709=CARTESIAN_POINT('Ctrl Pts',(43.4000606249794,-6.28023239731441,0.193874921974653));
#64710=CARTESIAN_POINT('Ctrl Pts',(43.3665373216601,-6.24808896351293,1.23510414473776));
#64711=CARTESIAN_POINT('Ctrl Pts',(43.3330140183409,-5.95142955534036,2.26816758466867));
#64712=CARTESIAN_POINT('Ctrl Pts',(43.2994907150216,-5.42622399835116,3.16780674432107));
#64713=CARTESIAN_POINT('Ctrl Pts',(43.2659674117023,-4.90101844136195,4.06744590397347));
#64714=CARTESIAN_POINT('Ctrl Pts',(43.2324441083831,-4.14726673555611,4.83366078334737));
#64715=CARTESIAN_POINT('Ctrl Pts',(43.1989208050638,-3.25636095083704,5.37354815810855));
#64716=CARTESIAN_POINT('Ctrl Pts',(43.1653975017446,-2.36545516611797,5.91343553286973));
#64717=CARTESIAN_POINT('Ctrl Pts',(43.1318741984253,-1.33739530248567,6.2269954030182));
#64718=CARTESIAN_POINT('Ctrl Pts',(43.098350895106,-0.296833175913861,6.27620876925911));
#64719=CARTESIAN_POINT('Ctrl Pts',(43.0648275917867,0.74372895065801,6.32542213550003));
#64720=CARTESIAN_POINT('Ctrl Pts',(43.0313042884675,1.79679334016941,6.11028899783336));
#64721=CARTESIAN_POINT('Ctrl Pts',(42.9977809851482,2.73467638864608,5.65689415660482));
#64722=CARTESIAN_POINT('Ctrl Pts',(42.964257681829,3.67255943712274,5.20349931537627));
#64723=CARTESIAN_POINT('Ctrl Pts',(42.9307343785097,4.49526114456468,4.51184277058584));
#64724=CARTESIAN_POINT('Ctrl Pts',(42.8972110751904,5.10302928304715,3.66578758059048));
#64725=CARTESIAN_POINT('Ctrl Pts',(42.8636877718711,5.71079742152959,2.81973239059516));
#64726=CARTESIAN_POINT('Ctrl Pts',(42.8301644685519,6.10363199105259,1.81927855539492));
#64727=CARTESIAN_POINT('Ctrl Pts',(42.7966411652326,6.23390196914313,0.785730671898131));
#64728=CARTESIAN_POINT('Ctrl Pts',(42.7631178619133,6.36417194723367,-0.247817211598693));
#64729=CARTESIAN_POINT('Ctrl Pts',(42.7295945585941,6.23187733389174,-1.31445914339201));
#64730=CARTESIAN_POINT('Ctrl Pts',(42.6960712552748,5.85305879404355,-2.28486524835001));
#64731=CARTESIAN_POINT('Ctrl Pts',(42.6625479519555,5.47424025419536,-3.25527135330798));
#64732=CARTESIAN_POINT('Ctrl Pts',(42.6290246486363,4.84889778784092,-4.12944163143057));
#64733=CARTESIAN_POINT('Ctrl Pts',(42.595501345317,4.05285389986933,-4.80138331275082));
#64734=CARTESIAN_POINT('Ctrl Pts',(42.5619780419977,3.25681001189774,-5.47332499407108));
#64735=CARTESIAN_POINT('Ctrl Pts',(42.5284547386785,2.29006470230899,-5.94303807858901));
#64736=CARTESIAN_POINT('Ctrl Pts',(42.4949314353592,1.2698354237897,-6.15357005697805));
#64737=CARTESIAN_POINT('Ctrl Pts',(42.4614081320399,0.249606145270341,-6.36410203536712));
#64738=CARTESIAN_POINT('Ctrl Pts',(42.4278848287207,-0.82410710217959,-6.31545290762728));
#64739=CARTESIAN_POINT('Ctrl Pts',(42.3943615254014,-1.82111704944835,-6.0135213595577));
#64740=CARTESIAN_POINT('Ctrl Pts',(42.3608382220821,-2.8181269967171,-5.71158981148812));
#64741=CARTESIAN_POINT('Ctrl Pts',(42.3273149187629,-3.7384336438047,-5.1563758430888));
#64742=CARTESIAN_POINT('Ctrl Pts',(42.2937916154436,-4.47045020586492,-4.41519890905613));
#64743=CARTESIAN_POINT('Ctrl Pts',(42.2602683121243,-5.20246676792509,-3.67402197502349));
#64744=CARTESIAN_POINT('Ctrl Pts',(42.2267450088051,-5.74619324495793,-2.74688207535751));
#64745=CARTESIAN_POINT('Ctrl Pts',(42.1932217054858,-6.03570303565085,-1.74619452383838));
#64746=CARTESIAN_POINT('Ctrl Pts',(42.1742472806807,-6.19956760775252,-1.17979835103651));
#64747=CARTESIAN_POINT('Ctrl Pts',(42.1552728558756,-6.28199032068262,-0.589840162731772));
#64748=CARTESIAN_POINT('Ctrl Pts',(42.1362984310705,-6.28219522128395,6.19374010119023E-5));
#64749=CARTESIAN_POINT('Ctrl Pts',(41.9500381542954,-6.28216889122489,-3.39632393438963E-5));
#64750=CARTESIAN_POINT('Ctrl Pts',(41.965607963856,-6.28226061281764,-0.484094673557285));
#64751=CARTESIAN_POINT('Ctrl Pts',(41.9811777734167,-6.22701450793077,-0.968134784699993));
#64752=CARTESIAN_POINT('Ctrl Pts',(41.9967475829773,-6.11619962718259,-1.43909994292342));
#64753=CARTESIAN_POINT('Ctrl Pts',(42.0302708862965,-5.87760448925595,-2.45313340238563));
#64754=CARTESIAN_POINT('Ctrl Pts',(42.0637941896158,-5.38140224358531,-3.40655367119862));
#64755=CARTESIAN_POINT('Ctrl Pts',(42.0973174929351,-4.68775719888566,-4.18375895213459));
#64756=CARTESIAN_POINT('Ctrl Pts',(42.1308407962544,-3.99411215418602,-4.96096423307055));
#64757=CARTESIAN_POINT('Ctrl Pts',(42.1643640995736,-3.10302431045737,-5.56195452612949));
#64758=CARTESIAN_POINT('Ctrl Pts',(42.1978874028929,-2.12253768521484,-5.91386001695285));
#64759=CARTESIAN_POINT('Ctrl Pts',(42.2314107062122,-1.1420510599723,-6.2657655077762));
#64760=CARTESIAN_POINT('Ctrl Pts',(42.2649340095314,-0.0721656532158725,
-6.36858619636397));
#64761=CARTESIAN_POINT('Ctrl Pts',(42.2984573128507,0.957395389979257,-6.20985511848039));
#64762=CARTESIAN_POINT('Ctrl Pts',(42.33198061617,1.98695643317445,-6.0511240405968));
#64763=CARTESIAN_POINT('Ctrl Pts',(42.3655039194892,2.97619311280833,-5.63084119624184));
#64764=CARTESIAN_POINT('Ctrl Pts',(42.3990272228085,3.80516090725694,-4.99996569939777));
#64765=CARTESIAN_POINT('Ctrl Pts',(42.4325505261278,4.63412870170551,-4.36909020255373));
#64766=CARTESIAN_POINT('Ctrl Pts',(42.466073829447,5.30282761096882,-3.52762205322063));
#64767=CARTESIAN_POINT('Ctrl Pts',(42.4995971327663,5.73017818011631,-2.57758890232512));
#64768=CARTESIAN_POINT('Ctrl Pts',(42.5331204360856,6.15752874926381,-1.62755575142959));
#64769=CARTESIAN_POINT('Ctrl Pts',(42.5666437394049,6.34353097829547,-0.568957598971652));
#64770=CARTESIAN_POINT('Ctrl Pts',(42.6001670427241,6.26563217699923,0.469850984698985));
#64771=CARTESIAN_POINT('Ctrl Pts',(42.6336903460434,6.18773337570298,1.50865956836962));
#64772=CARTESIAN_POINT('Ctrl Pts',(42.6672136493627,5.84593354407884,2.52767858325296));
#64773=CARTESIAN_POINT('Ctrl Pts',(42.7007369526819,5.28167576459567,3.40335241239479));
#64774=CARTESIAN_POINT('Ctrl Pts',(42.7342602560012,4.71741798511252,4.27902624153659));
#64775=CARTESIAN_POINT('Ctrl Pts',(42.7677835593204,3.93070225777035,5.01135488493689));
#64776=CARTESIAN_POINT('Ctrl Pts',(42.8013068626397,3.01691752589568,5.51154380978815));
#64777=CARTESIAN_POINT('Ctrl Pts',(42.834830165959,2.10313279402099,6.01173273463943));
#64778=CARTESIAN_POINT('Ctrl Pts',(42.8683534692782,1.06227905761378,6.27978194094166));
#64779=CARTESIAN_POINT('Ctrl Pts',(42.9018767725975,0.0205593842150595,
6.28319057780292));
#64780=CARTESIAN_POINT('Ctrl Pts',(42.9354000759168,-1.02116028918366,6.28659921466418));
#64781=CARTESIAN_POINT('Ctrl Pts',(42.9689233792361,-2.06374589957381,6.02536728208448));
#64782=CARTESIAN_POINT('Ctrl Pts',(43.0024466825553,-2.98078439043953,5.53116903945113));
#64783=CARTESIAN_POINT('Ctrl Pts',(43.0359699858746,-3.89782288130523,5.03697079681779));
#64784=CARTESIAN_POINT('Ctrl Pts',(43.0694932891938,-4.6893142526465,4.30980624413073));
#64785=CARTESIAN_POINT('Ctrl Pts',(43.1030165925131,-5.2592905163573,3.43784377042135));
#64786=CARTESIAN_POINT('Ctrl Pts',(43.1365398958324,-5.82926678006814,2.56588129671191));
#64787=CARTESIAN_POINT('Ctrl Pts',(43.1700631991517,-6.17772793614856,1.54912090198006));
#64788=CARTESIAN_POINT('Ctrl Pts',(43.2035865024709,-6.2624232194065,0.510844346458796));
#64789=CARTESIAN_POINT('Ctrl Pts',(43.2090703864124,-6.27627803256008,0.34099866999205));
#64790=CARTESIAN_POINT('Ctrl Pts',(43.2145542703539,-6.2830745231639,0.170577225321256));
#64791=CARTESIAN_POINT('Ctrl Pts',(43.2200381542954,-6.28290773611714,0.000142516273084187));
#64792=CARTESIAN_POINT('Origin',(37.,0.,0.));
#64793=CARTESIAN_POINT('',(44.6762984310705,-6.28244611237991,-0.000146669898813401));
#64794=CARTESIAN_POINT('',(44.4900381542954,-6.28276315662069,-0.000157922487962832));
#64795=CARTESIAN_POINT('',(37.,-6.28269,-7.69407619853508E-16));
#64796=CARTESIAN_POINT('Ctrl Pts',(44.6762984310705,-6.28244611237991,-0.000146669898813401));
#64797=CARTESIAN_POINT('Ctrl Pts',(44.6531654688713,-6.28182129015504,0.718959259511916));
#64798=CARTESIAN_POINT('Ctrl Pts',(44.6300325066722,-6.15849154096994,1.43827402723654));
#64799=CARTESIAN_POINT('Ctrl Pts',(44.606899544473,-5.91650025717146,2.11516693349206));
#64800=CARTESIAN_POINT('Ctrl Pts',(44.5733762411537,-5.56581679789122,3.09609129655964));
#64801=CARTESIAN_POINT('Ctrl Pts',(44.5398529378345,-4.96593733257438,3.98792732547428));
#64802=CARTESIAN_POINT('Ctrl Pts',(44.5063296345153,-4.18959698819389,4.6825402855891));
#64803=CARTESIAN_POINT('Ctrl Pts',(44.472806331196,-3.41325664381335,5.37715324570395));
#64804=CARTESIAN_POINT('Ctrl Pts',(44.4392830278767,-2.46045542036912,5.87454313701897));
#64805=CARTESIAN_POINT('Ctrl Pts',(44.4057597245574,-1.44672005610452,6.11440164929595));
#64806=CARTESIAN_POINT('Ctrl Pts',(44.3722364212382,-0.432984691839915,
6.35426016157292));
#64807=CARTESIAN_POINT('Ctrl Pts',(44.3387131179189,0.641684813245083,6.33658729481186));
#64808=CARTESIAN_POINT('Ctrl Pts',(44.3051898145996,1.64698524421207,6.06352587650088));
#64809=CARTESIAN_POINT('Ctrl Pts',(44.2716665112804,2.65228567517911,5.79046445818989));
#64810=CARTESIAN_POINT('Ctrl Pts',(44.2381432079611,3.58821703202816,5.26201448832894));
#64811=CARTESIAN_POINT('Ctrl Pts',(44.2046199046418,4.34129804057951,4.54225029831125));
#64812=CARTESIAN_POINT('Ctrl Pts',(44.1710966013226,5.09437904913085,3.82248610829356));
#64813=CARTESIAN_POINT('Ctrl Pts',(44.1375732980033,5.66460970938452,2.91140769811911));
#64814=CARTESIAN_POINT('Ctrl Pts',(44.104049994684,5.98284979922019,1.91948293288038));
#64815=CARTESIAN_POINT('Ctrl Pts',(44.0705266913647,6.30108988905583,0.927558167641697));
#64816=CARTESIAN_POINT('Ctrl Pts',(44.0370033880455,6.36733940847352,-0.145212952661282));
#64817=CARTESIAN_POINT('Ctrl Pts',(44.0034800847262,6.17356563175858,-1.16875739142789));
#64818=CARTESIAN_POINT('Ctrl Pts',(43.969956781407,5.97979185504364,-2.19230183019453));
#64819=CARTESIAN_POINT('Ctrl Pts',(43.9364334780877,5.52599478219611,-3.16661958742472));
#64820=CARTESIAN_POINT('Ctrl Pts',(43.9029101747684,4.86719711297792,-3.97357505441478));
#64821=CARTESIAN_POINT('Ctrl Pts',(43.8693868714492,4.20839944375971,-4.78053052140487));
#64822=CARTESIAN_POINT('Ctrl Pts',(43.8358635681299,3.34460117817085,-5.42012369815475));
#64823=CARTESIAN_POINT('Ctrl Pts',(43.8023402648106,2.38053748412285,-5.81480418727356));
#64824=CARTESIAN_POINT('Ctrl Pts',(43.7688169614914,1.41647379007491,-6.20948467639234));
#64825=CARTESIAN_POINT('Ctrl Pts',(43.7352936581721,0.352144667567816,-6.35925247788009));
#64826=CARTESIAN_POINT('Ctrl Pts',(43.7017703548528,-0.683400435396939,
-6.24594831026861));
#64827=CARTESIAN_POINT('Ctrl Pts',(43.6682470515336,-1.71894553836169,-6.13264414265714));
#64828=CARTESIAN_POINT('Ctrl Pts',(43.6347237482143,-2.72570662178413,-5.75626800594644));
#64829=CARTESIAN_POINT('Ctrl Pts',(43.601200444895,-3.58161433762367,-5.16245534471501));
#64830=CARTESIAN_POINT('Ctrl Pts',(43.5676771415757,-4.43752205346327,-4.56864268348355));
#64831=CARTESIAN_POINT('Ctrl Pts',(43.5341538382565,-5.14257640171996,-3.75739349773132));
#64832=CARTESIAN_POINT('Ctrl Pts',(43.5006305349372,-5.61128984613312,-2.82707140205752));
#64833=CARTESIAN_POINT('Ctrl Pts',(43.469186500315,-6.05093153757615,-1.95445214053635));
#64834=CARTESIAN_POINT('Ctrl Pts',(43.4377424656927,-6.28264099937016,-0.977072783542306));
#64835=CARTESIAN_POINT('Ctrl Pts',(43.4062984310705,-6.2831673517952,6.56348350827965E-5));
#64836=CARTESIAN_POINT('Ctrl Pts',(43.2200381542954,-6.28290773611714,0.000142516273084187));
#64837=CARTESIAN_POINT('Ctrl Pts',(43.2480775736732,-6.2820549441907,-0.871300120826209));
#64838=CARTESIAN_POINT('Ctrl Pts',(43.276116993051,-6.09915862784975,-1.74308953341376));
#64839=CARTESIAN_POINT('Ctrl Pts',(43.3041564124287,-5.7469236826231,-2.5400343917704));
#64840=CARTESIAN_POINT('Ctrl Pts',(43.337679715748,-5.32579945214628,-3.49284385816776));
#64841=CARTESIAN_POINT('Ctrl Pts',(43.3712030190673,-4.66262158075713,-4.33867007465187));
#64842=CARTESIAN_POINT('Ctrl Pts',(43.4047263223865,-3.83780009992036,-4.97495697652974));
#64843=CARTESIAN_POINT('Ctrl Pts',(43.4382496257058,-3.01297861908352,-5.61124387840767));
#64844=CARTESIAN_POINT('Ctrl Pts',(43.4717729290251,-2.02651352879907,-6.03799146567932));
#64845=CARTESIAN_POINT('Ctrl Pts',(43.5052962323443,-0.998013296675183,
-6.20345677706633));
#64846=CARTESIAN_POINT('Ctrl Pts',(43.5388195356636,0.0304869354486183,
-6.36892208845333));
#64847=CARTESIAN_POINT('Ctrl Pts',(43.5723428389829,1.10102230941182,-6.2731051239557));
#64848=CARTESIAN_POINT('Ctrl Pts',(43.6058661423021,2.08379087189511,-5.92762364927779));
#64849=CARTESIAN_POINT('Ctrl Pts',(43.6393894456214,3.06655943437841,-5.58214217459987));
#64850=CARTESIAN_POINT('Ctrl Pts',(43.6729127489407,3.96156118538184,-4.98699618974166));
#64851=CARTESIAN_POINT('Ctrl Pts',(43.7064360522599,4.6602775478178,-4.21434688920786));
#64852=CARTESIAN_POINT('Ctrl Pts',(43.7399593555792,5.3589939102538,-3.44169758867402));
#64853=CARTESIAN_POINT('Ctrl Pts',(43.7734826588984,5.86142488412234,-2.49154497246454));
#64854=CARTESIAN_POINT('Ctrl Pts',(43.8070059622177,6.10665093009532,-1.47909463633556));
#64855=CARTESIAN_POINT('Ctrl Pts',(43.840529265537,6.3518769760683,-0.466644300206603));
#64856=CARTESIAN_POINT('Ctrl Pts',(43.8740525688563,6.33989809414575,0.608103755841807));
#64857=CARTESIAN_POINT('Ctrl Pts',(43.9075758721756,6.07216671860491,1.6148367926009));
#64858=CARTESIAN_POINT('Ctrl Pts',(43.9410991754948,5.80443534306408,2.62156982935996));
#64859=CARTESIAN_POINT('Ctrl Pts',(43.974622478814,5.28095147390495,3.56028784682966));
#64860=CARTESIAN_POINT('Ctrl Pts',(44.0081457821333,4.56518730494811,4.31717168942946));
#64861=CARTESIAN_POINT('Ctrl Pts',(44.0416690854526,3.84942313599124,5.07405553202931));
#64862=CARTESIAN_POINT('Ctrl Pts',(44.0751923887719,2.94137866723662,5.64910519975927));
#64863=CARTESIAN_POINT('Ctrl Pts',(44.1087156920912,1.95115389968543,5.97259616791668));
#64864=CARTESIAN_POINT('Ctrl Pts',(44.1422389954104,0.960929132134289,6.29608713607408));
#64865=CARTESIAN_POINT('Ctrl Pts',(44.1757622987296,-0.111475934213448,
6.36801940465896));
#64866=CARTESIAN_POINT('Ctrl Pts',(44.2092856020489,-1.13603264664161,6.17967121706609));
#64867=CARTESIAN_POINT('Ctrl Pts',(44.2428089053682,-2.16058935906979,5.99132302947322));
#64868=CARTESIAN_POINT('Ctrl Pts',(44.2763322086875,-3.13729771757836,5.54269438570263));
#64869=CARTESIAN_POINT('Ctrl Pts',(44.3098555120068,-3.94773225408754,4.88818131571524));
#64870=CARTESIAN_POINT('Ctrl Pts',(44.343378815326,-4.75816679059674,4.23366824572783));
#64871=CARTESIAN_POINT('Ctrl Pts',(44.3769021186452,-5.4023275051065,3.37327074952362));
#64872=CARTESIAN_POINT('Ctrl Pts',(44.4104254219645,-5.80211018823849,2.41131165318998));
#64873=CARTESIAN_POINT('Ctrl Pts',(44.4369629994081,-6.11858448712231,1.64980960867396));
#64874=CARTESIAN_POINT('Ctrl Pts',(44.4635005768518,-6.28191792026545,0.824663417087317));
#64875=CARTESIAN_POINT('Ctrl Pts',(44.4900381542954,-6.28276315662069,-0.000157922487962832));
#64876=CARTESIAN_POINT('Origin',(37.,0.,0.));
#64877=CARTESIAN_POINT('',(45.9462984310705,-6.28242372114921,0.000143169579051167));
#64878=CARTESIAN_POINT('',(45.7600381542954,-6.28221291207239,7.44799067214229E-5));
#64879=CARTESIAN_POINT('',(37.,-6.28269,-7.69407619853508E-16));
#64880=CARTESIAN_POINT('Ctrl Pts',(45.9462984310705,-6.28242372114921,0.000143169579051167));
#64881=CARTESIAN_POINT('Ctrl Pts',(45.9356350786884,-6.28270336338794,0.331625072851757));
#64882=CARTESIAN_POINT('Ctrl Pts',(45.9249717263064,-6.25692034458445,0.663063898107308));
#64883=CARTESIAN_POINT('Ctrl Pts',(45.9143083739244,-6.20469555259325,0.990282560321853));
#64884=CARTESIAN_POINT('Ctrl Pts',(45.8807850706052,-6.04051195629183,2.01898817485789));
#64885=CARTESIAN_POINT('Ctrl Pts',(45.8472617672859,-5.61499390834304,3.00598425704312));
#64886=CARTESIAN_POINT('Ctrl Pts',(45.8137384639667,-4.97973528891159,3.8315979567299));
#64887=CARTESIAN_POINT('Ctrl Pts',(45.7802151606474,-4.34447666948014,4.65721165641667));
#64888=CARTESIAN_POINT('Ctrl Pts',(45.7466918573281,-3.49947747856605,5.32144297360496));
#64889=CARTESIAN_POINT('Ctrl Pts',(45.7131685540089,-2.54719350436786,5.74375414698038));
#64890=CARTESIAN_POINT('Ctrl Pts',(45.6796452506896,-1.59490953016972,6.16606532035578));
#64891=CARTESIAN_POINT('Ctrl Pts',(45.6461219473703,-0.535340772687518,
6.34645634991833));
#64892=CARTESIAN_POINT('Ctrl Pts',(45.6125986440511,0.503040512287664,6.26305490097647));
#64893=CARTESIAN_POINT('Ctrl Pts',(45.5790753407318,1.54142179726296,6.17965345203461));
#64894=CARTESIAN_POINT('Ctrl Pts',(45.5455520374125,2.5586156097312,5.83245952458827));
#64895=CARTESIAN_POINT('Ctrl Pts',(45.5120287340933,3.43128763774544,5.26357023290308));
#64896=CARTESIAN_POINT('Ctrl Pts',(45.478505430774,4.30395966575968,4.69468094121789));
#64897=CARTESIAN_POINT('Ctrl Pts',(45.4449821274547,5.03210990931988,3.90409628529387));
#64898=CARTESIAN_POINT('Ctrl Pts',(45.4114588241355,5.52745046480069,2.9876743143828));
#64899=CARTESIAN_POINT('Ctrl Pts',(45.3779355208162,6.0227910202815,2.07125234347174));
#64900=CARTESIAN_POINT('Ctrl Pts',(45.3444122174969,6.28532188768291,1.02899305757366));
#64901=CARTESIAN_POINT('Ctrl Pts',(45.3108889141777,6.28321131232954,-0.0127300534996296));
#64902=CARTESIAN_POINT('Ctrl Pts',(45.2773656108584,6.28110073697618,-1.0544531645728));
#64903=CARTESIAN_POINT('Ctrl Pts',(45.2438423075391,6.01434871886806,-2.09564010082135));
#64904=CARTESIAN_POINT('Ctrl Pts',(45.2103190042198,5.51529882538695,-3.01004739436664));
#64905=CARTESIAN_POINT('Ctrl Pts',(45.1767957009006,5.01624893190582,-3.92445468791197));
#64906=CARTESIAN_POINT('Ctrl Pts',(45.1432723975813,4.28490116305167,-4.71208233875417));
#64907=CARTESIAN_POINT('Ctrl Pts',(45.1097490942621,3.40993112101547,-5.27743083323489));
#64908=CARTESIAN_POINT('Ctrl Pts',(45.0762257909428,2.53496107897927,-5.8427793277156));
#64909=CARTESIAN_POINT('Ctrl Pts',(45.0427024876235,1.51636876376106,-6.18584866583481));
#64910=CARTESIAN_POINT('Ctrl Pts',(45.0091791843042,0.477658055164268,-6.26504183800753));
#64911=CARTESIAN_POINT('Ctrl Pts',(44.975655880985,-0.561052653432527,-6.34423501018025));
#64912=CARTESIAN_POINT('Ctrl Pts',(44.9421325776657,-1.61988175540787,-6.15955201640649));
#64913=CARTESIAN_POINT('Ctrl Pts',(44.9086092743465,-2.57044667788251,-5.73338559019109));
#64914=CARTESIAN_POINT('Ctrl Pts',(44.8750859710272,-3.52101160035721,-5.30721916397567));
#64915=CARTESIAN_POINT('Ctrl Pts',(44.8415626677079,-4.36331234333117,-4.6395693053186));
#64916=CARTESIAN_POINT('Ctrl Pts',(44.8080393643886,-4.99522030425713,-3.81138827221596));
#64917=CARTESIAN_POINT('Ctrl Pts',(44.7745160610694,-5.6271282651831,-2.98320723911332));
#64918=CARTESIAN_POINT('Ctrl Pts',(44.7409927577501,-6.04864344406104,-1.99449503156515));
#64919=CARTESIAN_POINT('Ctrl Pts',(44.7074694544309,-6.2086573068782,-0.96513257918072));
#64920=CARTESIAN_POINT('Ctrl Pts',(44.6970791133107,-6.25825261682677,-0.646088035310425));
#64921=CARTESIAN_POINT('Ctrl Pts',(44.6866887721906,-6.28272675590493,-0.32313841837267));
#64922=CARTESIAN_POINT('Ctrl Pts',(44.6762984310705,-6.28244611237991,-0.000146669898813401));
#64923=CARTESIAN_POINT('Ctrl Pts',(44.4900381542954,-6.28276315662069,-0.000157922487962832));
#64924=CARTESIAN_POINT('Ctrl Pts',(44.4970238801711,-6.28298565581039,-0.217283083474969));
#64925=CARTESIAN_POINT('Ctrl Pts',(44.5040096060467,-6.27194857089511,-0.434385733912797));
#64926=CARTESIAN_POINT('Ctrl Pts',(44.5109953319224,-6.24948139636436,-0.650299009507491));
#64927=CARTESIAN_POINT('Ctrl Pts',(44.5445186352416,-6.14166526960405,-1.68642987940837));
#64928=CARTESIAN_POINT('Ctrl Pts',(44.5780419385609,-5.77062836432919,-2.69517092274707));
#64929=CARTESIAN_POINT('Ctrl Pts',(44.6115652418801,-5.18135874560474,-3.55421272219544));
#64930=CARTESIAN_POINT('Ctrl Pts',(44.6450885451994,-4.59208912688028,-4.41325452164384));
#64931=CARTESIAN_POINT('Ctrl Pts',(44.6786118485187,-3.78458679470619,-5.1225970772019));
#64932=CARTESIAN_POINT('Ctrl Pts',(44.712135151838,-2.85676105929807,-5.59623290931935));
#64933=CARTESIAN_POINT('Ctrl Pts',(44.7456584551572,-1.92893532388997,-6.06986874143678));
#64934=CARTESIAN_POINT('Ctrl Pts',(44.7791817584765,-0.88078618524785,-6.30779785011365));
#64935=CARTESIAN_POINT('Ctrl Pts',(44.8127050617957,0.160598724706423,-6.281171433331));
#64936=CARTESIAN_POINT('Ctrl Pts',(44.846228365115,1.2019836346607,-6.25454501654834));
#64937=CARTESIAN_POINT('Ctrl Pts',(44.8797516684343,2.23660431592705,-5.96336307430617));
#64938=CARTESIAN_POINT('Ctrl Pts',(44.9132749717535,3.13901345621759,-5.44293129177244));
#64939=CARTESIAN_POINT('Ctrl Pts',(44.9467982750728,4.04142259650808,-4.92249950923873));
#64940=CARTESIAN_POINT('Ctrl Pts',(44.9803215783921,4.81162019582283,-4.1728178864134));
#64941=CARTESIAN_POINT('Ctrl Pts',(45.0138448817113,5.35622012674883,-3.28478499739046));
#64942=CARTESIAN_POINT('Ctrl Pts',(45.0473681850306,5.90082005767485,-2.39675210836748));
#64943=CARTESIAN_POINT('Ctrl Pts',(45.0808914883498,6.21982232021221,-1.37036795314681));
#64944=CARTESIAN_POINT('Ctrl Pts',(45.1144147916691,6.27454802733141,-0.330081168778459));
#64945=CARTESIAN_POINT('Ctrl Pts',(45.1479380949884,6.32927373445062,0.710205615589953));
#64946=CARTESIAN_POINT('Ctrl Pts',(45.1814613983077,6.11972288615163,1.764395029106));
#64947=CARTESIAN_POINT('Ctrl Pts',(45.214984701627,5.671303432597,2.70466705911914));
#64948=CARTESIAN_POINT('Ctrl Pts',(45.2485080049462,5.22288397904237,3.64493908913229));
#64949=CARTESIAN_POINT('Ctrl Pts',(45.2820313082655,4.53559592023213,4.47129373564248));
#64950=CARTESIAN_POINT('Ctrl Pts',(45.3155546115847,3.69277263747835,5.08353585343527));
#64951=CARTESIAN_POINT('Ctrl Pts',(45.349077914904,2.84994935472466,5.695777971228));
#64952=CARTESIAN_POINT('Ctrl Pts',(45.3826012182233,1.85159084802752,6.09390756030336));
#64953=CARTESIAN_POINT('Ctrl Pts',(45.4161245215426,0.81874765661607,6.22965157934666));
#64954=CARTESIAN_POINT('Ctrl Pts',(45.4496478248618,-0.214095534795499,
6.36539559838998));
#64955=CARTESIAN_POINT('Ctrl Pts',(45.4831711281811,-1.28142341092133,6.23875404740119));
#64956=CARTESIAN_POINT('Ctrl Pts',(45.5166944315003,-2.25382292617444,5.86508215992932));
#64957=CARTESIAN_POINT('Ctrl Pts',(45.5502177348196,-3.22622244142749,5.49141027245747));
#64958=CARTESIAN_POINT('Ctrl Pts',(45.5837410381389,-4.10369359580792,4.87070804850249));
#64959=CARTESIAN_POINT('Ctrl Pts',(45.6172643414582,-4.77984338952302,4.07823536555993));
#64960=CARTESIAN_POINT('Ctrl Pts',(45.6507876447775,-5.45599318323813,3.28576268261738));
#64961=CARTESIAN_POINT('Ctrl Pts',(45.6843109480967,-5.93082161628803,2.32151954068721));
#64962=CARTESIAN_POINT('Ctrl Pts',(45.7178342514159,-6.14675594553841,1.30242000570432));
#64963=CARTESIAN_POINT('Ctrl Pts',(45.7319022190424,-6.23737222891632,0.87475751881359));
#64964=CARTESIAN_POINT('Ctrl Pts',(45.7459701866689,-6.28239623692835,0.437434604199986));
#64965=CARTESIAN_POINT('Ctrl Pts',(45.7600381542954,-6.28221291207239,7.44799067214229E-5));
#64966=CARTESIAN_POINT('Origin',(37.,0.,0.));
#64967=CARTESIAN_POINT('',(47.2162984310705,-6.28318057928199,-5.75008399550381E-5));
#64968=CARTESIAN_POINT('',(47.0300381542954,-6.28318961685052,5.11731766753689E-5));
#64969=CARTESIAN_POINT('',(37.,-6.28269,-7.69407619853508E-16));
#64970=CARTESIAN_POINT('Ctrl Pts',(47.2162984310705,-6.28318057928199,-5.75008399550381E-5));
#64971=CARTESIAN_POINT('Ctrl Pts',(47.1845813851863,-6.28270696309185,0.985558841135021));
#64972=CARTESIAN_POINT('Ctrl Pts',(47.1528643393022,-6.04681012366187,1.97139394049844));
#64973=CARTESIAN_POINT('Ctrl Pts',(47.1211472934181,-5.59978829242448,2.84978552345151));
#64974=CARTESIAN_POINT('Ctrl Pts',(47.0876239900988,-5.12730896715399,3.77820072252161));
#64975=CARTESIAN_POINT('Ctrl Pts',(47.0541006867795,-4.4189731699039,4.58658631969245));
#64976=CARTESIAN_POINT('Ctrl Pts',(47.0205773834603,-3.56066631121291,5.17692590924784));
#64977=CARTESIAN_POINT('Ctrl Pts',(46.987054080141,-2.70235945252192,5.76726549880322));
#64978=CARTESIAN_POINT('Ctrl Pts',(46.9535307768217,-1.69408153239001,6.13955908074314));
#64979=CARTESIAN_POINT('Ctrl Pts',(46.9200074735025,-0.658085814655917,
6.24866621849789));
#64980=CARTESIAN_POINT('Ctrl Pts',(46.8864841701832,0.377909903078239,6.35777335625264));
#64981=CARTESIAN_POINT('Ctrl Pts',(46.8529608668639,1.44162341841459,6.20369404982219));
#64982=CARTESIAN_POINT('Ctrl Pts',(46.8194375635447,2.40407992545615,5.80511034879328));
#64983=CARTESIAN_POINT('Ctrl Pts',(46.7859142602254,3.36653643249765,5.40652664776439));
#64984=CARTESIAN_POINT('Ctrl Pts',(46.7523909569062,4.22773593124438,4.76343855213707));
#64985=CARTESIAN_POINT('Ctrl Pts',(46.7188676535869,4.88325835314589,3.9538202167118));
#64986=CARTESIAN_POINT('Ctrl Pts',(46.6853443502676,5.53878077504741,3.14420188128653));
#64987=CARTESIAN_POINT('Ctrl Pts',(46.6518210469483,5.98862612010372,2.1680533060633));
#64988=CARTESIAN_POINT('Ctrl Pts',(46.6182977436291,6.17825083384663,1.14373208563958));
#64989=CARTESIAN_POINT('Ctrl Pts',(46.5847744403098,6.36787554758956,0.119410865215797));
#64990=CARTESIAN_POINT('Ctrl Pts',(46.5512511369906,6.29727963001906,-0.953083000408475));
#64991=CARTESIAN_POINT('Ctrl Pts',(46.5177278336713,5.97502280575507,-1.94371009164303));
#64992=CARTESIAN_POINT('Ctrl Pts',(46.484204530352,5.65276598149109,-2.93433718287752));
#64993=CARTESIAN_POINT('Ctrl Pts',(46.4506812270327,5.07884825053365,-3.8430974997223));
#64994=CARTESIAN_POINT('Ctrl Pts',(46.4171579237134,4.3228568907389,-4.55980424490342));
#64995=CARTESIAN_POINT('Ctrl Pts',(46.3836346203942,3.56686553094416,-5.27651099008454));
#64996=CARTESIAN_POINT('Ctrl Pts',(46.3501113170749,2.62880054231211,-5.801164163602));
#64997=CARTESIAN_POINT('Ctrl Pts',(46.3165880137557,1.62240190095777,-6.07014979398504));
#64998=CARTESIAN_POINT('Ctrl Pts',(46.2830647104364,0.616003259603381,-6.33913542436811));
#64999=CARTESIAN_POINT('Ctrl Pts',(46.2495414071171,-0.458729034473312,
-6.35245351161674));
#65000=CARTESIAN_POINT('Ctrl Pts',(46.2160181037979,-1.47148415319569,-6.10848924338433));
#65001=CARTESIAN_POINT('Ctrl Pts',(46.1824948004786,-2.484239271918,-5.86452497515194));
#65002=CARTESIAN_POINT('Ctrl Pts',(46.1489714971593,-3.43501721528601,-5.36327835143854));
#65003=CARTESIAN_POINT('Ctrl Pts',(46.1154481938401,-4.20853656689479,-4.66552530962565));
#65004=CARTESIAN_POINT('Ctrl Pts',(46.0819248905208,-4.98205591850362,-3.96777226781271));
#65005=CARTESIAN_POINT('Ctrl Pts',(46.0484015872015,-5.57831667835322,-3.07351280790027));
#65006=CARTESIAN_POINT('Ctrl Pts',(46.0148782838823,-5.92502248595098,-2.0911755045006));
#65007=CARTESIAN_POINT('Ctrl Pts',(45.992018332945,-6.16144542064411,-1.42130767119992));
#65008=CARTESIAN_POINT('Ctrl Pts',(45.9691583820077,-6.28182422789153,-0.710483261391549));
#65009=CARTESIAN_POINT('Ctrl Pts',(45.9462984310705,-6.28242372114921,0.000143169579051167));
#65010=CARTESIAN_POINT('Ctrl Pts',(45.7600381542954,-6.28221291207239,7.44799067214229E-5));
#65011=CARTESIAN_POINT('Ctrl Pts',(45.7794934899882,-6.28195938244337,-0.604773943310985));
#65012=CARTESIAN_POINT('Ctrl Pts',(45.798948825681,-6.19524418226229,-1.20969353221928));
#65013=CARTESIAN_POINT('Ctrl Pts',(45.8184041613738,-6.02308547606459,-1.78923108437408));
#65014=CARTESIAN_POINT('Ctrl Pts',(45.851927464693,-5.7264404518895,-2.7878267114341));
#65015=CARTESIAN_POINT('Ctrl Pts',(45.8854507680123,-5.17611017808843,-3.71106203751854));
#65016=CARTESIAN_POINT('Ctrl Pts',(45.9189740713315,-4.43882196348974,-4.44699517671334));
#65017=CARTESIAN_POINT('Ctrl Pts',(45.9524973746508,-3.7015337488911,-5.1829283159081));
#65018=CARTESIAN_POINT('Ctrl Pts',(45.9860206779701,-2.77728759349483,-5.73155926821328));
#65019=CARTESIAN_POINT('Ctrl Pts',(46.0195439812894,-1.77814794583397,-6.02636676680047));
#65020=CARTESIAN_POINT('Ctrl Pts',(46.0530672846086,-0.779008298173049,
-6.32117426538768));
#65021=CARTESIAN_POINT('Ctrl Pts',(46.0865905879279,0.295024841752511,-6.36215831025689));
#65022=CARTESIAN_POINT('Ctrl Pts',(46.1201138912471,1.31372541800596,-6.14434960360783));
#65023=CARTESIAN_POINT('Ctrl Pts',(46.1536371945664,2.33242599425934,-5.92654089695879));
#65024=CARTESIAN_POINT('Ctrl Pts',(46.1871604978857,3.29579400684066,-5.4499394387915));
#65025=CARTESIAN_POINT('Ctrl Pts',(46.220683801205,4.08702149887179,-4.77233295077266));
#65026=CARTESIAN_POINT('Ctrl Pts',(46.2542071045243,4.87824899090288,-4.09472646275386));
#65027=CARTESIAN_POINT('Ctrl Pts',(46.2877304078435,5.49733596238385,-3.21611494488349));
#65028=CARTESIAN_POINT('Ctrl Pts',(46.3212537111627,5.86921838448651,-2.24302966553638));
#65029=CARTESIAN_POINT('Ctrl Pts',(46.354777014482,6.24110080658921,-1.26994438618916));
#65030=CARTESIAN_POINT('Ctrl Pts',(46.3883003178013,6.36577867931357,-0.202385345365309));
#65031=CARTESIAN_POINT('Ctrl Pts',(46.4218236211206,6.22813486425494,0.830206382728294));
#65032=CARTESIAN_POINT('Ctrl Pts',(46.4553469244398,6.0904910491963,1.86279811082196));
#65033=CARTESIAN_POINT('Ctrl Pts',(46.4888702277591,5.69052554635458,2.86042252618523));
#65034=CARTESIAN_POINT('Ctrl Pts',(46.5223935310784,5.0767340007985,3.70211809784712));
#65035=CARTESIAN_POINT('Ctrl Pts',(46.5559168343976,4.46294245524248,4.54381366950891));
#65036=CARTESIAN_POINT('Ctrl Pts',(46.5894401377169,3.63532486697211,5.22958039746938));
#65037=CARTESIAN_POINT('Ctrl Pts',(46.6229634410362,2.69422951234673,5.67626936112713));
#65038=CARTESIAN_POINT('Ctrl Pts',(46.6564867443554,1.75313415772135,6.12295832478488));
#65039=CARTESIAN_POINT('Ctrl Pts',(46.6900100476747,0.698561036740914,6.33056952413993));
#65040=CARTESIAN_POINT('Ctrl Pts',(46.723533350994,-0.34162331357906,6.27393019062931));
#65041=CARTESIAN_POINT('Ctrl Pts',(46.7570566543132,-1.38180766389903,6.21729085711869));
#65042=CARTESIAN_POINT('Ctrl Pts',(46.7905799576325,-2.40760324355858,5.8964009907424));
#65043=CARTESIAN_POINT('Ctrl Pts',(46.8241032609518,-3.29463278004108,5.35016834968298));
#65044=CARTESIAN_POINT('Ctrl Pts',(46.857626564271,-4.18166231652358,4.80393570862355));
#65045=CARTESIAN_POINT('Ctrl Pts',(46.8911498675903,-4.92992580982906,4.03236029288097));
#65046=CARTESIAN_POINT('Ctrl Pts',(46.9246731709096,-5.44869663345755,3.12899528951692));
#65047=CARTESIAN_POINT('Ctrl Pts',(46.9581964742288,-5.96746745708607,2.22563028615281));
#65048=CARTESIAN_POINT('Ctrl Pts',(46.9917197775481,-6.25674561103759,1.1904756951672));
#65049=CARTESIAN_POINT('Ctrl Pts',(47.0252430808674,-6.28145624365494,0.149043565171735));
#65050=CARTESIAN_POINT('Ctrl Pts',(47.0268414386767,-6.28263442207732,0.0993891154884421));
#65051=CARTESIAN_POINT('Ctrl Pts',(47.0284397964861,-6.28321116240861,0.0497203951529533));
#65052=CARTESIAN_POINT('Ctrl Pts',(47.0300381542954,-6.28318961685052,5.11731766753689E-5));
#65053=CARTESIAN_POINT('Origin',(37.,0.,0.));
#65054=CARTESIAN_POINT('',(48.4862984310705,-6.28220485483637,-6.9117828764842E-5));
#65055=CARTESIAN_POINT('',(48.3000381542954,-6.28240712885383,-0.000140271569211771));
#65056=CARTESIAN_POINT('',(37.,-6.28269,-7.69407619853508E-16));
#65057=CARTESIAN_POINT('Ctrl Pts',(48.4862984310705,-6.28220485483637,-6.9117828764842E-5));
#65058=CARTESIAN_POINT('Ctrl Pts',(48.4670509950035,-6.28197246600328,0.598318092477962));
#65059=CARTESIAN_POINT('Ctrl Pts',(48.4478035589365,-6.19712683672702,1.19676983422775));
#65060=CARTESIAN_POINT('Ctrl Pts',(48.4285561228695,-6.02857778477818,1.77063727017338));
#65061=CARTESIAN_POINT('Ctrl Pts',(48.3950328195502,-5.73501551638082,2.77014349288841));
#65062=CARTESIAN_POINT('Ctrl Pts',(48.361509516231,-5.18753666879845,3.69507256413081));
#65063=CARTESIAN_POINT('Ctrl Pts',(48.3279862129117,-4.4525228166577,4.43327723211516));
#65064=CARTESIAN_POINT('Ctrl Pts',(48.2944629095924,-3.71750896451704,5.17148190009943));
#65065=CARTESIAN_POINT('Ctrl Pts',(48.2609396062731,-2.79496010781804,5.72296216482569));
#65066=CARTESIAN_POINT('Ctrl Pts',(48.2274163029539,-1.7967348983572,6.02085128156089));
#65067=CARTESIAN_POINT('Ctrl Pts',(48.1938929996346,-0.798509688896358,
6.3187403982961));
#65068=CARTESIAN_POINT('Ctrl Pts',(48.1603696963154,0.275391873326325,6.36303836704025));
#65069=CARTESIAN_POINT('Ctrl Pts',(48.1268463929961,1.29475968611398,6.14837407814961));
#65070=CARTESIAN_POINT('Ctrl Pts',(48.0933230896769,2.3141274989017,5.93370978925896));
#65071=CARTESIAN_POINT('Ctrl Pts',(48.0597997863575,3.27896156225439,5.46008324273347));
#65072=CARTESIAN_POINT('Ctrl Pts',(48.0262764830383,4.07227616126894,4.78492145348372));
#65073=CARTESIAN_POINT('Ctrl Pts',(47.992753179719,4.86559076028345,4.10975966423401));
#65074=CARTESIAN_POINT('Ctrl Pts',(47.9592298763998,5.48738589495984,3.23306263226006));
#65075=CARTESIAN_POINT('Ctrl Pts',(47.9257065730805,5.86226917284815,2.26112949534572));
#65076=CARTESIAN_POINT('Ctrl Pts',(47.8921832697613,6.23715245073648,1.28919635843133));
#65077=CARTESIAN_POINT('Ctrl Pts',(47.8586599664419,6.36512387183669,0.222027116576553));
#65078=CARTESIAN_POINT('Ctrl Pts',(47.8251366631227,6.23066695642113,-0.810984418968658));
#65079=CARTESIAN_POINT('Ctrl Pts',(47.7916133598034,6.09621004100557,-1.84399595451381));
#65080=CARTESIAN_POINT('Ctrl Pts',(47.7580900564842,5.69932478907427,-2.8428497837494));
#65081=CARTESIAN_POINT('Ctrl Pts',(47.7245667531649,5.08813336659879,-3.68643530980162));
#65082=CARTESIAN_POINT('Ctrl Pts',(47.6910434498457,4.4769419441233,-4.53002083585385));
#65083=CARTESIAN_POINT('Ctrl Pts',(47.6575201465264,3.65144435110363,-5.21833805872271));
#65084=CARTESIAN_POINT('Ctrl Pts',(47.6239968432071,2.7117318153874,-5.66792881139697));
#65085=CARTESIAN_POINT('Ctrl Pts',(47.5904735398878,1.77201927967118,-6.11751956407122));
#65086=CARTESIAN_POINT('Ctrl Pts',(47.5569502365686,0.718091801258396,-6.32838384655087));
#65087=CARTESIAN_POINT('Ctrl Pts',(47.5234269332493,-0.32226236671889,-6.27495445534426));
#65088=CARTESIAN_POINT('Ctrl Pts',(47.48990362993,-1.36261653469624,-6.22152506413766));
#65089=CARTESIAN_POINT('Ctrl Pts',(47.4563803266108,-2.38939739223809,-5.90380199924476));
#65090=CARTESIAN_POINT('Ctrl Pts',(47.4228570232915,-3.27810820230869,-5.36030904553129));
#65091=CARTESIAN_POINT('Ctrl Pts',(47.3893337199722,-4.16681901237924,-4.81681609181785));
#65092=CARTESIAN_POINT('Ctrl Pts',(47.355810416653,-4.91745977497856,-4.04755324928385));
#65093=CARTESIAN_POINT('Ctrl Pts',(47.3222871133337,-5.43901562072804,-3.14579330648479));
#65094=CARTESIAN_POINT('Ctrl Pts',(47.2887638100144,-5.96057146647754,-2.24403336368567));
#65095=CARTESIAN_POINT('Ctrl Pts',(47.2552405066951,-6.25304239537717,-1.20977632062147));
#65096=CARTESIAN_POINT('Ctrl Pts',(47.2217172033759,-6.28096643318152,-0.168425398604667));
#65097=CARTESIAN_POINT('Ctrl Pts',(47.2199109459407,-6.28247099854081,-0.11231673211768));
#65098=CARTESIAN_POINT('Ctrl Pts',(47.2181046885056,-6.28320755130102,-0.0561874712158831));
#65099=CARTESIAN_POINT('Ctrl Pts',(47.2162984310705,-6.28318057928199,-5.75008399550381E-5));
#65100=CARTESIAN_POINT('Ctrl Pts',(47.0300381542954,-6.28318961685052,5.11731766753689E-5));
#65101=CARTESIAN_POINT('Ctrl Pts',(47.0619630998053,-6.28275927468073,-0.992021562876977));
#65102=CARTESIAN_POINT('Ctrl Pts',(47.0938880453153,-6.04364615948199,-1.98429442568766));
#65103=CARTESIAN_POINT('Ctrl Pts',(47.1258129908252,-5.59096812202356,-2.86705109542662));
#65104=CARTESIAN_POINT('Ctrl Pts',(47.1593362941445,-5.11562625649168,-3.79400395702412));
#65105=CARTESIAN_POINT('Ctrl Pts',(47.1928595974637,-4.40479941414474,-4.60020001121386));
#65106=CARTESIAN_POINT('Ctrl Pts',(47.226382900783,-3.54467504366722,-5.18788833342367));
#65107=CARTESIAN_POINT('Ctrl Pts',(47.2599062041023,-2.68455067318971,-5.77557665563349));
#65108=CARTESIAN_POINT('Ctrl Pts',(47.2934295074215,-1.67512877458163,-6.14475724586337));
#65109=CARTESIAN_POINT('Ctrl Pts',(47.3269528107408,-0.638801318579545,
-6.25066711644859));
#65110=CARTESIAN_POINT('Ctrl Pts',(47.36047611406,0.397526137422538,-6.3565769870338));
#65111=CARTESIAN_POINT('Ctrl Pts',(47.3939994173793,1.46075915081862,-6.19921613797434));
#65112=CARTESIAN_POINT('Ctrl Pts',(47.4275227206986,2.42198117636517,-5.79766450448829));
#65113=CARTESIAN_POINT('Ctrl Pts',(47.4610460240179,3.38320320191172,-5.39611287100225));
#65114=CARTESIAN_POINT('Ctrl Pts',(47.4945693273371,4.24241423960874,-4.75037045308961));
#65115=CARTESIAN_POINT('Ctrl Pts',(47.5280926306564,4.89543532095221,-3.93873324098551));
#65116=CARTESIAN_POINT('Ctrl Pts',(47.5616159339756,5.54845640229572,-3.12709602888136));
#65117=CARTESIAN_POINT('Ctrl Pts',(47.5951392372949,5.99528752728566,-2.14956402258571));
#65118=CARTESIAN_POINT('Ctrl Pts',(47.6286625406142,6.18175061433953,-1.12466255711813));
#65119=CARTESIAN_POINT('Ctrl Pts',(47.6621858439335,6.36821370139339,-0.0997610916506096));
#65120=CARTESIAN_POINT('Ctrl Pts',(47.6957091472527,6.2943087505112,0.972509832988839));
#65121=CARTESIAN_POINT('Ctrl Pts',(47.729232450572,5.96899670517768,1.96213782870847));
#65122=CARTESIAN_POINT('Ctrl Pts',(47.7627557538913,5.64368465984415,2.95176582442809));
#65123=CARTESIAN_POINT('Ctrl Pts',(47.7962790572105,5.06696552005929,3.8587508912279));
#65124=CARTESIAN_POINT('Ctrl Pts',(47.8298023605298,4.30876623329383,4.57312148013779));
#65125=CARTESIAN_POINT('Ctrl Pts',(47.8633256638491,3.55056694652832,5.28749206904772));
#65126=CARTESIAN_POINT('Ctrl Pts',(47.8968489671683,2.61088751278218,5.80924818006771));
#65127=CARTESIAN_POINT('Ctrl Pts',(47.9303722704876,1.60366365894564,6.0751271093079));
#65128=CARTESIAN_POINT('Ctrl Pts',(47.9638955738069,0.59643980510915,6.34100603854808));
#65129=CARTESIAN_POINT('Ctrl Pts',(47.9974188771261,-0.478328468817734,
6.35100778600848));
#65130=CARTESIAN_POINT('Ctrl Pts',(48.0309421804454,-1.49032597221706,6.10391964411443));
#65131=CARTESIAN_POINT('Ctrl Pts',(48.0644654837646,-2.50232347561639,5.85683150222037));
#65132=CARTESIAN_POINT('Ctrl Pts',(48.0979887870839,-3.45155020848816,5.35265347097187));
#65133=CARTESIAN_POINT('Ctrl Pts',(48.1315120904032,-4.22291283803247,4.65251691965233));
#65134=CARTESIAN_POINT('Ctrl Pts',(48.1650353937225,-4.99427546757683,3.95238036833276));
#65135=CARTESIAN_POINT('Ctrl Pts',(48.1985586970417,-5.5877739937937,3.05628529694214));
#65136=CARTESIAN_POINT('Ctrl Pts',(48.232082000361,-5.93144697582958,2.07288284719442));
#65137=CARTESIAN_POINT('Ctrl Pts',(48.2547340516725,-6.16367045181887,1.40838739042628));
#65138=CARTESIAN_POINT('Ctrl Pts',(48.2773861029839,-6.2818273788379,0.704028710778029));
#65139=CARTESIAN_POINT('Ctrl Pts',(48.3000381542954,-6.28240712885383,-0.000140271569211771));
#65140=CARTESIAN_POINT('Origin',(37.,0.,0.));
#65141=CARTESIAN_POINT('',(49.7562984310704,-6.28278348713276,0.000156540911899483));
#65142=CARTESIAN_POINT('',(49.5700381542954,-6.28246359837908,0.000149097063601992));
#65143=CARTESIAN_POINT('',(37.,-6.28269,-7.69407619853508E-16));
#65144=CARTESIAN_POINT('Ctrl Pts',(49.7562984310704,-6.28278348713276,0.000156540911899483));
#65145=CARTESIAN_POINT('Ctrl Pts',(49.7495206048206,-6.28299901254035,0.210817954556831));
#65146=CARTESIAN_POINT('Ctrl Pts',(49.7427427785708,-6.27261027340816,0.421458208397696));
#65147=CARTESIAN_POINT('Ctrl Pts',(49.7359649523209,-6.25145825089702,0.63101203391033));
#65148=CARTESIAN_POINT('Ctrl Pts',(49.7024416490017,-6.14683980239764,1.66747065580799));
#65149=CARTESIAN_POINT('Ctrl Pts',(49.6689183456824,-5.77891731260458,2.67735179578619));
#65150=CARTESIAN_POINT('Ctrl Pts',(49.6353950423631,-5.19230122504616,3.53820780028988));
#65151=CARTESIAN_POINT('Ctrl Pts',(49.6018717390439,-4.60568513748774,4.39906380479358));
#65152=CARTESIAN_POINT('Ctrl Pts',(49.5683484357246,-3.80037545216395,5.11089467382279));
#65153=CARTESIAN_POINT('Ctrl Pts',(49.5348251324053,-2.87401562180346,5.58739122088992));
#65154=CARTESIAN_POINT('Ctrl Pts',(49.501301829086,-1.94765579144292,6.06388776795708));
#65155=CARTESIAN_POINT('Ctrl Pts',(49.4677785257668,-0.900245816045651,
6.30504999306214));
#65156=CARTESIAN_POINT('Ctrl Pts',(49.4342552224475,0.141216295691665,6.2816370802108));
#65157=CARTESIAN_POINT('Ctrl Pts',(49.4007319191283,1.18267840742892,6.25822416735945));
#65158=CARTESIAN_POINT('Ctrl Pts',(49.367208615809,2.21819265550626,5.97023611655172));
#65159=CARTESIAN_POINT('Ctrl Pts',(49.3336853124897,3.12220338304444,5.45259135499387));
#65160=CARTESIAN_POINT('Ctrl Pts',(49.3001620091704,4.02621411058273,4.93494659343596));
#65161=CARTESIAN_POINT('Ctrl Pts',(49.2666387058512,4.79872131758188,4.18764512112786));
#65162=CARTESIAN_POINT('Ctrl Pts',(49.2331154025319,5.34605883769137,3.30129691993769));
#65163=CARTESIAN_POINT('Ctrl Pts',(49.1995920992126,5.89339635780079,2.41494871874763));
#65164=CARTESIAN_POINT('Ctrl Pts',(49.1660687958934,6.21556419102064,1.38955378867549));
#65165=CARTESIAN_POINT('Ctrl Pts',(49.1325454925741,6.27349962623864,0.349440823647891));
#65166=CARTESIAN_POINT('Ctrl Pts',(49.0990221892548,6.33143506145664,-0.690672141379647));
#65167=CARTESIAN_POINT('Ctrl Pts',(49.0654988859356,6.12513809867287,-1.74550314136252));
#65168=CARTESIAN_POINT('Ctrl Pts',(49.0319755826163,5.67962215583164,-2.68715437156751));
#65169=CARTESIAN_POINT('Ctrl Pts',(48.9984522792971,5.23410621299034,-3.62880560177266));
#65170=CARTESIAN_POINT('Ctrl Pts',(48.9649289759778,4.54937129009149,-4.45727706219976));
#65171=CARTESIAN_POINT('Ctrl Pts',(48.9314056726585,3.70844120181689,-5.07211694485794));
#65172=CARTESIAN_POINT('Ctrl Pts',(48.8978823693393,2.86751111354239,-5.68695682751605));
#65173=CARTESIAN_POINT('Ctrl Pts',(48.86435906602,1.87038585989214,-6.08816513240533));
#65174=CARTESIAN_POINT('Ctrl Pts',(48.8308357627007,0.837966448694264,-6.22709552524375));
#65175=CARTESIAN_POINT('Ctrl Pts',(48.7973124593814,-0.194452962503611,
-6.36602591808218));
#65176=CARTESIAN_POINT('Ctrl Pts',(48.7637891560622,-1.26216653124915,-6.24267839886975));
#65177=CARTESIAN_POINT('Ctrl Pts',(48.7302658527429,-2.23571444689116,-5.87200880122044));
#65178=CARTESIAN_POINT('Ctrl Pts',(48.6967425494236,-3.20926236253323,-5.5013392035711));
#65179=CARTESIAN_POINT('Ctrl Pts',(48.6632192461044,-4.08864462507178,-4.88334752748483));
#65180=CARTESIAN_POINT('Ctrl Pts',(48.6296959427851,-4.76723651367273,-4.09296499769465));
#65181=CARTESIAN_POINT('Ctrl Pts',(48.5961726394658,-5.44582840227364,-3.30258246790451));
#65182=CARTESIAN_POINT('Ctrl Pts',(48.5626493361466,-5.92362991693698,-2.33980908441044));
#65183=CARTESIAN_POINT('Ctrl Pts',(48.5291260328273,-6.14270782966245,-1.32138070556966));
#65184=CARTESIAN_POINT('Ctrl Pts',(48.514850165575,-6.23600195316186,-0.887683936375279));
#65185=CARTESIAN_POINT('Ctrl Pts',(48.5005742983228,-6.28237721816416,-0.443894277194152));
#65186=CARTESIAN_POINT('Ctrl Pts',(48.4862984310705,-6.28220485483637,-6.9117828764842E-5));
#65187=CARTESIAN_POINT('Ctrl Pts',(48.3000381542954,-6.28240712885383,-0.000140271569211771));
#65188=CARTESIAN_POINT('Ctrl Pts',(48.3109094063032,-6.28268536451726,-0.338087522257749));
#65189=CARTESIAN_POINT('Ctrl Pts',(48.321780658311,-6.25588245148254,-0.675991080616301));
#65190=CARTESIAN_POINT('Ctrl Pts',(48.3326519103188,-6.2016103279476,-1.00942353131101));
#65191=CARTESIAN_POINT('Ctrl Pts',(48.3661752136381,-6.03425326017489,-2.03761763196401));
#65192=CARTESIAN_POINT('Ctrl Pts',(48.3996985169573,-5.60569168677457,-3.02329600516527));
#65193=CARTESIAN_POINT('Ctrl Pts',(48.4332218202766,-4.9678885140624,-3.84694557241424));
#65194=CARTESIAN_POINT('Ctrl Pts',(48.4667451235959,-4.33008534135019,-4.67059513966326));
#65195=CARTESIAN_POINT('Ctrl Pts',(48.5002684269152,-3.48304056932611,-5.33221590095997));
#65196=CARTESIAN_POINT('Ctrl Pts',(48.5337917302344,-2.52945801201786,-5.75158662376821));
#65197=CARTESIAN_POINT('Ctrl Pts',(48.5673150335537,-1.57587545470966,-6.17095734657642));
#65198=CARTESIAN_POINT('Ctrl Pts',(48.6008383368729,-0.515755112117303,
-6.34807803089618));
#65199=CARTESIAN_POINT('Ctrl Pts',(48.6343616401922,0.522363880510887,-6.261472869989));
#65200=CARTESIAN_POINT('Ctrl Pts',(48.6678849435115,1.56048287313908,-6.17486770908183));
#65201=CARTESIAN_POINT('Ctrl Pts',(48.7014082468308,2.5766005158031,-5.82453670294771));
#65202=CARTESIAN_POINT('Ctrl Pts',(48.73493155015,3.44751298168156,-5.25295733529293));
#65203=CARTESIAN_POINT('Ctrl Pts',(48.7684548534693,4.31842544756001,-4.68137796763816));
#65204=CARTESIAN_POINT('Ctrl Pts',(48.8019781567885,5.04413273665289,-3.88855023846271));
#65205=CARTESIAN_POINT('Ctrl Pts',(48.8355014601078,5.53664315251252,-2.9706041686847));
#65206=CARTESIAN_POINT('Ctrl Pts',(48.869024763427,6.02915356837218,-2.05265809890663));
#65207=CARTESIAN_POINT('Ctrl Pts',(48.9025480667464,6.28846711099855,-1.00959368852598));
#65208=CARTESIAN_POINT('Ctrl Pts',(48.9360713700656,6.28314212496046,0.032117951648468));
#65209=CARTESIAN_POINT('Ctrl Pts',(48.9695946733849,6.27781713892237,1.07382959182286));
#65210=CARTESIAN_POINT('Ctrl Pts',(49.0031179767041,6.00785362421983,2.11418846179105));
#65211=CARTESIAN_POINT('Ctrl Pts',(49.0366412800234,5.50598454081438,3.02705149635478));
#65212=CARTESIAN_POINT('Ctrl Pts',(49.0701645833427,5.0041154574089,3.93991453091856));
#65213=CARTESIAN_POINT('Ctrl Pts',(49.103687886662,4.27034080530048,4.72528173007786));
#65214=CARTESIAN_POINT('Ctrl Pts',(49.1372111899812,3.39363044523012,5.28792765896791));
#65215=CARTESIAN_POINT('Ctrl Pts',(49.1707344933005,2.51692008515981,5.85057358785794));
#65216=CARTESIAN_POINT('Ctrl Pts',(49.2042577966197,1.49727401712759,6.19049824647874));
#65217=CARTESIAN_POINT('Ctrl Pts',(49.237781099939,0.458323888012076,6.266485916281));
#65218=CARTESIAN_POINT('Ctrl Pts',(49.2713044032583,-0.58062624110344,6.34247358608326));
#65219=CARTESIAN_POINT('Ctrl Pts',(49.3048277065776,-1.63888043130225,6.15452426706698));
#65220=CARTESIAN_POINT('Ctrl Pts',(49.3383510098968,-2.58812581751054,5.72542673326679));
#65221=CARTESIAN_POINT('Ctrl Pts',(49.3718743132161,-3.53737120371888,5.29632919946658));
#65222=CARTESIAN_POINT('Ctrl Pts',(49.4053976165353,-4.37760778593669,4.62608345088244));
#65223=CARTESIAN_POINT('Ctrl Pts',(49.4389209198546,-5.00695724021992,3.79595649604682));
#65224=CARTESIAN_POINT('Ctrl Pts',(49.4724442231739,-5.6363066945031,2.96582954121125));
#65225=CARTESIAN_POINT('Ctrl Pts',(49.5059675264932,-6.05476902085173,1.97582138012422));
#65226=CARTESIAN_POINT('Ctrl Pts',(49.5394908298125,-6.21160584230822,0.945970076203819));
#65227=CARTESIAN_POINT('Ctrl Pts',(49.5496732713068,-6.25924380159368,0.633160787985427));
#65228=CARTESIAN_POINT('Ctrl Pts',(49.5598557128011,-6.28274437057092,0.31667559863472));
#65229=CARTESIAN_POINT('Ctrl Pts',(49.5700381542954,-6.28246359837908,0.000149097063601992));
#65230=CARTESIAN_POINT('Origin',(37.,0.,0.));
#65231=CARTESIAN_POINT('',(51.0262984310705,-6.28288820464993,-0.000145391911651194));
#65232=CARTESIAN_POINT('',(50.8400381542954,-6.28315629679635,-7.16818851180851E-5));
#65233=CARTESIAN_POINT('',(37.,-6.28269,-7.69407619853508E-16));
#65234=CARTESIAN_POINT('Ctrl Pts',(51.0262984310705,-6.28288820464993,-0.000145391911651194));
#65235=CARTESIAN_POINT('Ctrl Pts',(50.9984669113185,-6.28203197644536,0.864843652156353));
#65236=CARTESIAN_POINT('Ctrl Pts',(50.9706353915665,-6.10191477910553,1.73017821842932));
#65237=CARTESIAN_POINT('Ctrl Pts',(50.9428038718145,-5.75473404259442,2.5222891485024));
#65238=CARTESIAN_POINT('Ctrl Pts',(50.9092805684953,-5.33655187933529,3.47639353115891));
#65239=CARTESIAN_POINT('Ctrl Pts',(50.875757265176,-4.67598711202248,4.32426207259923));
#65240=CARTESIAN_POINT('Ctrl Pts',(50.8422339618567,-3.85313293437611,4.96309107710852));
#65241=CARTESIAN_POINT('Ctrl Pts',(50.8087106585375,-3.03027875672973,5.60192008161782));
#65242=CARTESIAN_POINT('Ctrl Pts',(50.7751873552182,-2.04513516874982,6.03170954919608));
#65243=CARTESIAN_POINT('Ctrl Pts',(50.7416640518989,-1.01715040645896,6.200347691887));
#65244=CARTESIAN_POINT('Ctrl Pts',(50.7081407485797,0.010834355831897,6.36898583457792));
#65245=CARTESIAN_POINT('Ctrl Pts',(50.6746174452604,1.08166029243366,6.2764726523815));
#65246=CARTESIAN_POINT('Ctrl Pts',(50.6410941419412,2.06549021943224,5.93402532882005));
#65247=CARTESIAN_POINT('Ctrl Pts',(50.6075708386219,3.04932014643076,5.59157800525862));
#65248=CARTESIAN_POINT('Ctrl Pts',(50.5740475353026,3.94615406382622,4.99919654033207));
#65249=CARTESIAN_POINT('Ctrl Pts',(50.5405242319833,4.64725124514435,4.22870693169346));
#65250=CARTESIAN_POINT('Ctrl Pts',(50.5070009286641,5.34834842646256,3.45821732305477));
#65251=CARTESIAN_POINT('Ctrl Pts',(50.4734776253448,5.85370887170347,2.50961957070406));
#65252=CARTESIAN_POINT('Ctrl Pts',(50.4399543220256,6.10205784439616,1.49793074382345));
#65253=CARTESIAN_POINT('Ctrl Pts',(50.4064310187063,6.35040681708886,0.486241916942795));
#65254=CARTESIAN_POINT('Ctrl Pts',(50.372907715387,6.3417443172332,-0.588537984467577));
#65255=CARTESIAN_POINT('Ctrl Pts',(50.3393844120677,6.07712066920823,-1.59609235996233));
#65256=CARTESIAN_POINT('Ctrl Pts',(50.3058611087484,5.81249702118332,-2.60364673545692));
#65257=CARTESIAN_POINT('Ctrl Pts',(50.2723378054292,5.29191222498908,-3.54397558503604));
#65258=CARTESIAN_POINT('Ctrl Pts',(50.23881450211,4.57848696309705,-4.303064440419));
#65259=CARTESIAN_POINT('Ctrl Pts',(50.2052911987907,3.86506170120498,-5.06215329580199));
#65260=CARTESIAN_POINT('Ctrl Pts',(50.1717678954714,2.95879597361505,-5.64000215698894));
#65261=CARTESIAN_POINT('Ctrl Pts',(50.1382445921521,1.96957410972775,-5.96654709827537));
#65262=CARTESIAN_POINT('Ctrl Pts',(50.1047212888328,0.980352245840442,-6.2930920395618));
#65263=CARTESIAN_POINT('Ctrl Pts',(50.0711979855136,-0.0918257543442044,
-6.36833306094771));
#65264=CARTESIAN_POINT('Ctrl Pts',(50.0376746821943,-1.11695876978463,-6.18314722097487));
#65265=CARTESIAN_POINT('Ctrl Pts',(50.0041513788751,-2.14209178522506,-5.99796138100203));
#65266=CARTESIAN_POINT('Ctrl Pts',(49.9706280755558,-3.12017981592124,-5.55234867967045));
#65267=CARTESIAN_POINT('Ctrl Pts',(49.9371047722365,-3.9326301091344,-4.90033946521847));
#65268=CARTESIAN_POINT('Ctrl Pts',(49.9035814689172,-4.7450804023476,-4.24833025076646));
#65269=CARTESIAN_POINT('Ctrl Pts',(49.870058165598,-5.39189295807774,-3.38992452319404));
#65270=CARTESIAN_POINT('Ctrl Pts',(49.8365348622787,-5.79464203233995,-2.42920360749922));
#65271=CARTESIAN_POINT('Ctrl Pts',(49.8097893852093,-6.11596228016352,-1.66272367632657));
#65272=CARTESIAN_POINT('Ctrl Pts',(49.7830439081399,-6.28193301831962,-0.831118826789475));
#65273=CARTESIAN_POINT('Ctrl Pts',(49.7562984310704,-6.28278348713276,0.000156540911899483));
#65274=CARTESIAN_POINT('Ctrl Pts',(49.5700381542954,-6.28246359837908,0.000149097063601992));
#65275=CARTESIAN_POINT('Ctrl Pts',(49.5933790161204,-6.28181999390192,-0.725413759468975));
#65276=CARTESIAN_POINT('Ctrl Pts',(49.6167198779453,-6.15621775461188,-1.45119369032999));
#65277=CARTESIAN_POINT('Ctrl Pts',(49.6400607397702,-5.90994537476529,-2.13341327280043));
#65278=CARTESIAN_POINT('Ctrl Pts',(49.6735840430895,-5.5562367692015,-3.11325087113057));
#65279=CARTESIAN_POINT('Ctrl Pts',(49.7071073464088,-4.95360824150956,-4.003231621037));
#65280=CARTESIAN_POINT('Ctrl Pts',(49.7406306497281,-4.17512824129216,-4.69544573965404));
#65281=CARTESIAN_POINT('Ctrl Pts',(49.7741539530473,-3.39664824107481,-5.38765985827105));
#65282=CARTESIAN_POINT('Ctrl Pts',(49.8076772563666,-2.44231676833202,-5.88210734559869));
#65283=CARTESIAN_POINT('Ctrl Pts',(49.8412005596858,-1.42784610337591,-6.11883665661577));
#65284=CARTESIAN_POINT('Ctrl Pts',(49.8747238630051,-0.413375438419792,
-6.35556596763286));
#65285=CARTESIAN_POINT('Ctrl Pts',(49.9082471663244,0.661234418749648,-6.3345771023394));
#65286=CARTESIAN_POINT('Ctrl Pts',(49.9417704696436,1.66568748547812,-6.05841495161831));
#65287=CARTESIAN_POINT('Ctrl Pts',(49.9752937729629,2.67014055220664,-5.7822528008972));
#65288=CARTESIAN_POINT('Ctrl Pts',(50.0088170762822,3.60443682849419,-5.25091736474844));
#65289=CARTESIAN_POINT('Ctrl Pts',(50.0423403796014,4.3552932929754,-4.52883283611067));
#65290=CARTESIAN_POINT('Ctrl Pts',(50.0758636829207,5.10614975745656,-3.80674830747294));
#65291=CARTESIAN_POINT('Ctrl Pts',(50.10938698624,5.67356641013141,-2.89391468634623));
#65292=CARTESIAN_POINT('Ctrl Pts',(50.1429102895593,5.98874422608738,-1.90101265639547));
#65293=CARTESIAN_POINT('Ctrl Pts',(50.1764335928785,6.30392204204335,-0.908110626444702));
#65294=CARTESIAN_POINT('Ctrl Pts',(50.2099568961978,6.36686102128044,0.164859812330119));
#65295=CARTESIAN_POINT('Ctrl Pts',(50.243480199517,6.169929839656,1.18780145604941));
#65296=CARTESIAN_POINT('Ctrl Pts',(50.2770035028363,5.97299865803155,2.21074309976876));
#65297=CARTESIAN_POINT('Ctrl Pts',(50.3105268061556,5.51619731554554,3.18365594843258));
#65298=CARTESIAN_POINT('Ctrl Pts',(50.3440501094749,4.85491277836054,3.98857473789601));
#65299=CARTESIAN_POINT('Ctrl Pts',(50.3775734127941,4.19362824117558,4.79349352735939));
#65300=CARTESIAN_POINT('Ctrl Pts',(50.4110967161134,3.32786050929167,5.43041825762241));
#65301=CARTESIAN_POINT('Ctrl Pts',(50.4446200194326,2.36258354756087,5.82212207928221));
#65302=CARTESIAN_POINT('Ctrl Pts',(50.4781433227519,1.39730658583008,6.21382590094201));
#65303=CARTESIAN_POINT('Ctrl Pts',(50.5116666260712,0.332520394252399,6.36030881399858));
#65304=CARTESIAN_POINT('Ctrl Pts',(50.5451899293904,-0.702670159742614,
6.24380982829218));
#65305=CARTESIAN_POINT('Ctrl Pts',(50.5787132327097,-1.73786071373769,6.12731084258576));
#65306=CARTESIAN_POINT('Ctrl Pts',(50.612236536029,-2.74345563015009,5.74782995811634));
#65307=CARTESIAN_POINT('Ctrl Pts',(50.6457598393482,-3.59752695818729,5.15137906879181));
#65308=CARTESIAN_POINT('Ctrl Pts',(50.6792831426675,-4.45159828622444,4.55492817946731));
#65309=CARTESIAN_POINT('Ctrl Pts',(50.7128064459868,-5.15414602588641,3.74150728528773));
#65310=CARTESIAN_POINT('Ctrl Pts',(50.7463297493061,-5.61998656612579,2.80974331956433));
#65311=CARTESIAN_POINT('Ctrl Pts',(50.7775658843025,-6.0540445664117,1.94155008869493));
#65312=CARTESIAN_POINT('Ctrl Pts',(50.8088020192989,-6.28259281421262,0.97061112216302));
#65313=CARTESIAN_POINT('Ctrl Pts',(50.8400381542954,-6.28315629679635,-7.16818851180851E-5));
#65314=CARTESIAN_POINT('Origin',(37.,0.,0.));
#65315=CARTESIAN_POINT('',(52.2962984310704,-6.28217298973102,3.97775880020546E-5));
#65316=CARTESIAN_POINT('',(52.1100381542954,-6.28218861558386,-5.63730895511787E-5));
#65317=CARTESIAN_POINT('',(37.,-6.28269,-7.69407619853508E-16));
#65318=CARTESIAN_POINT('Ctrl Pts',(52.2962984310704,-6.28217298973102,3.97775880020546E-5));
#65319=CARTESIAN_POINT('Ctrl Pts',(52.2809365211356,-6.28227906390278,0.477636057591627));
#65320=CARTESIAN_POINT('Ctrl Pts',(52.2655746112008,-6.22851193741266,0.955208832619816));
#65321=CARTESIAN_POINT('Ctrl Pts',(52.250212701266,-6.12061110101499,1.42022047576571));
#65322=CARTESIAN_POINT('Ctrl Pts',(52.2166893979467,-5.88514607861162,2.43498533419222));
#65323=CARTESIAN_POINT('Ctrl Pts',(52.1831660946274,-5.39188814239352,3.38993218283741));
#65324=CARTESIAN_POINT('Ctrl Pts',(52.1496427913082,-4.70064460482311,4.16927412732642));
#65325=CARTESIAN_POINT('Ctrl Pts',(52.1161194879889,-4.00940106725278,4.94861607181534));
#65326=CARTESIAN_POINT('Ctrl Pts',(52.0825961846696,-3.12017192833018,5.55235311214812));
#65327=CARTESIAN_POINT('Ctrl Pts',(52.0490728813504,-2.14077583841207,5.90728239204119));
#65328=CARTESIAN_POINT('Ctrl Pts',(52.0155495780311,-1.16137974849396,6.26221167193427));
#65329=CARTESIAN_POINT('Ctrl Pts',(51.9820262747118,-0.0918167075805276,
6.36833319138765));
#65330=CARTESIAN_POINT('Ctrl Pts',(51.9485029713926,0.938229225972791,6.21277976184401));
#65331=CARTESIAN_POINT('Ctrl Pts',(51.9149796680733,1.96827515952611,6.05722633230036));
#65332=CARTESIAN_POINT('Ctrl Pts',(51.881456364754,2.95880398571927,5.63999795375958));
#65333=CARTESIAN_POINT('Ctrl Pts',(51.8479330614348,3.78971451071403,5.01168338753872));
#65334=CARTESIAN_POINT('Ctrl Pts',(51.8144097581155,4.62062503570879,4.38336882131786));
#65335=CARTESIAN_POINT('Ctrl Pts',(51.7808864547962,5.29191725950531,3.54396806741685));
#65336=CARTESIAN_POINT('Ctrl Pts',(51.747363151477,5.72219728890199,2.59525810595611));
#65337=CARTESIAN_POINT('Ctrl Pts',(51.7138398481577,6.15247731829869,1.64654814449533));
#65338=CARTESIAN_POINT('Ctrl Pts',(51.6803165448384,6.34174515329552,0.588528975474791));
#65339=CARTESIAN_POINT('Ctrl Pts',(51.6467932415192,6.26705215036274,-0.450515032248377));
#65340=CARTESIAN_POINT('Ctrl Pts',(51.6132699381999,6.19235914742996,-1.48955903997155));
#65341=CARTESIAN_POINT('Ctrl Pts',(51.5797466348806,5.85370530656757,-2.50962788639735));
#65342=CARTESIAN_POINT('Ctrl Pts',(51.5462233315613,5.29215226021866,-3.3870386629489));
#65343=CARTESIAN_POINT('Ctrl Pts',(51.5127000282421,4.73059921386977,-4.2644494395004));
#65344=CARTESIAN_POINT('Ctrl Pts',(51.4791767249228,3.94614696203438,-4.99920214617766));
#65345=CARTESIAN_POINT('Ctrl Pts',(51.4456534216036,3.03391000260804,-5.50220833354418));
#65346=CARTESIAN_POINT('Ctrl Pts',(51.4121301182843,2.12167304318169,-6.00521452091069));
#65347=CARTESIAN_POINT('Ctrl Pts',(51.378606814965,1.08165137616439,-6.27647418896646));
#65348=CARTESIAN_POINT('Ctrl Pts',(51.3450835116457,0.0399471810417346,
-6.28309721971377));
#65349=CARTESIAN_POINT('Ctrl Pts',(51.3115602083265,-1.00175701408092,-6.28972025046108));
#65350=CARTESIAN_POINT('Ctrl Pts',(51.2780369050072,-2.04514373730893,-6.03170664389993));
#65351=CARTESIAN_POINT('Ctrl Pts',(51.244513601688,-2.96370279753951,-5.54034043877311));
#65352=CARTESIAN_POINT('Ctrl Pts',(51.2109902983687,-3.88226185777009,-5.04897423364628));
#65353=CARTESIAN_POINT('Ctrl Pts',(51.1774669950494,-4.67599325500323,-4.32425542995378));
#65354=CARTESIAN_POINT('Ctrl Pts',(51.1439436917301,-5.24865739895781,-3.45405587071395));
#65355=CARTESIAN_POINT('Ctrl Pts',(51.1104203884109,-5.82132154291242,-2.58385631147407));
#65356=CARTESIAN_POINT('Ctrl Pts',(51.0768970850916,-6.17291843358843,-1.56817599668685));
#65357=CARTESIAN_POINT('Ctrl Pts',(51.0433737817723,-6.26081709932372,-0.530165727356866));
#65358=CARTESIAN_POINT('Ctrl Pts',(51.037681998205,-6.27574105166978,-0.353926239935505));
#65359=CARTESIAN_POINT('Ctrl Pts',(51.0319902146377,-6.28306331063293,-0.177043041439763));
#65360=CARTESIAN_POINT('Ctrl Pts',(51.0262984310705,-6.28288820464993,-0.000145391911651194));
#65361=CARTESIAN_POINT('Ctrl Pts',(50.8400381542954,-6.28315629679635,-7.16818851180851E-5));
#65362=CARTESIAN_POINT('Ctrl Pts',(50.8423253226182,-6.28319755604677,-0.0711468952931936));
#65363=CARTESIAN_POINT('Ctrl Pts',(50.844612490941,-6.28201648803129,-0.142220735300779));
#65364=CARTESIAN_POINT('Ctrl Pts',(50.8468996592638,-6.27960426962443,-0.213252765949846));
#65365=CARTESIAN_POINT('Ctrl Pts',(50.8804229625831,-6.2442480920669,-1.25437784847344));
#65366=CARTESIAN_POINT('Ctrl Pts',(50.9139462659024,-5.94440239613498,-2.28652097625335));
#65367=CARTESIAN_POINT('Ctrl Pts',(50.9474695692217,-5.41642334340257,-3.18453523929544));
#65368=CARTESIAN_POINT('Ctrl Pts',(50.9809928725409,-4.88844429067018,-4.08254950233747));
#65369=CARTESIAN_POINT('Ctrl Pts',(51.0145161758602,-4.1323318811373,-4.84643490064171));
#65370=CARTESIAN_POINT('Ctrl Pts',(51.0480394791794,-3.23976441901818,-5.38357065845099));
#65371=CARTESIAN_POINT('Ctrl Pts',(51.0815627824987,-2.34719695689906,-5.92070641626027));
#65372=CARTESIAN_POINT('Ctrl Pts',(51.115086085818,-1.31817444219368,-6.2310925335746));
#65373=CARTESIAN_POINT('Ctrl Pts',(51.1486093891372,-0.277465411904037,
-6.27709482726425));
#65374=CARTESIAN_POINT('Ctrl Pts',(51.1821326924565,0.763243618385662,-6.3230971209539));
#65375=CARTESIAN_POINT('Ctrl Pts',(51.2156559957758,1.81563916425966,-6.10471559101883));
#65376=CARTESIAN_POINT('Ctrl Pts',(51.249179299095,2.75211871874681,-5.64842890396915));
#65377=CARTESIAN_POINT('Ctrl Pts',(51.2827026024143,3.68859827323391,-5.19214221691949));
#65378=CARTESIAN_POINT('Ctrl Pts',(51.3162259057336,4.50916183633422,-4.49795037275522));
#65379=CARTESIAN_POINT('Ctrl Pts',(51.3497492090529,5.11431642920412,-3.65002383379116));
#65380=CARTESIAN_POINT('Ctrl Pts',(51.3832725123721,5.71947102207406,-2.80209729482705));
#65381=CARTESIAN_POINT('Ctrl Pts',(51.4167958156914,6.10921664471359,-1.80043606106309));
#65382=CARTESIAN_POINT('Ctrl Pts',(51.4503191190106,6.23629680812975,-0.76649112596386));
#65383=CARTESIAN_POINT('Ctrl Pts',(51.4838424223299,6.36337697154592,0.26745380913537));
#65384=CARTESIAN_POINT('Ctrl Pts',(51.5173657256492,6.22779167573876,1.33368244556975));
#65385=CARTESIAN_POINT('Ctrl Pts',(51.5508890289685,5.84598057946701,2.30291502009198));
#65386=CARTESIAN_POINT('Ctrl Pts',(51.5844123322877,5.46416948319528,3.27214759461415));
#65387=CARTESIAN_POINT('Ctrl Pts',(51.617935635607,4.83613258645898,4.14438410722406));
#65388=CARTESIAN_POINT('Ctrl Pts',(51.6514589389262,4.03801909267131,4.81386625619082));
#65389=CARTESIAN_POINT('Ctrl Pts',(51.6849822422455,3.23990559888364,5.48334840515759));
#65390=CARTESIAN_POINT('Ctrl Pts',(51.7185055455648,2.27171550804457,5.95007619048123));
#65391=CARTESIAN_POINT('Ctrl Pts',(51.7520288488841,1.25084145194549,6.15745906907757));
#65392=CARTESIAN_POINT('Ctrl Pts',(51.7855521522033,0.229967395846398,6.36484194767391));
#65393=CARTESIAN_POINT('Ctrl Pts',(51.8190754555226,-0.843590625512924,
6.31287991954294));
#65394=CARTESIAN_POINT('Ctrl Pts',(51.8525987588419,-1.83966416411708,6.00787335823035));
#65395=CARTESIAN_POINT('Ctrl Pts',(51.8861220621611,-2.83573770272123,5.70286679691777));
#65396=CARTESIAN_POINT('Ctrl Pts',(51.9196453654804,-3.75432675857026,5.14481570242368));
#65397=CARTESIAN_POINT('Ctrl Pts',(51.9531686687997,-4.48405280401665,4.40138352976211));
#65398=CARTESIAN_POINT('Ctrl Pts',(51.9866919721189,-5.21377884946307,3.65795135710051));
#65399=CARTESIAN_POINT('Ctrl Pts',(52.0202152754382,-5.75464188450669,2.72913810627147));
#65400=CARTESIAN_POINT('Ctrl Pts',(52.0537385787575,-6.04106249894367,1.72756198416353));
#65401=CARTESIAN_POINT('Ctrl Pts',(52.0725051039368,-6.20140229665138,1.16687429370754));
#65402=CARTESIAN_POINT('Ctrl Pts',(52.0912716291161,-6.2820044067331,0.583384025414971));
#65403=CARTESIAN_POINT('Ctrl Pts',(52.1100381542954,-6.28218861558386,-5.63730895511787E-5));
#65404=CARTESIAN_POINT('Origin',(37.,0.,0.));
#65405=CARTESIAN_POINT('',(53.5662984310705,-6.28311963543023,8.84621771294822E-5));
#65406=CARTESIAN_POINT('',(53.3800381542954,-6.28283028954965,0.000152413998317728));
#65407=CARTESIAN_POINT('',(37.,-6.28269,-7.69407619853508E-16));
#65408=CARTESIAN_POINT('Ctrl Pts',(53.5662984310705,-6.28311963543023,8.84621771294822E-5));
#65409=CARTESIAN_POINT('Ctrl Pts',(53.5634061309528,-6.28318170133873,0.0899700538258294));
#65410=CARTESIAN_POINT('Ctrl Pts',(53.5605138308351,-6.28129275480609,0.179849034806085));
#65411=CARTESIAN_POINT('Ctrl Pts',(53.5576215307174,-6.27743568838293,0.269643476396016));
#65412=CARTESIAN_POINT('Ctrl Pts',(53.5240982273981,-6.23273022824222,1.31040901915495));
#65413=CARTESIAN_POINT('Ctrl Pts',(53.4905749240788,-5.92362659308418,2.33981749945716));
#65414=CARTESIAN_POINT('Ctrl Pts',(53.4570516207596,-5.38760345798027,3.23305357860289));
#65415=CARTESIAN_POINT('Ctrl Pts',(53.4235283174403,-4.85158032287627,4.12628965774877));
#65416=CARTESIAN_POINT('Ctrl Pts',(53.3900050141211,-4.08863768782632,4.88335333573811));
#65417=CARTESIAN_POINT('Ctrl Pts',(53.3564817108018,-3.19128202285747,5.41245096927237));
#65418=CARTESIAN_POINT('Ctrl Pts',(53.3229584074825,-2.29392635788873,5.94154860280657));
#65419=CARTESIAN_POINT('Ctrl Pts',(53.2894351041632,-1.26215766300112,6.24268019188573));
#65420=CARTESIAN_POINT('Ctrl Pts',(53.255911800844,-0.221077446364313,6.27933366002215));
#65421=CARTESIAN_POINT('Ctrl Pts',(53.2223884975247,0.820002770272492,6.31598712815857));
#65422=CARTESIAN_POINT('Ctrl Pts',(53.1888651942055,1.87039450865849,6.08816247535226));
#65423=CARTESIAN_POINT('Ctrl Pts',(53.1553418908862,2.80273822159734,5.62348334316875));
#65424=CARTESIAN_POINT('Ctrl Pts',(53.1218185875669,3.73508193453619,5.15880421098525));
#65425=CARTESIAN_POINT('Ctrl Pts',(53.0882952842476,4.54937762202789,4.45727059942454));
#65426=CARTESIAN_POINT('Ctrl Pts',(53.0547719809284,5.14689228297022,3.60394315669717));
#65427=CARTESIAN_POINT('Ctrl Pts',(53.0212486776091,5.74440694391255,2.75061571396979));
#65428=CARTESIAN_POINT('Ctrl Pts',(52.9877253742898,6.12514057830551,1.74549444007574));
#65429=CARTESIAN_POINT('Ctrl Pts',(52.9542020709706,6.24292939658562,0.710449856979257));
#65430=CARTESIAN_POINT('Ctrl Pts',(52.9206787676513,6.36071821486574,-0.324594726117287));
#65431=CARTESIAN_POINT('Ctrl Pts',(52.8871554643321,6.21556221703297,-1.38956261841627));
#65432=CARTESIAN_POINT('Ctrl Pts',(52.8536321610128,5.82506150548354,-2.35532692141684));
#65433=CARTESIAN_POINT('Ctrl Pts',(52.8201088576935,5.43456079393411,-3.3210912244174));
#65434=CARTESIAN_POINT('Ctrl Pts',(52.7865855543742,4.79871536866802,-4.18765193811955));
#65435=CARTESIAN_POINT('Ctrl Pts',(52.753062251055,3.99462121375218,-4.84993894893488));
#65436=CARTESIAN_POINT('Ctrl Pts',(52.7195389477357,3.19052705883639,-5.51222595975018));
#65437=CARTESIAN_POINT('Ctrl Pts',(52.6860156444164,2.21818417427087,-5.97023926767867));
#65438=CARTESIAN_POINT('Ctrl Pts',(52.6524923410972,1.19548871633445,-6.16844495628597));
#65439=CARTESIAN_POINT('Ctrl Pts',(52.6189690377779,0.172793258398022,-6.36665064489327));
#65440=CARTESIAN_POINT('Ctrl Pts',(52.5854457344586,-0.90025477290931,-6.30504871417938));
#65441=CARTESIAN_POINT('Ctrl Pts',(52.5519224311394,-1.89354876566498,-5.9911083717206));
#65442=CARTESIAN_POINT('Ctrl Pts',(52.5183991278201,-2.8868427584207,-5.6771680292618));
#65443=CARTESIAN_POINT('Ctrl Pts',(52.4848758245008,-3.80038271262475,-5.11088927505809));
#65444=CARTESIAN_POINT('Ctrl Pts',(52.4513525211815,-4.52340230202128,-4.36093316432646));
#65445=CARTESIAN_POINT('Ctrl Pts',(52.4178292178623,-5.24642189141773,-3.61097705359491));
#65446=CARTESIAN_POINT('Ctrl Pts',(52.384305914543,-5.77892111600671,-2.6773435863355));
#65447=CARTESIAN_POINT('Ctrl Pts',(52.3507826112238,-6.05633467400686,-1.67323541860197));
#65448=CARTESIAN_POINT('Ctrl Pts',(52.3326212178393,-6.20662465912666,-1.12925551122031));
#65449=CARTESIAN_POINT('Ctrl Pts',(52.3144598244549,-6.28204758509257,-0.564591440593399));
#65450=CARTESIAN_POINT('Ctrl Pts',(52.2962984310704,-6.28217298973102,3.97775880020546E-5));
#65451=CARTESIAN_POINT('Ctrl Pts',(52.1100381542954,-6.28218861558386,-5.63730895511787E-5));
#65452=CARTESIAN_POINT('Ctrl Pts',(52.1247949324354,-6.28233346547568,-0.45883605853235));
#65453=CARTESIAN_POINT('Ctrl Pts',(52.1395517105753,-6.23275408168553,-0.917584908340834));
#65454=CARTESIAN_POINT('Ctrl Pts',(52.1543084887153,-6.13311973819662,-1.36519185545982));
#65455=CARTESIAN_POINT('Ctrl Pts',(52.1878317920346,-5.90677816918225,-2.38203057958831));
#65456=CARTESIAN_POINT('Ctrl Pts',(52.2213550953538,-5.42211683732318,-3.34136903445849));
#65457=CARTESIAN_POINT('Ctrl Pts',(52.2548783986731,-4.73790072050221,-4.12688784533034));
#65458=CARTESIAN_POINT('Ctrl Pts',(52.2884017019923,-4.05368460368123,-4.91240665620218));
#65459=CARTESIAN_POINT('Ctrl Pts',(52.3219250053116,-3.16991370189837,-5.52410582307568));
#65460=CARTESIAN_POINT('Ctrl Pts',(52.3554483086309,-2.19374485660695,-5.88781708525163));
#65461=CARTESIAN_POINT('Ctrl Pts',(52.3889716119501,-1.21757601131547,-6.25152834742761));
#65462=CARTESIAN_POINT('Ctrl Pts',(52.4224949152694,-0.149009222515451,
-6.36725170490601));
#65463=CARTESIAN_POINT('Ctrl Pts',(52.4560182185886,0.882392246577315,-6.22095575040135));
#65464=CARTESIAN_POINT('Ctrl Pts',(52.4895415219079,1.91379371566996,-6.07465979589671));
#65465=CARTESIAN_POINT('Ctrl Pts',(52.5230648252272,2.90802986505533,-5.66634452940909));
#65466=CARTESIAN_POINT('Ctrl Pts',(52.5565881285465,3.74454998955454,-5.04551800125575));
#65467=CARTESIAN_POINT('Ctrl Pts',(52.5901114318657,4.58107011405381,-4.42469147310237));
#65468=CARTESIAN_POINT('Ctrl Pts',(52.623634735185,5.25987421366686,-3.59135368328327));
#65469=CARTESIAN_POINT('Ctrl Pts',(52.6571580385042,5.69865758348159,-2.64654648013265));
#65470=CARTESIAN_POINT('Ctrl Pts',(52.6906813418235,6.13744095329634,-1.70173927698197));
#65471=CARTESIAN_POINT('Ctrl Pts',(52.7242046451428,6.33620359331273,-0.645462660499612));
#65472=CARTESIAN_POINT('Ctrl Pts',(52.7577279484621,6.27084561898115,0.394210284200658));
#65473=CARTESIAN_POINT('Ctrl Pts',(52.7912512517814,6.20548764464956,1.43388322890093));
#65474=CARTESIAN_POINT('Ctrl Pts',(52.8247745551006,5.87600905597011,2.45695250181907));
#65475=CARTESIAN_POINT('Ctrl Pts',(52.8582978584199,5.32235899000359,3.3393713939609));
#65476=CARTESIAN_POINT('Ctrl Pts',(52.8918211617391,4.76870892403713,4.22179028610262));
#65477=CARTESIAN_POINT('Ctrl Pts',(52.9253444650584,3.99088738078357,4.96355879746799));
#65478=CARTESIAN_POINT('Ctrl Pts',(52.9588677683777,3.08320488758523,5.47473781531546));
#65479=CARTESIAN_POINT('Ctrl Pts',(52.9923910716969,2.17552239438675,5.98591683316301));
#65480=CARTESIAN_POINT('Ctrl Pts',(53.0259143750162,1.13797895124335,6.26650635749272));
#65481=CARTESIAN_POINT('Ctrl Pts',(53.0594376783355,0.0963762540466073,
6.28248502926124));
#65482=CARTESIAN_POINT('Ctrl Pts',(53.0929609816548,-0.94522644315002,6.29846370102975));
#65483=CARTESIAN_POINT('Ctrl Pts',(53.126484284974,-1.99088839439997,6.04983152023715));
#65484=CARTESIAN_POINT('Ctrl Pts',(53.1600075882933,-2.91382353815079,5.56673503176638));
#65485=CARTESIAN_POINT('Ctrl Pts',(53.1935308916126,-3.83675868190156,5.08363854329565));
#65486=CARTESIAN_POINT('Ctrl Pts',(53.2270541949318,-4.6369670181532,4.36607774714679));
#65487=CARTESIAN_POINT('Ctrl Pts',(53.2605774982511,-5.21742363061766,3.50105658104994));
#65488=CARTESIAN_POINT('Ctrl Pts',(53.2941008015703,-5.79788024308219,2.63603541495299));
#65489=CARTESIAN_POINT('Ctrl Pts',(53.3276241048896,-6.15858513175947,1.62355387890804));
#65490=CARTESIAN_POINT('Ctrl Pts',(53.3611474082089,-6.25580298403,0.586374923284767));
#65491=CARTESIAN_POINT('Ctrl Pts',(53.3674443235711,-6.27406408979303,0.391554381980045));
#65492=CARTESIAN_POINT('Ctrl Pts',(53.3737412389332,-6.28302865535999,0.195862448454363));
#65493=CARTESIAN_POINT('Ctrl Pts',(53.3800381542954,-6.28283028954965,0.000152413998317728));
#65494=CARTESIAN_POINT('Origin',(37.,0.,0.));
#65495=CARTESIAN_POINT('',(54.8362984310704,-6.28252994889952,-0.000148679754663761));
#65496=CARTESIAN_POINT('',(54.6500381542954,-6.28284206479216,-0.000151303447314885));
#65497=CARTESIAN_POINT('',(37.,-6.28269,-7.69407619853508E-16));
#65498=CARTESIAN_POINT('Ctrl Pts',(54.8362984310704,-6.28252994889952,-0.000148679754663761));
#65499=CARTESIAN_POINT('Ctrl Pts',(54.8123524374506,-6.28183164615208,0.744205706882085));
#65500=CARTESIAN_POINT('Ctrl Pts',(54.7884064438308,-6.1494773107617,1.48879635703162));
#65501=CARTESIAN_POINT('Ctrl Pts',(54.764460450211,-5.8905402896867,2.18640382765216));
#65502=CARTESIAN_POINT('Ctrl Pts',(54.7309371468918,-5.52804022241435,3.16302259765179));
#65503=CARTESIAN_POINT('Ctrl Pts',(54.6974138435725,-4.91745419101602,4.04756031147763));
#65504=CARTESIAN_POINT('Ctrl Pts',(54.6638905402532,-4.13279136549942,4.73275600063913));
#65505=CARTESIAN_POINT('Ctrl Pts',(54.6303672369339,-3.34812853998279,5.41795168980066));
#65506=CARTESIAN_POINT('Ctrl Pts',(54.5968439336147,-2.38938892034787,5.90380535429783));
#65507=CARTESIAN_POINT('Ctrl Pts',(54.5633206302954,-1.37283159840298,6.13141314347905));
#65508=CARTESIAN_POINT('Ctrl Pts',(54.5297973269761,-0.356274276458217,
6.35902093266023));
#65509=CARTESIAN_POINT('Ctrl Pts',(54.4962740236568,0.718100747796503,6.32838284652552));
#65510=CARTESIAN_POINT('Ctrl Pts',(54.4627507203376,1.72003226351471,6.04321082867509));
#65511=CARTESIAN_POINT('Ctrl Pts',(54.4292274170183,2.72196377923304,5.75803881082463));
#65512=CARTESIAN_POINT('Ctrl Pts',(54.3957041136991,3.65145178641483,5.21833286125838));
#65513=CARTESIAN_POINT('Ctrl Pts',(54.3621808103798,4.39579304566329,4.48953358170574));
#65514=CARTESIAN_POINT('Ctrl Pts',(54.3286575070606,5.14013430491179,3.76073430215307));
#65515=CARTESIAN_POINT('Ctrl Pts',(54.2951342037413,5.69932881622692,2.842841692614));
#65516=CARTESIAN_POINT('Ctrl Pts',(54.261610900422,6.00557613055491,1.84714907670987));
#65517=CARTESIAN_POINT('Ctrl Pts',(54.2280875971027,6.31182344488285,0.851456460805907));
#65518=CARTESIAN_POINT('Ctrl Pts',(54.1945642937835,6.36512356222373,-0.222036161463082));
#65519=CARTESIAN_POINT('Ctrl Pts',(54.1610409904642,6.15901302578961,-1.2431678832118));
#65520=CARTESIAN_POINT('Ctrl Pts',(54.1275176871449,5.95290248935549,-2.26429960496059));
#65521=CARTESIAN_POINT('Ctrl Pts',(54.0939943838257,5.48738129914634,-3.23307042618909));
#65522=CARTESIAN_POINT('Ctrl Pts',(54.0604710805064,4.8188941286198,-4.0320175003176));
#65523=CARTESIAN_POINT('Ctrl Pts',(54.0269477771871,4.15040695809322,-4.83096457444614));
#65524=CARTESIAN_POINT('Ctrl Pts',(53.9934244738678,3.27895380724923,-5.46008790147467));
#65525=CARTESIAN_POINT('Ctrl Pts',(53.9599011705486,2.31019777605328,-5.84310644733658));
#65526=CARTESIAN_POINT('Ctrl Pts',(53.9263778672293,1.34144174485745,-6.22612499319844));
#65527=CARTESIAN_POINT('Ctrl Pts',(53.8928545639101,0.27538283330969,-6.36303875789375));
#65528=CARTESIAN_POINT('Ctrl Pts',(53.8593312605908,-0.758719662249247,
-6.23724705822467));
#65529=CARTESIAN_POINT('Ctrl Pts',(53.8258079572716,-1.7928221578083,-6.11145535855559));
#65530=CARTESIAN_POINT('Ctrl Pts',(53.7922846539523,-2.79496823737853,-5.72295819452207));
#65531=CARTESIAN_POINT('Ctrl Pts',(53.758761350633,-3.64364817746724,-5.11886065355629));
#65532=CARTESIAN_POINT('Ctrl Pts',(53.7252380473137,-4.49232811755596,-4.51476311259051));
#65533=CARTESIAN_POINT('Ctrl Pts',(53.6917147439944,-5.18754191816317,-3.69506519469248));
#65534=CARTESIAN_POINT('Ctrl Pts',(53.6581914406752,-5.64499517590509,-2.75915493313556));
#65535=CARTESIAN_POINT('Ctrl Pts',(53.6275604374736,-6.06298060141694,-1.90399248255254));
#65536=CARTESIAN_POINT('Ctrl Pts',(53.5969294342721,-6.28246232430602,-0.951805604666501));
#65537=CARTESIAN_POINT('Ctrl Pts',(53.5662984310705,-6.28311963543023,8.84621771294822E-5));
#65538=CARTESIAN_POINT('Ctrl Pts',(53.3800381542954,-6.28283028954965,0.000152413998317728));
#65539=CARTESIAN_POINT('Ctrl Pts',(53.4072645422525,-6.28197260222196,-0.846051960481647));
#65540=CARTESIAN_POINT('Ctrl Pts',(53.4344909302096,-6.1098143561761,-1.69259473097886));
#65541=CARTESIAN_POINT('Ctrl Pts',(53.4617173181667,-5.77715549886801,-2.47050214869888));
#65542=CARTESIAN_POINT('Ctrl Pts',(53.4952406214859,-5.36755934557172,-3.42832388985779));
#65543=CARTESIAN_POINT('Ctrl Pts',(53.5287639248052,-4.71463622311535,-4.28209099697412));
#65544=CARTESIAN_POINT('Ctrl Pts',(53.5622872281245,-3.89755277860976,-4.9282845761252));
#65545=CARTESIAN_POINT('Ctrl Pts',(53.5958105314438,-3.08046933410412,-5.57447815527632));
#65546=CARTESIAN_POINT('Ctrl Pts',(53.629333834763,-2.09922556754923,-6.01309820646219));
#65547=CARTESIAN_POINT('Ctrl Pts',(53.6628571380823,-1.07279686419783,-6.19096223659628));
#65548=CARTESIAN_POINT('Ctrl Pts',(53.6963804414015,-0.0463681608464844,
-6.36882626673037));
#65549=CARTESIAN_POINT('Ctrl Pts',(53.7299037447208,1.0252454793014,-6.2859342758127));
#65550=CARTESIAN_POINT('Ctrl Pts',(53.7634270480401,2.01211136537584,-5.9523368833727));
#65551=CARTESIAN_POINT('Ctrl Pts',(53.7969503513594,2.99897725145034,-5.61873949093267));
#65552=CARTESIAN_POINT('Ctrl Pts',(53.8304736546786,3.90109538345142,-5.03443669697027));
#65553=CARTESIAN_POINT('Ctrl Pts',(53.8639969579979,4.60908432271368,-4.27027496120012));
#65554=CARTESIAN_POINT('Ctrl Pts',(53.8975202613172,5.31707326197589,-3.50611322543002));
#65555=CARTESIAN_POINT('Ctrl Pts',(53.9310435646364,5.83093300849932,-2.56209254785216));
#65556=CARTESIAN_POINT('Ctrl Pts',(53.9645668679557,6.08835829593271,-1.55267503431523));
#65557=CARTESIAN_POINT('Ctrl Pts',(53.998090171275,6.3457835833661,-0.543257520778245));
#65558=CARTESIAN_POINT('Ctrl Pts',(54.0316134745942,6.34677441170943,0.531556828717691));
#65559=CARTESIAN_POINT('Ctrl Pts',(54.0651367779135,6.0912106302571,1.54144724672204));
#65560=CARTESIAN_POINT('Ctrl Pts',(54.0986600812328,5.8356468488048,2.55133766472626));
#65561=CARTESIAN_POINT('Ctrl Pts',(54.1321833845521,5.32352845755678,3.49630415123893));
#65562=CARTESIAN_POINT('Ctrl Pts',(54.1657066878713,4.61694961685463,4.26176990729727));
#65563=CARTESIAN_POINT('Ctrl Pts',(54.1992299911906,3.9103707761524,5.0272356633557));
#65564=CARTESIAN_POINT('Ctrl Pts',(54.2327532945098,3.00933148599608,5.61320068895984));
#65565=CARTESIAN_POINT('Ctrl Pts',(54.2662765978291,2.02308232195134,5.94861701454061));
#65566=CARTESIAN_POINT('Ctrl Pts',(54.2997999011483,1.0368331579066,6.28403334012138));
#65567=CARTESIAN_POINT('Ctrl Pts',(54.3333232044676,-0.0346258800264526,
6.36890096567867));
#65568=CARTESIAN_POINT('Ctrl Pts',(54.3668465077869,-1.06138074574406,6.19292965459644));
#65569=CARTESIAN_POINT('Ctrl Pts',(54.4003698111062,-2.0881356114616,6.01695834351422));
#65570=CARTESIAN_POINT('Ctrl Pts',(54.4338931144254,-3.07018630496374,5.5801480957925));
#65571=CARTESIAN_POINT('Ctrl Pts',(54.4674164177447,-3.88845979596622,4.93546210989902));
#65572=CARTESIAN_POINT('Ctrl Pts',(54.500939721064,-4.70673328696874,4.2907761240055));
#65573=CARTESIAN_POINT('Ctrl Pts',(54.5344630243832,-5.36122957547162,3.43821439994017));
#65574=CARTESIAN_POINT('Ctrl Pts',(54.5679863277025,-5.77259088926278,2.48114939807468));
#65575=CARTESIAN_POINT('Ctrl Pts',(54.5953369365668,-6.10820764779796,1.70031016291839));
#65576=CARTESIAN_POINT('Ctrl Pts',(54.6226875454311,-6.28198367935227,0.84990921015598));
#65577=CARTESIAN_POINT('Ctrl Pts',(54.6500381542954,-6.28284206479216,-0.000151303447314885));
#65578=CARTESIAN_POINT('Origin',(16.5082437683087,0.,0.));
#65579=CARTESIAN_POINT('',(55.2432437683087,-5.57769790490533,-0.000131999491044005));
#65580=CARTESIAN_POINT('',(55.26731,-5.57784,5.11151866531329E-13));
#65581=CARTESIAN_POINT('',(16.5082437683087,-5.57784,5.11151866531329E-13));
#65582=CARTESIAN_POINT('',(55.26731,-5.53834961081692,-0.66255766085986));
#65583=CARTESIAN_POINT('Ctrl Pts',(55.2432437683087,-5.57769790490533,-0.000131999491043942));
#65584=CARTESIAN_POINT('Ctrl Pts',(55.2512658455391,-5.57790559613044,-0.221520036468065));
#65585=CARTESIAN_POINT('Ctrl Pts',(55.2592879227696,-5.56499524171959,-0.442884532438414));
#65586=CARTESIAN_POINT('Ctrl Pts',(55.26731,-5.53879749490423,-0.662649316846852));
#65587=CARTESIAN_POINT('Origin',(55.26731,0.,0.));
#65588=CARTESIAN_POINT('Origin',(16.5082437683087,0.,0.));
#65589=CARTESIAN_POINT('',(53.9732437683087,-5.57822143497263,7.85376758110207E-5));
#65590=CARTESIAN_POINT('',(54.2430928170571,-5.57797500476393,-0.000134328833226449));
#65591=CARTESIAN_POINT('',(16.5082437683087,-5.57784,5.11151866531329E-13));
#65592=CARTESIAN_POINT('Ctrl Pts',(53.9732437683087,-5.57822143497263,7.85376758111623E-5));
#65593=CARTESIAN_POINT('Ctrl Pts',(54.0038747715103,-5.57763786706127,-0.845023290013137));
#65594=CARTESIAN_POINT('Ctrl Pts',(54.0680290780311,-5.16952209782556,-2.61556926080919));
#65595=CARTESIAN_POINT('Ctrl Pts',(54.1657066878714,-3.37111907823718,-4.73599208528508));
#65596=CARTESIAN_POINT('Ctrl Pts',(54.2662765978291,-0.701970757150338,
-5.77072801277767));
#65597=CARTESIAN_POINT('Ctrl Pts',(54.3668465077869,2.13740507033186,-5.40606745817384));
#65598=CARTESIAN_POINT('Ctrl Pts',(54.4674164177447,4.45846161278591,-3.73044001590026));
#65599=CARTESIAN_POINT('Ctrl Pts',(54.5679863277025,5.69834582588392,-1.15018443868033));
#65600=CARTESIAN_POINT('Ctrl Pts',(54.6685562376603,5.55638456732653,1.70899057466459));
#65601=CARTESIAN_POINT('Ctrl Pts',(54.7691261476182,4.06700779734722,4.15373547526812));
#65602=CARTESIAN_POINT('Ctrl Pts',(54.8696960575759,1.59137933916517,5.59120577878235));
#65603=CARTESIAN_POINT('Ctrl Pts',(54.9702659675337,-1.27014589220361,5.67280824955481));
#65604=CARTESIAN_POINT('Ctrl Pts',(55.0708358774915,-3.82368404225601,4.37876986600632));
#65605=CARTESIAN_POINT('Ctrl Pts',(55.1618284777499,-5.29506982353384,2.24721731124727));
#65606=CARTESIAN_POINT('Ctrl Pts',(55.2192977746889,-5.57707794418837,0.660713859839581));
#65607=CARTESIAN_POINT('Ctrl Pts',(55.2432437683087,-5.57769790490533,-0.000131999491043942));
#65608=CARTESIAN_POINT('',(55.26731,-1.93782473268743,5.23040479991605));
#65609=CARTESIAN_POINT('Origin',(55.26731,0.,0.));
#65610=CARTESIAN_POINT('Ctrl Pts',(54.2430928170571,-5.57797500476393,-0.000134328833225669));
#65611=CARTESIAN_POINT('Ctrl Pts',(54.249265511512,-5.57814699767408,-0.170459190757225));
#65612=CARTESIAN_POINT('Ctrl Pts',(54.2889615092863,-5.52896704997114,-1.26570281170263));
#65613=CARTESIAN_POINT('Ctrl Pts',(54.3621808103798,-4.83314809906796,-3.23028641703264));
#65614=CARTESIAN_POINT('Ctrl Pts',(54.4627507203376,-2.70537098973005,-5.14538998627536));
#65615=CARTESIAN_POINT('Ctrl Pts',(54.5633206302954,0.078446240209487,-5.81273346716538));
#65616=CARTESIAN_POINT('Ctrl Pts',(54.6638905402532,2.84325992667244,-5.0705086592284));
#65617=CARTESIAN_POINT('Ctrl Pts',(54.764460450211,4.91854716216131,-3.09866134240672));
#65618=CARTESIAN_POINT('Ctrl Pts',(54.8650303601689,5.8011660495001,-0.375447161461482));
#65619=CARTESIAN_POINT('Ctrl Pts',(54.9656002701266,5.27686000591952,2.43892212337069));
#65620=CARTESIAN_POINT('Ctrl Pts',(55.0661701800844,3.47320975124282,4.66163850225691));
#65621=CARTESIAN_POINT('Ctrl Pts',(55.1667400900422,0.826722671906332,5.75435770195244));
#65622=CARTESIAN_POINT('Ctrl Pts',(55.2337866966808,-1.07034715964058,5.55179856586871));
#65623=CARTESIAN_POINT('Ctrl Pts',(55.26731,-1.93782473268743,5.23040479991605));
#65624=CARTESIAN_POINT('Origin',(16.5082437683087,0.,0.));
#65625=CARTESIAN_POINT('',(52.7032437683088,-5.57738099270237,3.53149720619964E-5));
#65626=CARTESIAN_POINT('',(52.9730928170571,-5.57796455057653,0.000135314793302463));
#65627=CARTESIAN_POINT('',(16.5082437683087,-5.57784,5.11151866531329E-13));
#65628=CARTESIAN_POINT('Ctrl Pts',(52.7032437683088,-5.57738099270237,3.53149720621823E-5));
#65629=CARTESIAN_POINT('Ctrl Pts',(52.7214051616932,-5.57726965711069,-0.501250375396387));
#65630=CARTESIAN_POINT('Ctrl Pts',(52.7730898583969,-5.38670752464807,-1.92791989326071));
#65631=CARTESIAN_POINT('Ctrl Pts',(52.8582978584198,-4.18507142767569,-4.03475427685318));
#65632=CARTESIAN_POINT('Ctrl Pts',(52.9588677683777,-1.75191953024455,-5.54299944875284));
#65633=CARTESIAN_POINT('Ctrl Pts',(53.0594376783355,1.10607134513556,-5.70707202588776));
#65634=CARTESIAN_POINT('Ctrl Pts',(53.1600075882933,3.69584087152237,-4.48718454958579));
#65635=CARTESIAN_POINT('Ctrl Pts',(53.2605774982511,5.38937216792545,-2.1791586826484));
#65636=CARTESIAN_POINT('Ctrl Pts',(53.3611474082089,5.77598535317805,0.657311288835543));
#65637=CARTESIAN_POINT('Ctrl Pts',(53.4617173181667,4.76192706193859,3.33438383883116));
#65638=CARTESIAN_POINT('Ctrl Pts',(53.5622872281245,2.59310555832215,5.2028711778091));
#65639=CARTESIAN_POINT('Ctrl Pts',(53.6628571380823,-0.204541812806597,
5.80966673579904));
#65640=CARTESIAN_POINT('Ctrl Pts',(53.7634270480401,-2.95258796680689,5.00762310982228));
#65641=CARTESIAN_POINT('Ctrl Pts',(53.8639969579978,-4.98463408757047,2.99123519367383));
#65642=CARTESIAN_POINT('Ctrl Pts',(53.9339358647541,-5.55716187048982,1.08454472513754));
#65643=CARTESIAN_POINT('Ctrl Pts',(53.9703514681911,-5.57827653775616,0.0798763849612549));
#65644=CARTESIAN_POINT('Ctrl Pts',(53.9732437683087,-5.57822143497263,7.85376758111623E-5));
#65645=CARTESIAN_POINT('Ctrl Pts',(52.9730928170571,-5.57796455057653,0.000135314793302289));
#65646=CARTESIAN_POINT('Ctrl Pts',(53.0003192050142,-5.57720308650882,-0.751134063156271));
#65647=CARTESIAN_POINT('Ctrl Pts',(53.0610688962905,-5.23616546002432,-2.42809664728444));
#65648=CARTESIAN_POINT('Ctrl Pts',(53.1553418908863,-3.60603273460568,-4.55967026342535));
#65649=CARTESIAN_POINT('Ctrl Pts',(53.2559118008439,-0.99255631088897,-5.72790511170206));
#65650=CARTESIAN_POINT('Ctrl Pts',(53.3564817108019,1.86161416062682,-5.50712789877888));
#65651=CARTESIAN_POINT('Ctrl Pts',(53.4570516207595,4.26434480692677,-3.95087691570875));
#65652=CARTESIAN_POINT('Ctrl Pts',(53.5576215307175,5.63297549627246,-1.43654167257841));
#65653=CARTESIAN_POINT('Ctrl Pts',(53.6581914406752,5.63561450056838,1.42615367186469));
#65654=CARTESIAN_POINT('Ctrl Pts',(53.758761350633,4.2716217932542,3.94300801314016));
#65655=CARTESIAN_POINT('Ctrl Pts',(53.8593312605908,1.87176456925964,5.50368623779372));
#65656=CARTESIAN_POINT('Ctrl Pts',(53.9599011705486,-0.981994129710483,
5.72972541999358));
#65657=CARTESIAN_POINT('Ctrl Pts',(54.0604710805064,-3.59761974878958,4.56631086087063));
#65658=CARTESIAN_POINT('Ctrl Pts',(54.1548682960093,-5.23383330465535,2.43494193696294));
#65659=CARTESIAN_POINT('Ctrl Pts',(54.2157422081928,-5.57721292090455,0.754558571054565));
#65660=CARTESIAN_POINT('Ctrl Pts',(54.2430928170571,-5.57797500476393,-0.000134328833225669));
#65661=CARTESIAN_POINT('Origin',(16.5082437683087,0.,0.));
#65662=CARTESIAN_POINT('',(51.4332437683088,-5.57801596822771,-0.00012908050836989));
#65663=CARTESIAN_POINT('',(51.7030928170571,-5.57739486550319,-5.00486370436093E-5));
#65664=CARTESIAN_POINT('',(16.5082437683087,-5.57784,5.11151866531329E-13));
#65665=CARTESIAN_POINT('Ctrl Pts',(51.4332437683088,-5.57801596822771,-0.000129080508369864));
#65666=CARTESIAN_POINT('Ctrl Pts',(51.4389355518761,-5.57817142920959,-0.157180723267159));
#65667=CARTESIAN_POINT('Ctrl Pts',(51.4781506387626,-5.53338253817611,-1.23914222489699));
#65668=CARTESIAN_POINT('Ctrl Pts',(51.5508890289684,-4.85608058876542,-3.19570747170793));
#65669=CARTESIAN_POINT('Ctrl Pts',(51.6514589389262,-2.74203068176238,-5.12594700222191));
#65670=CARTESIAN_POINT('Ctrl Pts',(51.7520288488841,0.036959305149328,-5.81314879725927));
#65671=CARTESIAN_POINT('Ctrl Pts',(51.8525987588419,2.80698669237795,-5.09066701308651));
#65672=CARTESIAN_POINT('Ctrl Pts',(51.9531686687997,4.89632222303964,-3.13370286043244));
#65673=CARTESIAN_POINT('Ctrl Pts',(52.0537385787575,5.79830382950879,-0.41681846170471));
#65674=CARTESIAN_POINT('Ctrl Pts',(52.1543084887152,5.29420174866827,2.4011440551771));
#65675=CARTESIAN_POINT('Ctrl Pts',(52.2548783986731,3.50626030117625,4.63683120565213));
#65676=CARTESIAN_POINT('Ctrl Pts',(52.3554483086308,0.868053748938764,5.74809078027364));
#65677=CARTESIAN_POINT('Ctrl Pts',(52.4560182185887,-1.98065509017138,5.46544328880053));
#65678=CARTESIAN_POINT('Ctrl Pts',(52.5565881285464,-4.34905677491859,3.85743050460308));
#65679=CARTESIAN_POINT('Ctrl Pts',(52.6389966451198,-5.4255710484936,1.77329999683277));
#65680=CARTESIAN_POINT('Ctrl Pts',(52.6878818583739,-5.57747516649707,0.424050447734582));
#65681=CARTESIAN_POINT('Ctrl Pts',(52.7032437683088,-5.57738099270237,3.53149720621823E-5));
#65682=CARTESIAN_POINT('Ctrl Pts',(51.7030928170571,-5.57739486550319,-5.00486370434358E-5));
#65683=CARTESIAN_POINT('Ctrl Pts',(51.717849595197,-5.57752346480075,-0.407359605634272));
#65684=CARTESIAN_POINT('Ctrl Pts',(51.7661296766563,-5.43351169352543,-1.73987383596617));
#65685=CARTESIAN_POINT('Ctrl Pts',(51.8479330614348,-4.38352629472378,-3.81821453267259));
#65686=CARTESIAN_POINT('Ctrl Pts',(51.9485029713925,-2.02966225553008,-5.44743390253828));
#65687=CARTESIAN_POINT('Ctrl Pts',(52.0490728813504,0.816393133438721,-5.75565524034613));
#65688=CARTESIAN_POINT('Ctrl Pts',(52.1496427913082,3.46447389032224,-4.66813513700239));
#65689=CARTESIAN_POINT('Ctrl Pts',(52.250212701266,5.27242271112307,-2.44859628140164));
#65690=CARTESIAN_POINT('Ctrl Pts',(52.3507826112238,5.80181356312538,0.364725064619975));
#65691=CARTESIAN_POINT('Ctrl Pts',(52.4513525211815,4.9242696204448,3.08960089643144));
#65692=CARTESIAN_POINT('Ctrl Pts',(52.5519224311394,2.85259453374416,5.06525117048629));
#65693=CARTESIAN_POINT('Ctrl Pts',(52.6524923410972,0.0891677282345522,
5.81258239599026));
#65694=CARTESIAN_POINT('Ctrl Pts',(52.753062251055,-2.6958821746702,5.15036739414614));
#65695=CARTESIAN_POINT('Ctrl Pts',(52.8536321610128,-4.82718297079972,3.23919273272347));
#65696=CARTESIAN_POINT('Ctrl Pts',(52.9269756830135,-5.52781083299589,1.27256351205078));
#65697=CARTESIAN_POINT('Ctrl Pts',(52.9667959016949,-5.57814066188418,0.173888795959752));
#65698=CARTESIAN_POINT('Ctrl Pts',(52.9730928170571,-5.57796455057653,0.000135314793302289));
#65699=CARTESIAN_POINT('Origin',(16.5082437683087,0.,0.));
#65700=CARTESIAN_POINT('',(50.1632437683087,-5.5779229988856,0.000138978711251798));
#65701=CARTESIAN_POINT('',(50.4330928170571,-5.5782539833292,-6.36399508394114E-5));
#65702=CARTESIAN_POINT('',(16.5082437683087,-5.57784,5.11151866531329E-13));
#65703=CARTESIAN_POINT('Ctrl Pts',(50.1632437683087,-5.5779229988856,0.000138978711251916));
#65704=CARTESIAN_POINT('Ctrl Pts',(50.1899892453782,-5.57716794349296,-0.737876265870143));
#65705=CARTESIAN_POINT('Ctrl Pts',(50.2502580257669,-5.24512519452518,-2.40159339675091));
#65706=CARTESIAN_POINT('Ctrl Pts',(50.3440501094749,-3.63848643265499,-4.53381532582656));
#65707=CARTESIAN_POINT('Ctrl Pts',(50.4446200194326,-1.0334150980172,-5.72067462494628));
#65708=CARTESIAN_POINT('Ctrl Pts',(50.5451899293905,1.82225850829634,-5.52027525203731));
#65709=CARTESIAN_POINT('Ctrl Pts',(50.6457598393482,4.23603599500043,-3.98121388252061));
#65710=CARTESIAN_POINT('Ctrl Pts',(50.7463297493061,5.62257839941823,-1.47671157363573));
#65711=CARTESIAN_POINT('Ctrl Pts',(50.8468996592638,5.64565038205386,1.38589202066021));
#65712=CARTESIAN_POINT('Ctrl Pts',(50.9474695692217,4.29965700697908,3.91241799296163));
#65713=CARTESIAN_POINT('Ctrl Pts',(51.0480394791794,1.91100050897997,5.4901859698914));
#65714=CARTESIAN_POINT('Ctrl Pts',(51.1486093891373,-0.941071967402673,
5.73658857523205));
#65715=CARTESIAN_POINT('Ctrl Pts',(51.249179299095,-3.56493530179192,4.59187338929895));
#65716=CARTESIAN_POINT('Ctrl Pts',(51.3440574254855,-5.22473285590304,2.46143864477682));
#65717=CARTESIAN_POINT('Ctrl Pts',(51.4054122485568,-5.57725579958518,0.76781752987093));
#65718=CARTESIAN_POINT('Ctrl Pts',(51.4332437683088,-5.57801596822771,-0.000129080508369864));
#65719=CARTESIAN_POINT('Ctrl Pts',(50.4330928170571,-5.5782539833292,-6.36399508389517E-5));
#65720=CARTESIAN_POINT('Ctrl Pts',(50.4353799853799,-5.5782906137371,-0.0631649816304534));
#65721=CARTESIAN_POINT('Ctrl Pts',(50.471190457022,-5.5618731054905,-1.05113124534463));
#65722=CARTESIAN_POINT('Ctrl Pts',(50.5405242319834,-5.01129836816094,-2.94634581461765));
#65723=CARTESIAN_POINT('Ctrl Pts',(50.6410941419411,-2.99744409122436,-4.98090292156266));
#65724=CARTESIAN_POINT('Ctrl Pts',(50.7416640518989,-0.256712202451727,
-5.80759535773281));
#65725=CARTESIAN_POINT('Ctrl Pts',(50.8422339618567,2.54627217443023,-5.2259509189974));
#65726=CARTESIAN_POINT('Ctrl Pts',(50.9428038718146,4.73178774091697,-3.37701788105352));
#65727=CARTESIAN_POINT('Ctrl Pts',(51.0433737817723,5.76984885348993,-0.709160913988021));
#65728=CARTESIAN_POINT('Ctrl Pts',(51.1439436917302,5.40872658594295,2.13066696425354));
#65729=CARTESIAN_POINT('Ctrl Pts',(51.2445136016879,3.73599277729174,4.45380993780282));
#65730=CARTESIAN_POINT('Ctrl Pts',(51.3450835116458,1.15728393619704,5.69690783540226));
#65731=CARTESIAN_POINT('Ctrl Pts',(51.4456534216035,-1.70206526320226,5.55851048697829));
#65732=CARTESIAN_POINT('Ctrl Pts',(51.5462233315614,-4.14866510146161,4.07217913038731));
#65733=CARTESIAN_POINT('Ctrl Pts',(51.6320364633792,-5.37784278716992,1.96133692425061));
#65734=CARTESIAN_POINT('Ctrl Pts',(51.6843262918778,-5.57723132289702,0.517934635056378));
#65735=CARTESIAN_POINT('Ctrl Pts',(51.7030928170571,-5.57739486550319,-5.00486370434358E-5));
#65736=CARTESIAN_POINT('Origin',(16.5082437683087,0.,0.));
#65737=CARTESIAN_POINT('',(48.8932437683088,-5.57740928288687,-6.1363554564314E-5));
#65738=CARTESIAN_POINT('',(49.1630928170571,-5.57763899819707,0.000132369982857178));
#65739=CARTESIAN_POINT('',(16.5082437683087,-5.57784,5.11151866531329E-13));
#65740=CARTESIAN_POINT('Ctrl Pts',(48.8932437683088,-5.57740928288687,-6.13635545640076E-5));
#65741=CARTESIAN_POINT('Ctrl Pts',(48.9075196355611,-5.57756230890984,-0.394094130874663));
#65742=CARTESIAN_POINT('Ctrl Pts',(48.9553188061326,-5.43970662246569,-1.71330876178174));
#65743=CARTESIAN_POINT('Ctrl Pts',(49.0366412800234,-4.41066789779351,-3.78682896691783));
#65744=CARTESIAN_POINT('Ctrl Pts',(49.1372111899812,-2.06849270248174,-5.43280800959264));
#65745=CARTESIAN_POINT('Ctrl Pts',(49.2377810999391,0.775290192564016,-5.76133578665817));
#65746=CARTESIAN_POINT('Ctrl Pts',(49.3383510098967,3.43106588330503,-4.69274459498218));
#65747=CARTESIAN_POINT('Ctrl Pts',(49.4389209198547,5.25481105090448,-2.48616687867213));
#65748=CARTESIAN_POINT('Ctrl Pts',(49.5394908298124,5.80426906215165,0.323304165552166));
#65749=CARTESIAN_POINT('Ctrl Pts',(49.6400607397703,4.94619682230831,3.05437422793956));
#65750=CARTESIAN_POINT('Ctrl Pts',(49.740630649728,2.88867611088328,5.04476116934454));
#65751=CARTESIAN_POINT('Ctrl Pts',(49.8412005596858,0.130653929224284,5.81179786985854));
#65752=CARTESIAN_POINT('Ctrl Pts',(49.9417704696436,-2.65905171780094,5.16947858989416));
#65753=CARTESIAN_POINT('Ctrl Pts',(50.0423403796015,-4.80393961224742,3.27356520191584));
#65754=CARTESIAN_POINT('Ctrl Pts',(50.1161648124898,-5.52327275317913,1.29912495283839));
#65755=CARTESIAN_POINT('Ctrl Pts',(50.1564659420589,-5.57811434466893,0.187166455713234));
#65756=CARTESIAN_POINT('Ctrl Pts',(50.1632437683087,-5.5779229988856,0.000138978711251916));
#65757=CARTESIAN_POINT('Ctrl Pts',(49.1630928170571,-5.57763899819707,0.000132369982857247));
#65758=CARTESIAN_POINT('Ctrl Pts',(49.186433678882,-5.57706759919496,-0.644030166077704));
#65759=CARTESIAN_POINT('Ctrl Pts',(49.2432978440262,-5.30539891262772,-2.21384039930619));
#65760=CARTESIAN_POINT('Ctrl Pts',(49.3336853124898,-3.86284675623355,-4.3442467623172));
#65761=CARTESIAN_POINT('Ctrl Pts',(49.4342552224475,-1.3210494073637,-5.66117421188848));
#65762=CARTESIAN_POINT('Ctrl Pts',(49.5348251324054,1.54110128559463,-5.60527178837798));
#65763=CARTESIAN_POINT('Ctrl Pts',(49.6353950423631,4.02953624342044,-4.19009578136448));
#65764=CARTESIAN_POINT('Ctrl Pts',(49.735964952321,5.54081213095715,-1.75882515432473));
#65765=CARTESIAN_POINT('Ctrl Pts',(49.8365348622786,5.70844584642674,1.09895905859165));
#65766=CARTESIAN_POINT('Ctrl Pts',(49.9371047722366,4.49178635813174,3.69024664581502));
#65767=CARTESIAN_POINT('Ctrl Pts',(50.0376746821943,2.18587254464829,5.38665259809838));
#65768=CARTESIAN_POINT('Ctrl Pts',(50.1382445921522,-0.650113479250571,
5.77679993232794));
#65769=CARTESIAN_POINT('Ctrl Pts',(50.2388145021098,-3.32844754406752,4.76607825580302));
#65770=CARTESIAN_POINT('Ctrl Pts',(50.337097243745,-5.15708123981284,2.64885721594067));
#65771=CARTESIAN_POINT('Ctrl Pts',(50.4018566820606,-5.57775371740881,0.861719031441649));
#65772=CARTESIAN_POINT('Ctrl Pts',(50.4330928170571,-5.5782539833292,-6.36399508389517E-5));
#65773=CARTESIAN_POINT('Origin',(16.5082437683087,0.,0.));
#65774=CARTESIAN_POINT('',(47.6232437683088,-5.57827554158207,-5.10498665022794E-5));
#65775=CARTESIAN_POINT('',(47.8930928170571,-5.577588863943,-0.000124534612764571));
#65776=CARTESIAN_POINT('',(16.5082437683087,-5.57784,5.11151866531329E-13));
#65777=CARTESIAN_POINT('Ctrl Pts',(47.6232437683088,-5.57827554158207,-5.10498665022129E-5));
#65778=CARTESIAN_POINT('Ctrl Pts',(47.6250500257439,-5.57829948763171,-0.0498838434567743));
#65779=CARTESIAN_POINT('Ctrl Pts',(47.6603795864984,-5.56550912456252,-1.0245779380622));
#65780=CARTESIAN_POINT('Ctrl Pts',(47.729232450572,-5.03220084112436,-2.91050161035883));
#65781=CARTESIAN_POINT('Ctrl Pts',(47.8298023605298,-3.03291992582039,-4.95938117640456));
#65782=CARTESIAN_POINT('Ctrl Pts',(47.9303722704876,-0.298158539329414,
-5.80561507634972));
#65783=CARTESIAN_POINT('Ctrl Pts',(48.0309421804455,2.50890603628552,-5.24399231792002));
#65784=CARTESIAN_POINT('Ctrl Pts',(48.1315120904031,4.70756305783949,-3.41070593657371));
#65785=CARTESIAN_POINT('Ctrl Pts',(48.2320820003611,5.76464009027266,-0.750326301641742));
#65786=CARTESIAN_POINT('Ctrl Pts',(48.3326519103187,5.42379686318222,2.09200681553594));
#65787=CARTESIAN_POINT('Ctrl Pts',(48.4332218202766,3.76768756572999,4.42703008080563));
#65788=CARTESIAN_POINT('Ctrl Pts',(48.5337917302344,1.19791727692173,5.6885023623944));
#65789=CARTESIAN_POINT('Ctrl Pts',(48.6343616401922,-1.6623469203385,5.57051771792849));
#65790=CARTESIAN_POINT('Ctrl Pts',(48.73493155015,-4.11949342041254,4.10168732212634));
#65791=CARTESIAN_POINT('Ctrl Pts',(48.8212255928555,-5.37067912645522,1.98789235424378));
#65792=CARTESIAN_POINT('Ctrl Pts',(48.8739963322418,-5.57720296557236,0.531193260999239));
#65793=CARTESIAN_POINT('Ctrl Pts',(48.8932437683088,-5.57740928288687,-6.13635545640076E-5));
#65794=CARTESIAN_POINT('Ctrl Pts',(47.8930928170571,-5.577588863943,-0.000124534612764085));
#65795=CARTESIAN_POINT('Ctrl Pts',(47.9039640690649,-5.57783588456841,-0.300157751719058));
#65796=CARTESIAN_POINT('Ctrl Pts',(47.948358624392,-5.48066132849218,-1.52523460204365));
#65797=CARTESIAN_POINT('Ctrl Pts',(48.0262764830383,-4.59631199877497,-3.55921072767047));
#65798=CARTESIAN_POINT('Ctrl Pts',(48.1268463929962,-2.34026552289286,-5.32139288874693));
#65799=CARTESIAN_POINT('Ctrl Pts',(48.2274163029538,0.483293327723093,-5.79314185510984));
#65800=CARTESIAN_POINT('Ctrl Pts',(48.3279862129118,3.18965396239895,-4.8600589085113));
#65801=CARTESIAN_POINT('Ctrl Pts',(48.4285561228695,5.12252625693867,-2.74841586027683));
#65802=CARTESIAN_POINT('Ctrl Pts',(48.5291260328273,5.81319034378827,0.0297156681595752));
#65803=CARTESIAN_POINT('Ctrl Pts',(48.629695942785,5.09416077643017,2.80064117264737));
#65804=CARTESIAN_POINT('Ctrl Pts',(48.730265852743,3.13980160598745,4.89241360364045));
#65805=CARTESIAN_POINT('Ctrl Pts',(48.8308357627007,0.424043248924028,5.79777994728061));
#65806=CARTESIAN_POINT('Ctrl Pts',(48.9314056726585,-2.39454523097487,5.29718964460052));
#65807=CARTESIAN_POINT('Ctrl Pts',(49.0319755826163,-4.63245855365558,3.51203541307753));
#65808=CARTESIAN_POINT('Ctrl Pts',(49.1092046307492,-5.48833418586149,1.48718441118965));
#65809=CARTESIAN_POINT('Ctrl Pts',(49.1529103755628,-5.57788827077974,0.281148014797861));
#65810=CARTESIAN_POINT('Ctrl Pts',(49.1630928170571,-5.57763899819707,0.000132369982857247));
#65811=CARTESIAN_POINT('Origin',(16.5082437683087,0.,0.));
#65812=CARTESIAN_POINT('',(46.3532437683088,-5.57760359476194,0.000127107498088562));
#65813=CARTESIAN_POINT('',(46.6230928170571,-5.57828356523297,4.54320993283769E-5));
#65814=CARTESIAN_POINT('',(16.5082437683087,-5.57784,5.11151866531329E-13));
#65815=CARTESIAN_POINT('Ctrl Pts',(46.3532437683088,-5.57760359476194,0.000127107498088495));
#65816=CARTESIAN_POINT('Ctrl Pts',(46.376103719246,-5.57707135817663,-0.63077470871854));
#65817=CARTESIAN_POINT('Ctrl Pts',(46.4324869735025,-5.3134714216754,-2.18730507792145));
#65818=CARTESIAN_POINT('Ctrl Pts',(46.5223935310784,-3.89375628397183,-4.31656425069105));
#65819=CARTESIAN_POINT('Ctrl Pts',(46.6229634410361,-1.36142352031365,-5.65160074029039));
#65820=CARTESIAN_POINT('Ctrl Pts',(46.723533350994,1.50105327506819,-5.61612891542932));
#65821=CARTESIAN_POINT('Ctrl Pts',(46.8241032609517,3.99952594339569,-4.21875066310145));
#65822=CARTESIAN_POINT('Ctrl Pts',(46.9246731709096,5.52811701335638,-1.79832900659305));
#65823=CARTESIAN_POINT('Ctrl Pts',(47.0252430808674,5.71614446633981,1.05818588596099));
#65824=CARTESIAN_POINT('Ctrl Pts',(47.1258129908252,4.5180118068569,3.65809161208624));
#65825=CARTESIAN_POINT('Ctrl Pts',(47.226382900783,2.22426517344535,5.37091327127076));
#65826=CARTESIAN_POINT('Ctrl Pts',(47.3269528107408,-0.608863849815457,
5.78129308560828));
#65827=CARTESIAN_POINT('Ctrl Pts',(47.4275227206986,-3.29434391362348,4.78971430338867));
#65828=CARTESIAN_POINT('Ctrl Pts',(47.5262863732212,-5.14706458748218,2.675303717135));
#65829=CARTESIAN_POINT('Ctrl Pts',(47.5915267224247,-5.57785506001607,0.874989777696537));
#65830=CARTESIAN_POINT('Ctrl Pts',(47.6232437683088,-5.57827554158207,-5.10498665022129E-5));
#65831=CARTESIAN_POINT('Ctrl Pts',(46.6230928170571,-5.57828356523297,4.54320993282641E-5));
#65832=CARTESIAN_POINT('Ctrl Pts',(46.655017762567,-5.57790150280944,-0.880727451819953));
#65833=CARTESIAN_POINT('Ctrl Pts',(46.7204660113962,-5.14269869890383,-2.68673433595031));
#65834=CARTESIAN_POINT('Ctrl Pts',(46.8194375635447,-3.27954872353672,-4.79985678577976));
#65835=CARTESIAN_POINT('Ctrl Pts',(46.9200074735025,-0.591021750409563,
-5.78314432507005));
#65836=CARTESIAN_POINT('Ctrl Pts',(47.0205773834603,2.24082748842343,-5.36402434382742));
#65837=CARTESIAN_POINT('Ctrl Pts',(47.1211472934181,4.52927799028237,-3.64413307671263));
#65838=CARTESIAN_POINT('Ctrl Pts',(47.2217172033759,5.71938247843022,-1.04054267546927));
#65839=CARTESIAN_POINT('Ctrl Pts',(47.3222871133337,5.52254163896719,1.8153784288464));
#65840=CARTESIAN_POINT('Ctrl Pts',(47.4228570232915,3.98648920601686,4.23107182689664));
#65841=CARTESIAN_POINT('Ctrl Pts',(47.5234269332493,1.48371657229165,5.62073394915242));
#65842=CARTESIAN_POINT('Ctrl Pts',(47.6239968432071,-1.37885605298849,5.64737292722768));
#65843=CARTESIAN_POINT('Ctrl Pts',(47.7245667531649,-3.90705727237777,4.30452883187085));
#65844=CARTESIAN_POINT('Ctrl Pts',(47.8142654111149,-5.31692771113889,2.17583281045649));
#65845=CARTESIAN_POINT('Ctrl Pts',(47.8704407657456,-5.57707415562073,0.62504428901131));
#65846=CARTESIAN_POINT('Ctrl Pts',(47.8930928170571,-5.577588863943,-0.000124534612764085));
#65847=CARTESIAN_POINT('Origin',(16.5082437683087,0.,0.));
#65848=CARTESIAN_POINT('',(45.0832437683088,-5.57762347393826,-0.000130215119483779));
#65849=CARTESIAN_POINT('',(45.3530928170571,-5.57741643618798,6.6124065845885E-5));
#65850=CARTESIAN_POINT('',(16.5082437683087,-5.57784,5.11151866531329E-13));
#65851=CARTESIAN_POINT('Ctrl Pts',(45.0832437683088,-5.57762347393826,-0.000130215119483572));
#65852=CARTESIAN_POINT('Ctrl Pts',(45.0936341094289,-5.57787263228915,-0.286885775923387));
#65853=CARTESIAN_POINT('Ctrl Pts',(45.1375477538683,-5.48603989704716,-1.49866881654569));
#65854=CARTESIAN_POINT('Ctrl Pts',(45.2149847016269,-4.62159948960023,-3.52631295931618));
#65855=CARTESIAN_POINT('Ctrl Pts',(45.3155546115848,-2.3781884143173,-5.30455321354411));
#65856=CARTESIAN_POINT('Ctrl Pts',(45.4161245215426,0.441931304224746,-5.79644387979909));
#65857=CARTESIAN_POINT('Ctrl Pts',(45.5166944315003,3.15488306191939,-4.88270189494794));
#65858=CARTESIAN_POINT('Ctrl Pts',(45.6172643414582,5.1027783929124,-2.78490890374179));
#65859=CARTESIAN_POINT('Ctrl Pts',(45.717834251416,5.81325435624223,-0.0117779007076735));
#65860=CARTESIAN_POINT('Ctrl Pts',(45.8184041613737,5.11402114239932,2.76420923310936));
#65861=CARTESIAN_POINT('Ctrl Pts',(45.9189740713316,3.1746422038206,4.86987800740792));
#65862=CARTESIAN_POINT('Ctrl Pts',(46.0195439812894,0.465415263638452,5.79460555704065));
#65863=CARTESIAN_POINT('Ctrl Pts',(46.1201138912472,-2.35667447733314,5.3141462472537));
#65864=CARTESIAN_POINT('Ctrl Pts',(46.220683801205,-4.60727268624445,3.54501104707727));
#65865=CARTESIAN_POINT('Ctrl Pts',(46.2983937602255,-5.4829987578168,1.51375007970848));
#65866=CARTESIAN_POINT('Ctrl Pts',(46.3425804159268,-5.57785186416004,0.294420319378661));
#65867=CARTESIAN_POINT('Ctrl Pts',(46.3532437683088,-5.57760359476194,0.000127107498088495));
#65868=CARTESIAN_POINT('Ctrl Pts',(45.3530928170571,-5.57741643618798,6.61240658456769E-5));
#65869=CARTESIAN_POINT('Ctrl Pts',(45.3725481527499,-5.57719134984669,-0.536924835055485));
#65870=CARTESIAN_POINT('Ctrl Pts',(45.4255267917619,-5.36754962672399,-1.99937184209296));
#65871=CARTESIAN_POINT('Ctrl Pts',(45.5120287340932,-4.1068173316415,-4.11437922396275));
#65872=CARTESIAN_POINT('Ctrl Pts',(45.6125986440511,-1.64515019125313,-5.57562066879259));
#65873=CARTESIAN_POINT('Ctrl Pts',(45.7131685540088,1.21546445432158,-5.68477890109438));
#65874=CARTESIAN_POINT('Ctrl Pts',(45.8137384639667,3.78133001603,-4.41538314350158));
#65875=CARTESIAN_POINT('Ctrl Pts',(45.9143083739244,5.43022630392851,-2.07526077449805));
#65876=CARTESIAN_POINT('Ctrl Pts',(46.0148782838823,5.76229738761891,0.768110545877321));
#65877=CARTESIAN_POINT('Ctrl Pts',(46.11544819384,4.69701631516247,3.42521572008903));
#65878=CARTESIAN_POINT('Ctrl Pts',(46.2160181037979,2.4927128296055,5.25170903070299));
#65879=CARTESIAN_POINT('Ctrl Pts',(46.3165880137556,-0.316071371332041,
5.80466742219323));
#65880=CARTESIAN_POINT('Ctrl Pts',(46.4171579237135,-3.04820853680487,4.94999896062587));
#65881=CARTESIAN_POINT('Ctrl Pts',(46.5177278336712,-5.04115775608791,2.89496001220778));
#65882=CARTESIAN_POINT('Ctrl Pts',(46.5863727981191,-5.56705141744763,1.01309914407614));
#65883=CARTESIAN_POINT('Ctrl Pts',(46.6214944592478,-5.57830269361201,0.0441423035201426));
#65884=CARTESIAN_POINT('Ctrl Pts',(46.6230928170571,-5.57828356523297,4.54320993282641E-5));
#65885=CARTESIAN_POINT('Origin',(16.5082437683087,0.,0.));
#65886=CARTESIAN_POINT('',(43.8132437683088,-5.57826379807651,5.82713151345457E-5));
#65887=CARTESIAN_POINT('',(44.0830928170571,-5.57790494923753,-0.000140205289279327));
#65888=CARTESIAN_POINT('',(16.5082437683087,-5.57784,5.11151866531329E-13));
#65889=CARTESIAN_POINT('Ctrl Pts',(43.8132437683088,-5.57826379807651,5.82713151345022E-5));
#65890=CARTESIAN_POINT('Ctrl Pts',(43.844687802931,-5.5777964967119,-0.867455764163641));
#65891=CARTESIAN_POINT('Ctrl Pts',(43.9096551408726,-5.15276511634523,-2.66029104170784));
#65892=CARTESIAN_POINT('Ctrl Pts',(44.0081457821333,-3.31372511850974,-4.77632607432447));
#65893=CARTESIAN_POINT('Ctrl Pts',(44.1087156920912,-0.632285046713879,
-5.77877846512705));
#65894=CARTESIAN_POINT('Ctrl Pts',(44.2092856020489,2.202483604621,-5.37988205267457));
#65895=CARTESIAN_POINT('Ctrl Pts',(44.3098555120068,4.50315187779634,-3.67636887360525));
#65896=CARTESIAN_POINT('Ctrl Pts',(44.4104254219645,5.71180969704834,-1.08133940741041));
#65897=CARTESIAN_POINT('Ctrl Pts',(44.5109953319224,5.53535858165572,1.77591393423347));
#65898=CARTESIAN_POINT('Ctrl Pts',(44.6115652418801,4.01658777520697,4.20250967558343));
#65899=CARTESIAN_POINT('Ctrl Pts',(44.712135151838,1.52379789086441,5.61000043824521));
#65900=CARTESIAN_POINT('Ctrl Pts',(44.8127050617957,-1.33851167028378,5.65707092388173));
#65901=CARTESIAN_POINT('Ctrl Pts',(44.9132749717536,-3.87623330361735,4.33230658024589));
#65902=CARTESIAN_POINT('Ctrl Pts',(45.0034545405912,-5.30890197702976,2.20236946067521));
#65903=CARTESIAN_POINT('Ctrl Pts',(45.0601108061096,-5.57706875002244,0.638299791343409));
#65904=CARTESIAN_POINT('Ctrl Pts',(45.0832437683088,-5.57762347393826,-0.000130215119483572));
#65905=CARTESIAN_POINT('Ctrl Pts',(44.0830928170571,-5.57790494923753,-0.000140205289278963));
#65906=CARTESIAN_POINT('Ctrl Pts',(44.0900785429327,-5.5781024864199,-0.192906266953961));
#65907=CARTESIAN_POINT('Ctrl Pts',(44.1305875721276,-5.52128067157015,-1.31060778880162));
#65908=CARTESIAN_POINT('Ctrl Pts',(44.2046199046419,-4.79381558281113,-3.28837302507556));
#65909=CARTESIAN_POINT('Ctrl Pts',(44.3051898145996,-2.64308772173875,-5.17765895837504));
#65910=CARTESIAN_POINT('Ctrl Pts',(44.4057597245574,0.148586636609559,-5.81136705134586));
#65911=CARTESIAN_POINT('Ctrl Pts',(44.5063296345153,2.90422886348763,-5.03582363695677));
#65912=CARTESIAN_POINT('Ctrl Pts',(44.606899544473,4.95559809101348,-3.03909732558712));
#65913=CARTESIAN_POINT('Ctrl Pts',(44.7074694544309,5.80523904738957,-0.305392528904701));
#65914=CARTESIAN_POINT('Ctrl Pts',(44.8080393643886,5.24711453208993,2.50236969314653));
#65915=CARTESIAN_POINT('Ctrl Pts',(44.9086092743465,3.41656925962507,4.70330941872129));
#65916=CARTESIAN_POINT('Ctrl Pts',(45.0091791843043,0.757508882781974,5.76370065899971));
#65917=CARTESIAN_POINT('Ctrl Pts',(45.109749094262,-2.08524674605032,5.42639945102955));
#65918=CARTESIAN_POINT('Ctrl Pts',(45.2103190042198,-4.42233183400564,3.77320104738504));
#65919=CARTESIAN_POINT('Ctrl Pts',(45.2914335784849,-5.44235309585835,1.701824445005));
#65920=CARTESIAN_POINT('Ctrl Pts',(45.3390248494306,-5.57757919397393,0.388359163462492));
#65921=CARTESIAN_POINT('Ctrl Pts',(45.3530928170571,-5.57741643618798,6.61240658456769E-5));
#65922=CARTESIAN_POINT('Origin',(16.5082437683087,0.,0.));
#65923=CARTESIAN_POINT('',(42.5432437683088,-5.57740073011504,5.4988692936847E-5));
#65924=CARTESIAN_POINT('',(42.8130928170571,-5.57803330847514,0.000126527485840092));
#65925=CARTESIAN_POINT('',(16.5082437683087,-5.57784,5.11151866531329E-13));
#65926=CARTESIAN_POINT('Ctrl Pts',(42.5432437683088,-5.57740073011504,5.49886929369914E-5));
#65927=CARTESIAN_POINT('Ctrl Pts',(42.5622181931139,-5.57721881714937,-0.523666463456379));
#65928=CARTESIAN_POINT('Ctrl Pts',(42.6147159212383,-5.37475882476217,-1.97281714130688));
#65929=CARTESIAN_POINT('Ctrl Pts',(42.7007369526818,-4.13607991865755,-4.08496117922704));
#65930=CARTESIAN_POINT('Ctrl Pts',(42.8013068626397,-1.68490539227271,-5.56373604230149));
#65931=CARTESIAN_POINT('Ctrl Pts',(42.9018767725975,1.1748572413234,-5.69330970454131));
#65932=CARTESIAN_POINT('Ctrl Pts',(43.0024466825553,3.74971800524932,-4.4422606643941));
#65933=CARTESIAN_POINT('Ctrl Pts',(43.1030165925131,5.41527538076706,-2.11396723715677));
#65934=CARTESIAN_POINT('Ctrl Pts',(43.2035865024709,5.76763313807318,0.726961425327436));
#65935=CARTESIAN_POINT('Ctrl Pts',(43.3041564124287,4.72134482434061,3.39160256795904));
#65936=CARTESIAN_POINT('Ctrl Pts',(43.4047263223865,2.5301344549744,5.23378300744937));
#65937=CARTESIAN_POINT('Ctrl Pts',(43.5052962323444,-0.274631341710833,
5.80677557302366));
#65938=CARTESIAN_POINT('Ctrl Pts',(43.6058661423021,-3.01279927444167,4.97163006077864));
#65939=CARTESIAN_POINT('Ctrl Pts',(43.7064360522599,-5.02036597662438,2.93086853851659));
#65940=CARTESIAN_POINT('Ctrl Pts',(43.7755619275955,-5.56345669958936,1.03965202892801));
#65941=CARTESIAN_POINT('Ctrl Pts',(43.8111644996118,-5.57829469885344,0.0574235172151608));
#65942=CARTESIAN_POINT('Ctrl Pts',(43.8132437683088,-5.57826379807651,5.82713151345022E-5));
#65943=CARTESIAN_POINT('Ctrl Pts',(42.8130928170571,-5.57803330847514,0.000126527485840109));
#65944=CARTESIAN_POINT('Ctrl Pts',(42.8411322364349,-5.57727619059748,-0.77354965244955));
#65945=CARTESIAN_POINT('Ctrl Pts',(42.9026949591319,-5.22076416624656,-2.47289174149367));
#65946=CARTESIAN_POINT('Ctrl Pts',(42.9977809851481,-3.55074929685554,-4.60285177090544));
#65947=CARTESIAN_POINT('Ctrl Pts',(43.0983508951061,-0.923366230433899,
-5.73946511432395));
#65948=CARTESIAN_POINT('Ctrl Pts',(43.1989208050638,1.92793235200782,-5.48426310821507));
#65949=CARTESIAN_POINT('Ctrl Pts',(43.2994907150216,4.31170899870712,-3.89913201937502));
#65950=CARTESIAN_POINT('Ctrl Pts',(43.4000606249794,5.64989992486267,-1.36846477232117));
#65951=CARTESIAN_POINT('Ctrl Pts',(43.5006305349373,5.61799498283493,1.49405400400684));
#65952=CARTESIAN_POINT('Ctrl Pts',(43.601200444895,4.22373109360091,3.99426597048771));
#65953=CARTESIAN_POINT('Ctrl Pts',(43.7017703548528,1.80521605007753,5.52587187750403));
#65954=CARTESIAN_POINT('Ctrl Pts',(43.8023402648106,-1.05106233160792,5.71745861105458));
#65955=CARTESIAN_POINT('Ctrl Pts',(43.9029101747684,-3.65245900266303,4.52256655317676));
#65956=CARTESIAN_POINT('Ctrl Pts',(43.9964943588506,-5.24896409347016,2.39013445685884));
#65957=CARTESIAN_POINT('Ctrl Pts',(44.0565552396135,-5.57715453927749,0.732145083454281));
#65958=CARTESIAN_POINT('Ctrl Pts',(44.0830928170571,-5.57790494923753,-0.000140205289278963));
#65959=CARTESIAN_POINT('Origin',(16.5082437683087,0.,0.));
#65960=CARTESIAN_POINT('',(41.2732437683088,-5.57794663527581,-0.000137039997376016));
#65961=CARTESIAN_POINT('',(41.5430928170571,-5.57737735400439,-3.01529304447268E-5));
#65962=CARTESIAN_POINT('',(16.5082437683087,-5.57784,5.11151866531329E-13));
#65963=CARTESIAN_POINT('Ctrl Pts',(41.2732437683088,-5.57794663527581,-0.000137039997375726));
#65964=CARTESIAN_POINT('Ctrl Pts',(41.2797485832967,-5.57812947862225,-0.179628846193896));
#65965=CARTESIAN_POINT('Ctrl Pts',(41.319776701604,-5.52586098423105,-1.28404603494069));
#65966=CARTESIAN_POINT('Ctrl Pts',(41.3933281232305,-4.81716488388169,-3.25407243478249));
#65967=CARTESIAN_POINT('Ctrl Pts',(41.4938980331883,-2.6799769691159,-5.15866149057317));
#65968=CARTESIAN_POINT('Ctrl Pts',(41.5944679431461,0.107103053659489,-5.81227957562358));
#65969=CARTESIAN_POINT('Ctrl Pts',(41.6950378531039,2.8682106781198,-5.0564248669622));
#65970=CARTESIAN_POINT('Ctrl Pts',(41.7956077630617,4.93377968217404,-3.07439148077804));
#65971=CARTESIAN_POINT('Ctrl Pts',(41.8961776730195,5.80291136044017,-0.346820807029599));
#65972=CARTESIAN_POINT('Ctrl Pts',(41.9967475829773,5.26484202911207,2.46485361387027));
#65973=CARTESIAN_POINT('Ctrl Pts',(42.0973174929351,3.4500530378513,4.67880315522326));
#65974=CARTESIAN_POINT('Ctrl Pts',(42.1978874028929,0.798629154816186,5.75814695908256));
#65975=CARTESIAN_POINT('Ctrl Pts',(42.2984573128507,-2.04646161077897,5.44114508214238));
#65976=CARTESIAN_POINT('Ctrl Pts',(42.3990272228085,-4.39528719741307,3.80467020667639));
#65977=CARTESIAN_POINT('Ctrl Pts',(42.4806227079612,-5.43620232966336,1.72838970928726));
#65978=CARTESIAN_POINT('Ctrl Pts',(42.5286948897946,-5.57754021416608,0.401624989409368));
#65979=CARTESIAN_POINT('Ctrl Pts',(42.5432437683088,-5.57740073011504,5.49886929369914E-5));
#65980=CARTESIAN_POINT('Ctrl Pts',(41.5430928170571,-5.57737735400439,-3.0152930444588E-5));
#65981=CARTESIAN_POINT('Ctrl Pts',(41.5586626266178,-5.57745878542451,-0.429784476705716));
#65982=CARTESIAN_POINT('Ctrl Pts',(41.6077557394976,-5.42280542730085,-1.7847836899185));
#65983=CARTESIAN_POINT('Ctrl Pts',(41.6903721556968,-4.33713329105347,-3.87083192733591));
#65984=CARTESIAN_POINT('Ctrl Pts',(41.7909420656546,-1.96378107173494,-5.4715289358956));
#65985=CARTESIAN_POINT('Ctrl Pts',(41.8915119756124,0.88578636700025,-5.74538488754965));
#65986=CARTESIAN_POINT('Ctrl Pts',(41.9920818855702,3.52055137424819,-4.62598994976497));
#65987=CARTESIAN_POINT('Ctrl Pts',(42.0926517955281,5.30158570383253,-2.38479643134711));
#65988=CARTESIAN_POINT('Ctrl Pts',(42.1932217054858,5.7969900639945,0.434708168771271));
#65989=CARTESIAN_POINT('Ctrl Pts',(42.2937916154436,4.88662932385308,3.14879641217187));
#65990=CARTESIAN_POINT('Ctrl Pts',(42.3943615254014,2.79126517922797,5.09930423619505));
#65991=CARTESIAN_POINT('Ctrl Pts',(42.4949314353592,0.0190216314411856,
5.81323517256825));
#65992=CARTESIAN_POINT('Ctrl Pts',(42.595501345317,-2.75783464559572,5.11746158379321));
#65993=CARTESIAN_POINT('Ctrl Pts',(42.6960712552748,-4.86591839509884,3.18070796620598));
#65994=CARTESIAN_POINT('Ctrl Pts',(42.7686017458548,-5.53526120505294,1.22766026552409));
#65995=CARTESIAN_POINT('Ctrl Pts',(42.8076089331156,-5.57818138381562,0.151440301922733));
#65996=CARTESIAN_POINT('Ctrl Pts',(42.8130928170571,-5.57803330847514,0.000126527485840109));
#65997=CARTESIAN_POINT('Origin',(16.5082437683087,0.,0.));
#65998=CARTESIAN_POINT('',(40.0032437683088,-5.57799292358802,0.000132115289384061));
#65999=CARTESIAN_POINT('',(40.2730928170571,-5.57820901493156,-8.33809270067709E-5));
#66000=CARTESIAN_POINT('',(16.5082437683087,-5.57784,5.11151866531329E-13));
#66001=CARTESIAN_POINT('Ctrl Pts',(40.0032437683088,-5.57799292358802,0.00013211528938413));
#66002=CARTESIAN_POINT('Ctrl Pts',(40.0308022767989,-5.57723081277639,-0.760290445687694));
#66003=CARTESIAN_POINT('Ctrl Pts',(40.0918840886083,-5.22991270231027,-2.44639707817582));
#66004=CARTESIAN_POINT('Ctrl Pts',(40.1864892037368,-3.58351262028272,-4.57739032960799));
#66005=CARTESIAN_POINT('Ctrl Pts',(40.2870591136947,-0.964309291247043,
-5.73272819171892));
#66006=CARTESIAN_POINT('Ctrl Pts',(40.3876290236525,1.88873821081094,-5.49788440223482));
#66007=CARTESIAN_POINT('Ctrl Pts',(40.4881989336103,4.28376832262728,-3.92980837794532));
#66008=CARTESIAN_POINT('Ctrl Pts',(40.5887688435681,5.63998830379708,-1.40875720489588));
#66009=CARTESIAN_POINT('Ctrl Pts',(40.6893387535259,5.62851597635984,1.45391637764221));
#66010=CARTESIAN_POINT('Ctrl Pts',(40.7899086634837,4.25213336984329,3.964016490175));
#66011=CARTESIAN_POINT('Ctrl Pts',(40.8904785734415,1.84461208149807,5.51284601617945));
#66012=CARTESIAN_POINT('Ctrl Pts',(40.9910484833993,-1.01022604871547,5.7248151288763));
#66013=CARTESIAN_POINT('Ctrl Pts',(41.0916183933571,-3.62008523174703,4.54852150090567));
#66014=CARTESIAN_POINT('Ctrl Pts',(41.1856834883269,-5.24005244945936,2.41663978755469));
#66015=CARTESIAN_POINT('Ctrl Pts',(41.2462252799775,-5.57718717465606,0.745402576464613));
#66016=CARTESIAN_POINT('Ctrl Pts',(41.2732437683088,-5.57794663527581,-0.000137039997375726));
#66017=CARTESIAN_POINT('Ctrl Pts',(40.2730928170571,-5.57820901493156,-8.33809270062505E-5));
#66018=CARTESIAN_POINT('Ctrl Pts',(40.2761930168006,-5.57827097512514,-0.0856176805388213));
#66019=CARTESIAN_POINT('Ctrl Pts',(40.3128165198633,-5.55550823955623,-1.09602464080041));
#66020=CARTESIAN_POINT('Ctrl Pts',(40.3829633262454,-4.9753803739444,-3.00660192386958));
#66021=CARTESIAN_POINT('Ctrl Pts',(40.4835332362031,-2.93712200893205,-5.01671000743458));
#66022=CARTESIAN_POINT('Ctrl Pts',(40.584103146161,-0.186614085112543,-5.81027023272455));
#66023=CARTESIAN_POINT('Ctrl Pts',(40.6846730561188,2.609147593704,-5.19484492822605));
#66024=CARTESIAN_POINT('Ctrl Pts',(40.7852429660765,4.7721932270764,-3.31967420050424));
#66025=CARTESIAN_POINT('Ctrl Pts',(40.8858128760344,5.77798611092356,-0.639485336830895));
#66026=CARTESIAN_POINT('Ctrl Pts',(40.9863827859921,5.38262233672791,2.19577817053662));
#66027=CARTESIAN_POINT('Ctrl Pts',(41.08695269595,3.6819772793914,4.49856736173782));
#66028=CARTESIAN_POINT('Ctrl Pts',(41.1875226059078,1.08845590135412,5.7104578402134));
#66029=CARTESIAN_POINT('Ctrl Pts',(41.2880925158656,-1.76901509578748,5.53756720816311));
#66030=CARTESIAN_POINT('Ctrl Pts',(41.3886624258233,-4.19750145501954,4.02182129502992));
#66031=CARTESIAN_POINT('Ctrl Pts',(41.4736625262206,-5.38971481780673,1.91643858201631));
#66032=CARTESIAN_POINT('Ctrl Pts',(41.5251393232985,-5.57728345571441,0.495518077098019));
#66033=CARTESIAN_POINT('Ctrl Pts',(41.5430928170571,-5.57737735400439,-3.0152930444588E-5));
#66034=CARTESIAN_POINT('Origin',(16.5082437683087,0.,0.));
#66035=CARTESIAN_POINT('',(38.7332437683088,-5.57738665159885,-4.20214438878431E-5));
#66036=CARTESIAN_POINT('',(39.0030928170571,-5.57770250057755,0.000138966530263268));
#66037=CARTESIAN_POINT('',(16.5082437683087,-5.57784,5.11151866531329E-13));
#66038=CARTESIAN_POINT('Ctrl Pts',(38.7332437683088,-5.57738665159885,-4.20214438870761E-5));
#66039=CARTESIAN_POINT('Ctrl Pts',(38.7483326669818,-5.57749685500109,-0.416520364740088));
#66040=CARTESIAN_POINT('Ctrl Pts',(38.796944868974,-5.42917366098025,-1.75821956594524));
#66041=CARTESIAN_POINT('Ctrl Pts',(38.8790803742854,-4.36465164317584,-3.8397761605381));
#66042=CARTESIAN_POINT('Ctrl Pts',(38.9796502842433,-2.00278518012054,-5.45737266929827));
#66043=CARTESIAN_POINT('Ctrl Pts',(39.080220194201,0.844754965059067,-5.75156100361652));
#66044=CARTESIAN_POINT('Ctrl Pts',(39.1807901041589,3.48744275840115,-4.65100074566642));
#66045=CARTESIAN_POINT('Ctrl Pts',(39.2813600141166,5.28442868492169,-2.42257681060703));
#66046=CARTESIAN_POINT('Ctrl Pts',(39.3819299240745,5.79994520433648,0.39331991560096));
#66047=CARTESIAN_POINT('Ctrl Pts',(39.4824998340322,4.90898000445885,3.11383690085679));
#66048=CARTESIAN_POINT('Ctrl Pts',(39.5830697439901,2.8275913792907,5.07925111813494));
#66049=CARTESIAN_POINT('Ctrl Pts',(39.6836396539479,0.0605142787163216,
5.8129513116304));
#66050=CARTESIAN_POINT('Ctrl Pts',(39.7842095639056,-2.72123748235436,5.13701581601069));
#66051=CARTESIAN_POINT('Ctrl Pts',(39.8847794738635,-4.84309149647335,3.21535840709891));
#66052=CARTESIAN_POINT('Ctrl Pts',(39.9577908753311,-5.530887896341,1.25422042093262));
#66053=CARTESIAN_POINT('Ctrl Pts',(39.9972789734796,-5.57815787571633,0.164718836712659));
#66054=CARTESIAN_POINT('Ctrl Pts',(40.0032437683088,-5.57799292358802,0.00013211528938413));
#66055=CARTESIAN_POINT('Ctrl Pts',(39.0030928170571,-5.57770250057755,0.00013896653026358));
#66056=CARTESIAN_POINT('Ctrl Pts',(39.0272467103027,-5.57707034665817,-0.666439870181227));
#66057=CARTESIAN_POINT('Ctrl Pts',(39.0849239068676,-5.29150453091099,-2.25869376639851));
#66058=CARTESIAN_POINT('Ctrl Pts',(39.1761244067517,-3.81014410570237,-4.39054289215228));
#66059=CARTESIAN_POINT('Ctrl Pts',(39.2766943167096,-1.25264064176956,-5.67670295300313));
#66060=CARTESIAN_POINT('Ctrl Pts',(39.3772642266673,1.60862709948338,-5.58626743441943));
#66061=CARTESIAN_POINT('Ctrl Pts',(39.4778341366252,4.07980415386393,-4.14116687180823));
#66062=CARTESIAN_POINT('Ctrl Pts',(39.578404046583,5.5616322129449,-1.69183690761873));
#66063=CARTESIAN_POINT('Ctrl Pts',(39.6789739565408,5.69476924799924,1.16776205028657));
#66064=CARTESIAN_POINT('Ctrl Pts',(39.7795438664986,4.44692964263445,3.74417971624045));
#66065=CARTESIAN_POINT('Ctrl Pts',(39.8801137764563,2.12071342697536,5.41263702410329));
#66066=CARTESIAN_POINT('Ctrl Pts',(39.9806836864142,-0.719773969154297,
5.76853451297425));
#66067=CARTESIAN_POINT('Ctrl Pts',(40.081253596372,-3.38571679736614,4.72556734816892));
#66068=CARTESIAN_POINT('Ctrl Pts',(40.1787233065863,-5.17375445747103,2.6041302969216));
#66069=CARTESIAN_POINT('Ctrl Pts',(40.2426697134813,-5.57760098269404,0.839287973076047));
#66070=CARTESIAN_POINT('Ctrl Pts',(40.2730928170571,-5.57820901493156,-8.33809270062505E-5));
#66071=CARTESIAN_POINT('Origin',(16.5082437683087,0.,0.));
#66072=CARTESIAN_POINT('',(37.4632437683088,-5.57823681479003,-7.19583867586569E-5));
#66073=CARTESIAN_POINT('',(37.7330928170571,-5.5775348825402,-0.000112846948039924));
#66074=CARTESIAN_POINT('',(16.5082437683087,-5.57784,5.11151866531329E-13));
#66075=CARTESIAN_POINT('Ctrl Pts',(37.4632437683088,-5.57823681479003,-7.19583867583775E-5));
#66076=CARTESIAN_POINT('Ctrl Pts',(37.4658630571646,-5.57828328322656,-0.0723369141437499));
#66077=CARTESIAN_POINT('Ctrl Pts',(37.5020056493397,-5.55930617745199,-1.06946971283999));
#66078=CARTESIAN_POINT('Ctrl Pts',(37.5716715448341,-4.99671385197042,-2.97101255649336));
#66079=CARTESIAN_POINT('Ctrl Pts',(37.6722414547918,-2.97285496046918,-4.99561791106246));
#66080=CARTESIAN_POINT('Ctrl Pts',(37.7728113647497,-0.228081300173006,
-5.80879022257005));
#66081=CARTESIAN_POINT('Ctrl Pts',(37.8733812747074,2.57200187907619,-5.21333590547767));
#66082=CARTESIAN_POINT('Ctrl Pts',(37.9739511846653,4.74837681670243,-3.35365211909601));
#66083=CARTESIAN_POINT('Ctrl Pts',(38.074521094623,5.77327446381726,-0.680710580753474));
#66084=CARTESIAN_POINT('Ctrl Pts',(38.1750910045808,5.39815802325663,2.15730268744658));
#66085=CARTESIAN_POINT('Ctrl Pts',(38.2756609145386,3.71399290894551,4.47217191100887));
#66086=CARTESIAN_POINT('Ctrl Pts',(38.3762308244964,1.1291877113267,5.70254329592533));
#66087=CARTESIAN_POINT('Ctrl Pts',(38.4768007344543,-1.72944453425166,5.55005284049271));
#66088=CARTESIAN_POINT('Ctrl Pts',(38.5773706444121,-4.16868796902945,4.05167934888527));
#66089=CARTESIAN_POINT('Ctrl Pts',(38.6628516556969,-5.38272866987952,1.94299661298295));
#66090=CARTESIAN_POINT('Ctrl Pts',(38.7148093636625,-5.57725201393216,0.508777772045055));
#66091=CARTESIAN_POINT('Ctrl Pts',(38.7332437683088,-5.57738665159885,-4.20214438870761E-5));
#66092=CARTESIAN_POINT('Ctrl Pts',(37.7330928170571,-5.5775348825402,-0.000112846948039542));
#66093=CARTESIAN_POINT('Ctrl Pts',(37.7447771004856,-5.5777721557373,-0.32259368260295));
#66094=CARTESIAN_POINT('Ctrl Pts',(37.7899846872333,-5.47134065168775,-1.57014734993002));
#66095=CARTESIAN_POINT('Ctrl Pts',(37.8687155773003,-4.55302886484057,-3.61441463448453));
#66096=CARTESIAN_POINT('Ctrl Pts',(37.9692854872581,-2.27588264393015,-5.34924510422778));
#66097=CARTESIAN_POINT('Ctrl Pts',(38.0698553972159,0.553163158988311,-5.78688824097939));
#66098=CARTESIAN_POINT('Ctrl Pts',(38.1704253071738,3.24806737203082,-4.82121596081281));
#66099=CARTESIAN_POINT('Ctrl Pts',(38.2709952171315,5.15531804338536,-2.6864029603901));
#66100=CARTESIAN_POINT('Ctrl Pts',(38.3715651270894,5.81240852706456,0.0998604453944716));
#66101=CARTESIAN_POINT('Ctrl Pts',(38.4721350370471,5.0599949464186,2.86190777913362));
#66102=CARTESIAN_POINT('Ctrl Pts',(38.572704947005,3.08053694705489,4.92994494004518));
#66103=CARTESIAN_POINT('Ctrl Pts',(38.6732748569627,0.354051389844875,5.80247469683378));
#66104=CARTESIAN_POINT('Ctrl Pts',(38.7738447669205,-2.45829132462492,5.26790933457678));
#66105=CARTESIAN_POINT('Ctrl Pts',(38.8744146768784,-4.67450050904083,3.45588049345234));
#66106=CARTESIAN_POINT('Ctrl Pts',(38.9508306935905,-5.49712786015583,1.44227304681289));
#66107=CARTESIAN_POINT('Ctrl Pts',(38.9937234069834,-5.5779477160896,0.258708067753872));
#66108=CARTESIAN_POINT('Ctrl Pts',(39.0030928170571,-5.57770250057755,0.00013896653026358));
#66109=CARTESIAN_POINT('Origin',(16.5082437683087,0.,0.));
#66110=CARTESIAN_POINT('',(36.1932437683088,-5.57766442098412,0.000135422462255629));
#66111=CARTESIAN_POINT('',(36.4630928170571,-5.57830649769973,2.26809192473663E-5));
#66112=CARTESIAN_POINT('',(16.5082437683087,-5.57784,5.11151866531329E-13));
#66113=CARTESIAN_POINT('Ctrl Pts',(36.1932437683088,-5.57766442098412,0.00013542246225573));
#66114=CARTESIAN_POINT('Ctrl Pts',(36.2169167506667,-5.57706728688419,-0.653184446091782));
#66115=CARTESIAN_POINT('Ctrl Pts',(36.2741130363439,-5.29976066215789,-2.2321640105613));
#66116=CARTESIAN_POINT('Ctrl Pts',(36.3648326253404,-3.84138542393408,-4.36323537688503));
#66117=CARTESIAN_POINT('Ctrl Pts',(36.4654025352982,-1.29312733691379,-5.66761736709884));
#66118=CARTESIAN_POINT('Ctrl Pts',(36.565972445256,1.56871301614697,-5.59760702463875));
#66119=CARTESIAN_POINT('Ctrl Pts',(36.6665423552138,4.05014181318524,-4.17018179728447));
#66120=CARTESIAN_POINT('Ctrl Pts',(36.7671122651716,5.54941470700435,-1.73149107390076));
#66121=CARTESIAN_POINT('Ctrl Pts',(36.8676821751295,5.70295931147022,1.12708474438672));
#66122=CARTESIAN_POINT('Ctrl Pts',(36.9682520850872,4.47354119217547,3.71234348238731));
#66123=CARTESIAN_POINT('Ctrl Pts',(37.068821995045,2.15929318473071,5.39736212160066));
#66124=CARTESIAN_POINT('Ctrl Pts',(37.1693919050028,-0.678581561229704,
5.77352509252997));
#66125=CARTESIAN_POINT('Ctrl Pts',(37.2699618149606,-3.35190086273439,4.74961319853676));
#66126=CARTESIAN_POINT('Ctrl Pts',(37.3679124360626,-5.16393173391408,2.63058883473529));
#66127=CARTESIAN_POINT('Ctrl Pts',(37.4323397538453,-5.57768855100025,0.852555361794227));
#66128=CARTESIAN_POINT('Ctrl Pts',(37.4632437683088,-5.57823681479003,-7.19583867583775E-5));
#66129=CARTESIAN_POINT('Ctrl Pts',(36.4630928170571,-5.57830649769973,2.26809192474704E-5));
#66130=CARTESIAN_POINT('Ctrl Pts',(36.4958307939877,-5.57809885394134,-0.903170003029449));
#66131=CARTESIAN_POINT('Ctrl Pts',(36.5620920742375,-5.12541758812386,-2.73142201137822));
#66132=CARTESIAN_POINT('Ctrl Pts',(36.6618766578068,-3.22139075996267,-4.83908116956871));
#66133=CARTESIAN_POINT('Ctrl Pts',(36.7624465677644,-0.5211943400678,-5.78985504602047));
#66134=CARTESIAN_POINT('Ctrl Pts',(36.8630164777224,2.30539125863451,-5.33659405788552));
#66135=CARTESIAN_POINT('Ctrl Pts',(36.9635863876801,4.57292146166484,-3.58921360460651));
#66136=CARTESIAN_POINT('Ctrl Pts',(37.064156297638,5.73152214674337,-0.97145194190844));
#66137=CARTESIAN_POINT('Ctrl Pts',(37.1647262075957,5.50023364509525,1.88188598044871));
#66138=CARTESIAN_POINT('Ctrl Pts',(37.2652961175536,3.93514321927045,4.27886817252847));
#66139=CARTESIAN_POINT('Ctrl Pts',(37.3658660275113,1.41578395025668,5.63822851614255));
#66140=CARTESIAN_POINT('Ctrl Pts',(37.4664359374691,-1.44690170794694,5.63032329814084));
#66141=CARTESIAN_POINT('Ctrl Pts',(37.5670058474269,-3.9587149475079,4.25706952708373));
#66142=CARTESIAN_POINT('Ctrl Pts',(37.6558914739562,-5.33025071134417,2.13096314978175));
#66143=CARTESIAN_POINT('Ctrl Pts',(37.7112537971663,-5.57709139671561,0.602634033284536));
#66144=CARTESIAN_POINT('Ctrl Pts',(37.7330928170571,-5.5775348825402,-0.000112846948039542));
#66145=CARTESIAN_POINT('Origin',(16.5082437683087,0.,0.));
#66146=CARTESIAN_POINT('',(34.9232437683088,-5.57756608151389,-0.000120065769840256));
#66147=CARTESIAN_POINT('',(35.1930928170571,-5.57744951564134,8.38323760708748E-5));
#66148=CARTESIAN_POINT('',(16.5082437683087,-5.57784,5.11151866531329E-13));
#66149=CARTESIAN_POINT('Ctrl Pts',(34.9232437683088,-5.57756608151389,-0.000120065769840146));
#66150=CARTESIAN_POINT('Ctrl Pts',(34.9344471408496,-5.57781006450218,-0.309323022954409));
#66151=CARTESIAN_POINT('Ctrl Pts',(34.9791738167096,-5.47688847173027,-1.54358125097877));
#66152=CARTESIAN_POINT('Ctrl Pts',(35.057423795889,-4.57871148724481,-3.58182440187771));
#66153=CARTESIAN_POINT('Ctrl Pts',(35.1579937058468,-2.31400597626052,-5.33286426520916));
#66154=CARTESIAN_POINT('Ctrl Pts',(35.2585636158045,0.511843992004246,-5.79068913490987));
#66155=CARTESIAN_POINT('Ctrl Pts',(35.3591335257624,3.21357223281796,-4.84427687418623));
#66156=CARTESIAN_POINT('Ctrl Pts',(35.4597034357202,5.13601197350847,-2.72313164156489));
#66157=CARTESIAN_POINT('Ctrl Pts',(35.560273345678,5.81297323184956,0.0583706699861391));
#66158=CARTESIAN_POINT('Ctrl Pts',(35.6608432556358,5.08029348544121,2.82571814431267));
#66159=CARTESIAN_POINT('Ctrl Pts',(35.7614131655936,3.11564694207568,4.9078314011026));
#66160=CARTESIAN_POINT('Ctrl Pts',(35.8619830755514,0.395458697295045,5.79979976792715));
#66161=CARTESIAN_POINT('Ctrl Pts',(35.9625529855092,-2.42062794115745,5.28532168366335));
#66162=CARTESIAN_POINT('Ctrl Pts',(36.063122895467,-4.64971438762522,3.48915764086767));
#66163=CARTESIAN_POINT('Ctrl Pts',(36.1400198230669,-5.4919606905701,1.46883814539051));
#66164=CARTESIAN_POINT('Ctrl Pts',(36.1833934473475,-5.57791288830659,0.271981626644002));
#66165=CARTESIAN_POINT('Ctrl Pts',(36.1932437683088,-5.57766442098412,0.00013542246225573));
#66166=CARTESIAN_POINT('Ctrl Pts',(35.1930928170571,-5.57744951564134,8.38323760707013E-5));
#66167=CARTESIAN_POINT('Ctrl Pts',(35.2133611841706,-5.57714996681278,-0.559338285009587));
#66168=CARTESIAN_POINT('Ctrl Pts',(35.2671528546033,-5.35512132667755,-2.04426121989497));
#66169=CARTESIAN_POINT('Ctrl Pts',(35.3544678283553,-4.05687069717986,-4.16363604802468));
#66170=CARTESIAN_POINT('Ctrl Pts',(35.4550377383131,-1.57775019122715,-5.59506651686378));
#66171=CARTESIAN_POINT('Ctrl Pts',(35.5556076482709,1.28397337792556,-5.66969817175709));
#66172=CARTESIAN_POINT('Ctrl Pts',(35.6561775582287,3.83433450821241,-4.36943290063812));
#66173=CARTESIAN_POINT('Ctrl Pts',(35.7567474681865,5.45487282096287,-2.00958391244754));
#66174=CARTESIAN_POINT('Ctrl Pts',(35.8573173781443,5.75260917034078,0.837587444604104));
#66175=CARTESIAN_POINT('Ctrl Pts',(35.9578872881021,4.65534274792201,3.48164456735854));
#66176=CARTESIAN_POINT('Ctrl Pts',(36.05845719806,2.4291597165847,5.28140587962803));
#66177=CARTESIAN_POINT('Ctrl Pts',(36.1590271080177,-0.386092454934063,
5.80043081247336));
#66178=CARTESIAN_POINT('Ctrl Pts',(36.2595970179756,-3.10771753849076,4.91285626647109));
#66179=CARTESIAN_POINT('Ctrl Pts',(36.3601669279333,-5.07572379417585,2.83391830497715));
#66180=CARTESIAN_POINT('Ctrl Pts',(36.4279988609605,-5.57291174024723,0.968210876530677));
#66181=CARTESIAN_POINT('Ctrl Pts',(36.4623074906685,-5.57831147870766,0.0216886821586606));
#66182=CARTESIAN_POINT('Ctrl Pts',(36.4630928170571,-5.57830649769973,2.26809192474704E-5));
#66183=CARTESIAN_POINT('Origin',(16.5082437683087,0.,0.));
#66184=CARTESIAN_POINT('',(33.6532437683088,-5.57829460971474,3.62717574107884E-5));
#66185=CARTESIAN_POINT('',(33.9230928170571,-5.57783438402505,-0.000142925532344573));
#66186=CARTESIAN_POINT('',(16.5082437683087,-5.57784,5.11151866531329E-13));
#66187=CARTESIAN_POINT('Ctrl Pts',(33.6532437683088,-5.57829460971474,3.62717574106273E-5));
#66188=CARTESIAN_POINT('Ctrl Pts',(33.6855008343517,-5.57797904703139,-0.889894308257694));
#66189=CARTESIAN_POINT('Ctrl Pts',(33.7512812037139,-5.13567938972669,-2.70499181735756));
#66190=CARTESIAN_POINT('Ctrl Pts',(33.8505848763954,-3.2558486083957,-4.81596457301359));
#66191=CARTESIAN_POINT('Ctrl Pts',(33.9511547863532,-0.562507314318525,
-5.78598742226877));
#66192=CARTESIAN_POINT('Ctrl Pts',(34.051724696311,2.26724151925849,-5.35291330236766));
#66193=CARTESIAN_POINT('Ctrl Pts',(34.1522946062688,4.54718623612184,-3.62176231458366));
#66194=CARTESIAN_POINT('Ctrl Pts',(34.2528645162266,5.72444220507391,-1.01233708322999));
#66195=CARTESIAN_POINT('Ctrl Pts',(34.3534344261844,5.5135258670596,1.84257901935812));
#66196=CARTESIAN_POINT('Ctrl Pts',(34.4540043361422,3.96558425248456,4.25067129589676));
#66197=CARTESIAN_POINT('Ctrl Pts',(34.5545742461,1.45599187037064,5.62797944228023));
#66198=CARTESIAN_POINT('Ctrl Pts',(34.6551441560578,-1.40667728694861,5.64050741863682));
#66199=CARTESIAN_POINT('Ctrl Pts',(34.7557140660156,-3.92822841309095,4.28521720148455));
#66200=CARTESIAN_POINT('Ctrl Pts',(34.8450806034326,-5.3224072856642,2.15750467293659));
#66201=CARTESIAN_POINT('Ctrl Pts',(34.9009238375303,-5.57708000614775,0.615889852290342));
#66202=CARTESIAN_POINT('Ctrl Pts',(34.9232437683088,-5.57756608151389,-0.000120065769840146));
#66203=CARTESIAN_POINT('Ctrl Pts',(33.9230928170571,-5.57783438402505,-0.000142925532344608));
#66204=CARTESIAN_POINT('Ctrl Pts',(33.9308915743534,-5.57805340367234,-0.215351841616216));
#66205=CARTESIAN_POINT('Ctrl Pts',(33.972213634969,-5.51331437958064,-1.35551481940617));
#66206=CARTESIAN_POINT('Ctrl Pts',(34.0470589989039,-4.75378622921922,-3.34597989846517));
#66207=CARTESIAN_POINT('Ctrl Pts',(34.1476289088617,-2.58041721203297,-5.20917575110413));
#66208=CARTESIAN_POINT('Ctrl Pts',(34.2481988188195,0.218700757774141,-5.80915096830823));
#66209=CARTESIAN_POINT('Ctrl Pts',(34.3487687287773,2.96478398208491,-5.00041207638131));
#66210=CARTESIAN_POINT('Ctrl Pts',(34.4493386387351,4.99190964291116,-2.97907756043006));
#66211=CARTESIAN_POINT('Ctrl Pts',(34.5499085486929,5.80850151251044,-0.235319300549913));
#66212=CARTESIAN_POINT('Ctrl Pts',(34.6504784586507,5.21653676545061,2.56550368714399));
#66213=CARTESIAN_POINT('Ctrl Pts',(34.7510483686085,3.35956634331347,4.74419423916461));
#66214=CARTESIAN_POINT('Ctrl Pts',(34.8516182785663,0.687903974933855,5.7724217721263));
#66215=CARTESIAN_POINT('Ctrl Pts',(34.952188188524,-2.15057451519974,5.40084199441352));
#66216=CARTESIAN_POINT('Ctrl Pts',(35.0527580984819,-4.46754053667362,3.71956268225518));
#66217=CARTESIAN_POINT('Ctrl Pts',(35.1330596413262,-5.45251987727794,1.65691221806805));
#66218=CARTESIAN_POINT('Ctrl Pts',(35.1798378808513,-5.57764541206412,0.365930002250153));
#66219=CARTESIAN_POINT('Ctrl Pts',(35.1930928170571,-5.57744951564134,8.38323760707013E-5));
#66220=CARTESIAN_POINT('Origin',(16.5082437683087,0.,0.));
#66221=CARTESIAN_POINT('',(32.3832437683088,-5.57742896989317,7.35428515294205E-5));
#66222=CARTESIAN_POINT('',(32.6530928170571,-5.57809874629883,0.00011458596757101));
#66223=CARTESIAN_POINT('',(16.5082437683087,-5.57784,5.11151866531329E-13));
#66224=CARTESIAN_POINT('Ctrl Pts',(32.3832437683088,-5.57742896989317,7.35428515291625E-5));
#66225=CARTESIAN_POINT('Ctrl Pts',(32.4030312245346,-5.57717363126457,-0.546080832034013));
#66226=CARTESIAN_POINT('Ctrl Pts',(32.4563419840797,-5.36250926464525,-2.01770966254631));
#66227=CARTESIAN_POINT('Ctrl Pts',(32.5431760469439,-4.08648613702948,-4.13457325260782));
#66228=CARTESIAN_POINT('Ctrl Pts',(32.6437459569018,-1.61764590787947,-5.58366247601294));
#66229=CARTESIAN_POINT('Ctrl Pts',(32.7443158668595,1.24347206141533,-5.67871835556173));
#66230=CARTESIAN_POINT('Ctrl Pts',(32.8448857768174,3.80304912623336,-4.39668992229039));
#66231=CARTESIAN_POINT('Ctrl Pts',(32.9454556867751,5.44039005171353,-2.04846796766039));
#66232=CARTESIAN_POINT('Ctrl Pts',(33.046025596733,5.75844107289692,0.796505705747263));
#66233=CARTESIAN_POINT('Ctrl Pts',(33.1465955066908,4.68007509093404,3.44832743116613));
#66234=CARTESIAN_POINT('Ctrl Pts',(33.2471654166486,2.46679492816254,5.26393272294638));
#66235=CARTESIAN_POINT('Ctrl Pts',(33.3477353266064,-0.344680881200578,
5.80303886075641));
#66236=CARTESIAN_POINT('Ctrl Pts',(33.4483052365642,-3.07257187358376,4.93491307025526));
#66237=CARTESIAN_POINT('Ctrl Pts',(33.548875146522,-5.05536683158087,2.87007510833188));
#66238=CARTESIAN_POINT('Ctrl Pts',(33.6171879904368,-5.56947823032715,0.99476209986866));
#66239=CARTESIAN_POINT('Ctrl Pts',(33.6519775310325,-5.57830699699238,0.034970114539885));
#66240=CARTESIAN_POINT('Ctrl Pts',(33.6532437683088,-5.57829460971474,3.62717574106273E-5));
#66241=CARTESIAN_POINT('Ctrl Pts',(32.6530928170571,-5.57809874629883,0.000114585967571079));
#66242=CARTESIAN_POINT('Ctrl Pts',(32.6819452678556,-5.57736761763102,-0.795968132793007));
#66243=CARTESIAN_POINT('Ctrl Pts',(32.7443210219733,-5.20504218182127,-2.51767136306138));
#66244=CARTESIAN_POINT('Ctrl Pts',(32.8402200794103,-3.49494881941665,-4.64536303680407));
#66245=CARTESIAN_POINT('Ctrl Pts',(32.940789989368,-0.854041693849599,-5.75018936898723));
#66246=CARTESIAN_POINT('Ctrl Pts',(33.0413598993259,1.99396980729241,-5.46059972911893));
#66247=CARTESIAN_POINT('Ctrl Pts',(33.1419298092837,4.35844534663238,-3.8468193555801));
#66248=CARTESIAN_POINT('Ctrl Pts',(33.2424997192414,5.66600164128877,-1.30018859976555));
#66249=CARTESIAN_POINT('Ctrl Pts',(33.3430696291993,5.59955741538933,1.56173677225253));
#66250=CARTESIAN_POINT('Ctrl Pts',(33.443639539157,4.17522533651758,4.04494232138717));
#66251=CARTESIAN_POINT('Ctrl Pts',(33.5442094491149,1.73840470769403,5.54725283958776));
#66252=CARTESIAN_POINT('Ctrl Pts',(33.6447793590727,-1.1199775662767,5.70435931942268));
#66253=CARTESIAN_POINT('Ctrl Pts',(33.7453492690304,-3.70676624453413,4.47816357477366));
#66254=CARTESIAN_POINT('Ctrl Pts',(33.838120421692,-5.263777944182,2.34531388575583));
#66255=CARTESIAN_POINT('Ctrl Pts',(33.8973682710342,-5.57711193802725,0.709733206778817));
#66256=CARTESIAN_POINT('Ctrl Pts',(33.9230928170571,-5.57783438402505,-0.000142925532344608));
#66257=CARTESIAN_POINT('Origin',(16.5082437683087,0.,0.));
#66258=CARTESIAN_POINT('',(31.1132437683088,-5.57787607033853,-0.000141715837242922));
#66259=CARTESIAN_POINT('',(31.3830928170571,-5.57736868831649,-9.6464866874979E-6));
#66260=CARTESIAN_POINT('',(16.5082437683087,-5.57784,5.11151866531329E-13));
#66261=CARTESIAN_POINT('Ctrl Pts',(31.1132437683088,-5.57787607033853,-0.000141715837243019));
#66262=CARTESIAN_POINT('Ctrl Pts',(31.1205616147174,-5.57808293770935,-0.202075414452116));
#66263=CARTESIAN_POINT('Ctrl Pts',(31.1614027644454,-5.51806033372383,-1.3289519298113));
#66264=CARTESIAN_POINT('Ctrl Pts',(31.2357672174925,-4.7775477306356,-3.31196355819516));
#66265=CARTESIAN_POINT('Ctrl Pts',(31.3363371274504,-2.61753301334895,-5.19062480375363));
#66266=CARTESIAN_POINT('Ctrl Pts',(31.4369070374081,0.177231206427325,-5.81056400264058));
#66267=CARTESIAN_POINT('Ctrl Pts',(31.537476947366,2.92901701121071,-5.02144643278732));
#66268=CARTESIAN_POINT('Ctrl Pts',(31.6380468573237,4.97051871215735,-3.01463242558821));
#66269=CARTESIAN_POINT('Ctrl Pts',(31.7386167672815,5.80667390417087,-0.276772650265986));
#66270=CARTESIAN_POINT('Ctrl Pts',(31.8391866772394,5.23471567297435,2.52820425449188));
#66271=CARTESIAN_POINT('Ctrl Pts',(31.9397565871971,3.39334339727493,4.72009380388618));
#66272=CARTESIAN_POINT('Ctrl Pts',(32.040326497155,0.729088268823663,5.76736466903021));
#66273=CARTESIAN_POINT('Ctrl Pts',(32.1408964071127,-2.11197013719727,5.4160545666473));
#66274=CARTESIAN_POINT('Ctrl Pts',(32.2414663170706,-4.44087760299231,3.75135589414753));
#66275=CARTESIAN_POINT('Ctrl Pts',(32.3222487708025,-5.44654131005962,1.68347805483491));
#66276=CARTESIAN_POINT('Ctrl Pts',(32.3695079212153,-5.57760621816194,0.379197210758078));
#66277=CARTESIAN_POINT('Ctrl Pts',(32.3832437683088,-5.57742896989317,7.35428515291625E-5));
#66278=CARTESIAN_POINT('Ctrl Pts',(31.3830928170571,-5.57736868831649,-9.64648668739382E-6));
#66279=CARTESIAN_POINT('Ctrl Pts',(31.3994756580384,-5.57739604835976,-0.452207087798499));
#66280=CARTESIAN_POINT('Ctrl Pts',(31.449381802339,-5.4118049609828,-1.82969150179622));
#66281=CARTESIAN_POINT('Ctrl Pts',(31.5328112499588,-4.29010873851205,-3.92288567330096));
#66282=CARTESIAN_POINT('Ctrl Pts',(31.6333811599166,-1.89761393322384,-5.49482723609051));
#66283=CARTESIAN_POINT('Ctrl Pts',(31.7339510698744,0.955050617350668,-5.73427792423296));
#66284=CARTESIAN_POINT('Ctrl Pts',(31.8345209798323,3.57611621535257,-4.58317115197979));
#66285=CARTESIAN_POINT('Ctrl Pts',(31.93509088979,5.32997670955485,-2.32064932069671));
#66286=CARTESIAN_POINT('Ctrl Pts',(32.0356607997479,5.79132243988692,0.504627973173819));
#66287=CARTESIAN_POINT('Ctrl Pts',(32.1362307097056,4.84827746388286,3.20753341794796));
#66288=CARTESIAN_POINT('Ctrl Pts',(32.2368006196635,2.72952937642347,5.13261477000649));
#66289=CARTESIAN_POINT('Ctrl Pts',(32.3373705296212,-0.051127235161469,
5.8130414586404));
#66290=CARTESIAN_POINT('Ctrl Pts',(32.4379404395791,-2.81938553623152,5.0838105975868));
#66291=CARTESIAN_POINT('Ctrl Pts',(32.5385103495368,-4.90394527177332,3.12176004290838));
#66292=CARTESIAN_POINT('Ctrl Pts',(32.6102278086962,-5.54243391615643,1.18275932950451));
#66293=CARTESIAN_POINT('Ctrl Pts',(32.6484219645363,-5.57821710692632,0.128990465513416));
#66294=CARTESIAN_POINT('Ctrl Pts',(32.6530928170571,-5.57809874629883,0.000114585967571079));
#66295=CARTESIAN_POINT('Origin',(16.5082437683087,0.,0.));
#66296=CARTESIAN_POINT('',(29.8432437683088,-5.5780605344387,0.000122021361445272));
#66297=CARTESIAN_POINT('',(30.1130928170571,-5.57815516189836,-0.00010078891834242));
#66298=CARTESIAN_POINT('',(16.5082437683087,-5.57784,5.11151866531329E-13));
#66299=CARTESIAN_POINT('Ctrl Pts',(29.8432437683088,-5.5780605344387,0.000122021361445238));
#66300=CARTESIAN_POINT('Ctrl Pts',(29.8716153082195,-5.57731124588235,-0.782707136893296));
#66301=CARTESIAN_POINT('Ctrl Pts',(29.9335101514496,-5.21438063601642,-2.491185998848));
#66302=CARTESIAN_POINT('Ctrl Pts',(30.0289282979989,-3.52801699702796,-4.62029879964445));
#66303=CARTESIAN_POINT('Ctrl Pts',(30.1294982079567,-0.895063067200426,
-5.74394699096779));
#66304=CARTESIAN_POINT('Ctrl Pts',(30.2300681179145,1.95494288592725,-5.47469298153573));
#66305=CARTESIAN_POINT('Ctrl Pts',(30.3306380278723,4.33087687208847,-3.87783063685398));
#66306=CARTESIAN_POINT('Ctrl Pts',(30.4312079378301,5.65657694491125,-1.34059770088297));
#66307=CARTESIAN_POINT('Ctrl Pts',(30.5317778477879,5.61056197793671,1.52172902352723));
#66308=CARTESIAN_POINT('Ctrl Pts',(30.6323477577457,4.20399056104516,4.01503776968005));
#66309=CARTESIAN_POINT('Ctrl Pts',(30.7329176677035,1.77795505201581,5.53470331294511));
#66310=CARTESIAN_POINT('Ctrl Pts',(30.8334875776613,-1.07923302661269,5.71220806725234));
#66311=CARTESIAN_POINT('Ctrl Pts',(30.9340574876192,-3.67470802532234,4.50450728248337));
#66312=CARTESIAN_POINT('Ctrl Pts',(31.0273095511682,-5.25505371512234,2.37182694926743));
#66313=CARTESIAN_POINT('Ctrl Pts',(31.0870383113982,-5.57713527124692,0.722989727807046));
#66314=CARTESIAN_POINT('Ctrl Pts',(31.1132437683088,-5.57787607033853,-0.000141715837243019));
#66315=CARTESIAN_POINT('Ctrl Pts',(30.1130928170571,-5.57815516189836,-0.000100788918342126));
#66316=CARTESIAN_POINT('Ctrl Pts',(30.1170060482213,-5.57824565243898,-0.108069590543255));
#66317=CARTESIAN_POINT('Ctrl Pts',(30.1544425827047,-5.54886883866117,-1.1409207127355));
#66318=CARTESIAN_POINT('Ctrl Pts',(30.2254024205074,-4.93873789291885,-3.06642022871864));
#66319=CARTESIAN_POINT('Ctrl Pts',(30.3259723304652,-2.87637223950989,-5.05178658830954));
#66320=CARTESIAN_POINT('Ctrl Pts',(30.426542240423,-0.116488794083507,-5.81209904895815));
#66321=CARTESIAN_POINT('Ctrl Pts',(30.5271121503808,2.67164308363124,-5.16298249345597));
#66322=CARTESIAN_POINT('Ctrl Pts',(30.6276820603386,4.81190381339239,-3.26184712773408));
#66323=CARTESIAN_POINT('Ctrl Pts',(30.7282519702964,5.78528201063068,-0.569716641428254));
#66324=CARTESIAN_POINT('Ctrl Pts',(30.8288218802542,5.35573430042772,2.26056963999551));
#66325=CARTESIAN_POINT('Ctrl Pts',(30.929391790212,3.62742563274069,4.54266972968354));
#66326=CARTESIAN_POINT('Ctrl Pts',(31.0299617001698,1.01946937170607,5.72317632038368));
#66327=CARTESIAN_POINT('Ctrl Pts',(31.1305316101276,-1.8357073343788,5.51581758006511));
#66328=CARTESIAN_POINT('Ctrl Pts',(31.2311015200854,-4.24572659210633,3.97087782475468));
#66329=CARTESIAN_POINT('Ctrl Pts',(31.3152885890619,-5.40128803627012,1.87153638998712));
#66330=CARTESIAN_POINT('Ctrl Pts',(31.3659523547191,-5.57734006301324,0.473099579255527));
#66331=CARTESIAN_POINT('Ctrl Pts',(31.3830928170571,-5.57736868831649,-9.64648668739382E-6));
#66332=CARTESIAN_POINT('Origin',(16.5082437683087,0.,0.));
#66333=CARTESIAN_POINT('',(28.5732437683088,-5.5773727299529,-2.18264568977285E-5));
#66334=CARTESIAN_POINT('',(28.8430928170571,-5.57776963474036,0.000142506048256413));
#66335=CARTESIAN_POINT('',(16.5082437683087,-5.57784,5.11151866531329E-13));
#66336=CARTESIAN_POINT('Ctrl Pts',(28.5732437683088,-5.5773727299529,-2.18264568977583E-5));
#66337=CARTESIAN_POINT('Ctrl Pts',(28.5891456984024,-5.57743287143306,-0.438944304786934));
#66338=CARTESIAN_POINT('Ctrl Pts',(28.6385709318153,-5.41834739991601,-1.80312865329392));
#66339=CARTESIAN_POINT('Ctrl Pts',(28.7215194685475,-4.31799983261996,-3.89216422762556));
#66340=CARTESIAN_POINT('Ctrl Pts',(28.8220893785053,-1.93678602348512,-5.48114265719722));
#66341=CARTESIAN_POINT('Ctrl Pts',(28.9226592884631,0.91409672910392,-5.74094871072331));
#66342=CARTESIAN_POINT('Ctrl Pts',(29.0232291984209,3.54331181176593,-4.60857964387231));
#66343=CARTESIAN_POINT('Ctrl Pts',(29.1237991083787,5.31327683025914,-2.35863398057979));
#66344=CARTESIAN_POINT('Ctrl Pts',(29.2243690183365,5.79477679123556,0.463278392623556));
#66345=CARTESIAN_POINT('Ctrl Pts',(29.3249389282943,4.87104836864741,3.17284615441902));
#66346=CARTESIAN_POINT('Ctrl Pts',(29.4255088382521,2.76609490980042,5.11300145504481));
#66347=CARTESIAN_POINT('Ctrl Pts',(29.5260787482099,-0.00963418353934693,
5.81325830424054));
#66348=CARTESIAN_POINT('Ctrl Pts',(29.6266486581677,-2.78302699566422,5.10380501887743));
#66349=CARTESIAN_POINT('Ctrl Pts',(29.7272185681255,-4.88153815704996,3.15668340993825));
#66350=CARTESIAN_POINT('Ctrl Pts',(29.7994169381725,-5.53822470938508,1.20931809855868));
#66351=CARTESIAN_POINT('Ctrl Pts',(29.8380920049003,-5.57819659181801,0.142269773132362));
#66352=CARTESIAN_POINT('Ctrl Pts',(29.8432437683088,-5.5780605344387,0.000122021361445238));
#66353=CARTESIAN_POINT('Ctrl Pts',(28.8430928170571,-5.57776963474036,0.000142506048256483));
#66354=CARTESIAN_POINT('Ctrl Pts',(28.8680597417234,-5.57708554036205,-0.688849856278956));
#66355=CARTESIAN_POINT('Ctrl Pts',(28.926549969709,-5.27729829006175,-2.30353694477276));
#66356=CARTESIAN_POINT('Ctrl Pts',(29.0185635010138,-3.75688664349095,-4.43619969591165));
#66357=CARTESIAN_POINT('Ctrl Pts',(29.1191334109716,-1.18404947371506,-5.69140508467306));
#66358=CARTESIAN_POINT('Ctrl Pts',(29.2197033209294,1.67591867417301,-5.56644963972599));
#66359=CARTESIAN_POINT('Ctrl Pts',(29.3202732308872,4.12947798625297,-4.09163494890484));
#66360=CARTESIAN_POINT('Ctrl Pts',(29.420843140845,5.58164244143966,-1.62460230517097));
#66361=CARTESIAN_POINT('Ctrl Pts',(29.5214130508028,5.68026340941513,1.2363949990626));
#66362=CARTESIAN_POINT('Ctrl Pts',(29.6219829607606,4.40142539034105,3.79756758034778));
#66363=CARTESIAN_POINT('Ctrl Pts',(29.7225528707184,2.05524550298248,5.43783329245368));
#66364=CARTESIAN_POINT('Ctrl Pts',(29.8231227806762,-0.789329649635071,
5.75942911218241));
#66365=CARTESIAN_POINT('Ctrl Pts',(29.923692690634,-3.44249304169372,4.68436833008867));
#66366=CARTESIAN_POINT('Ctrl Pts',(30.0203493694276,-5.19010136525037,2.5593841261018));
#66367=CARTESIAN_POINT('Ctrl Pts',(30.083482744902,-5.57747045115051,0.816861938937919));
#66368=CARTESIAN_POINT('Ctrl Pts',(30.1130928170571,-5.57815516189836,-0.000100788918342126));
#66369=CARTESIAN_POINT('Origin',(16.5082437683087,0.,0.));
#66370=CARTESIAN_POINT('',(27.3032437683088,-5.57818796811726,-9.07968746462347E-5));
#66371=CARTESIAN_POINT('',(27.5730928170571,-5.57748734871596,-9.87876261981935E-5));
#66372=CARTESIAN_POINT('',(16.5082437683087,-5.57784,5.11151866531329E-13));
#66373=CARTESIAN_POINT('Ctrl Pts',(27.3032437683088,-5.57818796811726,-9.07968746462033E-5));
#66374=CARTESIAN_POINT('Ctrl Pts',(27.3066760885853,-5.57826130241348,-0.0947893148921463));
#66375=CARTESIAN_POINT('Ctrl Pts',(27.343631712181,-5.55282928699094,-1.11436421216366));
#66376=CARTESIAN_POINT('Ctrl Pts',(27.4141106390961,-4.96049926954682,-3.03109088054774));
#66377=CARTESIAN_POINT('Ctrl Pts',(27.5146805490538,-2.91235710475748,-5.03112721203537));
#66378=CARTESIAN_POINT('Ctrl Pts',(27.6152504590117,-0.157970849104978,
-5.81111952554301));
#66379=CARTESIAN_POINT('Ctrl Pts',(27.7158203689695,2.63472320146966,-5.18192035648482));
#66380=CARTESIAN_POINT('Ctrl Pts',(27.8163902789273,4.78849914373318,-3.2961099617247));
#66381=CARTESIAN_POINT('Ctrl Pts',(27.9169601888851,5.7810681657188,-0.610995738632328));
#66382=CARTESIAN_POINT('Ctrl Pts',(28.0175300988429,5.37173313402688,2.22228442511572));
#66383=CARTESIAN_POINT('Ctrl Pts',(28.1181000088007,3.65975744147539,4.51666252877937));
#66384=CARTESIAN_POINT('Ctrl Pts',(28.2186699187585,1.06029371979028,5.71575385728667));
#66385=CARTESIAN_POINT('Ctrl Pts',(28.3192398287163,-1.79629031621274,5.52877979568679));
#66386=CARTESIAN_POINT('Ctrl Pts',(28.4198097386741,-4.21727549683238,4.00108139296507));
#66387=CARTESIAN_POINT('Ctrl Pts',(28.5044777185383,-5.39447844165815,1.89809661666281));
#66388=CARTESIAN_POINT('Ctrl Pts',(28.5556223950832,-5.57730608549767,0.486360440489903));
#66389=CARTESIAN_POINT('Ctrl Pts',(28.5732437683088,-5.5773727299529,-2.18264568977583E-5));
#66390=CARTESIAN_POINT('Ctrl Pts',(27.5730928170571,-5.57748734871596,-9.87876261983323E-5));
#66391=CARTESIAN_POINT('Ctrl Pts',(27.5855901319063,-5.57770694637395,-0.345027339152668));
#66392=CARTESIAN_POINT('Ctrl Pts',(27.6316107500747,-5.46173274549469,-1.61506032531023));
#66393=CARTESIAN_POINT('Ctrl Pts',(27.7111546715624,-4.50908274454013,-3.66909223063931));
#66394=CARTESIAN_POINT('Ctrl Pts',(27.8117245815202,-2.21116836378188,-5.3763183928277));
#66395=CARTESIAN_POINT('Ctrl Pts',(27.912294491478,0.622952441756332,-5.77979197284445));
#66396=CARTESIAN_POINT('Ctrl Pts',(28.0128644014358,3.30600781642397,-4.78167097485711));
#66397=CARTESIAN_POINT('Ctrl Pts',(28.1134343113936,5.18735914151516,-2.62399888166641));
#66398=CARTESIAN_POINT('Ctrl Pts',(28.2140042213514,5.8107803402164,0.169990681514914));
#66399=CARTESIAN_POINT('Ctrl Pts',(28.3145741313092,5.02509230850153,2.92275765076171));
#66400=CARTESIAN_POINT('Ctrl Pts',(28.415144041267,3.02082371771862,4.96675840569238));
#66401=CARTESIAN_POINT('Ctrl Pts',(28.5157139512248,0.284007975800641,5.80632452277075));
#66402=CARTESIAN_POINT('Ctrl Pts',(28.6162838611826,-2.5216794557668,5.23786194132788));
#66403=CARTESIAN_POINT('Ctrl Pts',(28.7168537711404,-4.71586179004478,3.39922234801476));
#66404=CARTESIAN_POINT('Ctrl Pts',(28.7924567564319,-5.50563811108249,1.39736289418203));
#66405=CARTESIAN_POINT('Ctrl Pts',(28.8345364384041,-5.57800407973563,0.236266082334538));
#66406=CARTESIAN_POINT('Ctrl Pts',(28.8430928170571,-5.57776963474036,0.000142506048256483));
#66407=CARTESIAN_POINT('Origin',(16.5082437683087,0.,0.));
#66408=CARTESIAN_POINT('',(26.0332437683088,-5.57772954743397,0.00014079117121212));
#66409=CARTESIAN_POINT('',(26.3030928170571,-5.57831427568592,-8.04374804677406E-7));
#66410=CARTESIAN_POINT('',(16.5082437683087,-5.57784,5.11151866531329E-13));
#66411=CARTESIAN_POINT('Ctrl Pts',(26.0332437683088,-5.57772954743397,0.000140791171212053));
#66412=CARTESIAN_POINT('Ctrl Pts',(26.0577297820874,-5.57707497798415,-0.675594212321096));
#66413=CARTESIAN_POINT('Ctrl Pts',(26.1157390991853,-5.28573910446548,-2.27701333570043));
#66414=CARTESIAN_POINT('Ctrl Pts',(26.2072717196025,-3.78845520303171,-4.40927115336947));
#66415=CARTESIAN_POINT('Ctrl Pts',(26.3078416295602,-1.22464285560959,-5.68280870745432));
#66416=CARTESIAN_POINT('Ctrl Pts',(26.408411539518,1.63614433009017,-5.57827004190617));
#66417=CARTESIAN_POINT('Ctrl Pts',(26.5089814494759,4.100167924183,-4.12100569313063));
#66418=CARTESIAN_POINT('Ctrl Pts',(26.6095513594336,5.56990432620359,-1.66440101125078));
#66419=CARTESIAN_POINT('Ctrl Pts',(26.7101212693915,5.6889437238532,1.19581948309323));
#66420=CARTESIAN_POINT('Ctrl Pts',(26.8106911793493,4.42841916567433,3.76605478218288));
#66421=CARTESIAN_POINT('Ctrl Pts',(26.911261089307,2.09400677192963,5.42302503852111));
#66422=CARTESIAN_POINT('Ctrl Pts',(27.0118309992649,-0.748200461426902,
5.76491639131348));
#66423=CARTESIAN_POINT('Ctrl Pts',(27.1124009092227,-3.40896972695984,4.70882048181766));
#66424=CARTESIAN_POINT('Ctrl Pts',(27.209538498904,-5.18047142072391,2.58585388687039));
#66425=CARTESIAN_POINT('Ctrl Pts',(27.273152785266,-5.57754504994926,0.830126452765981));
#66426=CARTESIAN_POINT('Ctrl Pts',(27.3032437683088,-5.57818796811726,-9.07968746462033E-5));
#66427=CARTESIAN_POINT('Ctrl Pts',(26.3030928170571,-5.57831427096578,-8.04366799073348E-7));
#66428=CARTESIAN_POINT('Ctrl Pts',(26.3031205220891,-5.57831427759844,-0.000765142388995596));
#66429=CARTESIAN_POINT('Ctrl Pts',(26.3366715304404,-5.57812799481241,-0.926384403945683));
#66430=CARTESIAN_POINT('Ctrl Pts',(26.403745842111,-5.10726891650053,-2.77666512359608));
#66431=CARTESIAN_POINT('Ctrl Pts',(26.5043157520687,-3.16276371564756,-4.87760091366961));
#66432=CARTESIAN_POINT('Ctrl Pts',(26.6048856620266,-0.451291036347756,
-5.79572268095701));
#66433=CARTESIAN_POINT('Ctrl Pts',(26.7054555719843,2.36961933078211,-5.30838668723663));
#66434=CARTESIAN_POINT('Ctrl Pts',(26.8060254819422,4.61589905003359,-3.53377149147286));
#66435=CARTESIAN_POINT('Ctrl Pts',(26.9065953918999,5.74282722315021,-0.902219750998773));
#66436=CARTESIAN_POINT('Ctrl Pts',(27.0071653018578,5.47712473824325,1.94811950243589));
#66437=CARTESIAN_POINT('Ctrl Pts',(27.1077352118156,3.88322421917838,4.32604145352698));
#66438=CARTESIAN_POINT('Ctrl Pts',(27.2083051217733,1.34764516975351,5.65490207611833));
#66439=CARTESIAN_POINT('Ctrl Pts',(27.3088750317312,-1.51473667324498,5.61245381315286));
#66440=CARTESIAN_POINT('Ctrl Pts',(27.409444941689,-4.00979617691032,4.20899033185902));
#66441=CARTESIAN_POINT('Ctrl Pts',(27.4975175367976,-5.3432668877154,2.08608595628941));
#66442=CARTESIAN_POINT('Ctrl Pts',(27.552066828587,-5.57711788872549,0.580222972283408));
#66443=CARTESIAN_POINT('Ctrl Pts',(27.5730928170571,-5.57748734871596,-9.87876261983323E-5));
#66444=CARTESIAN_POINT('Origin',(16.5082437683087,0.,0.));
#66445=CARTESIAN_POINT('',(24.7632437683088,-5.57751463566409,-0.000107372944178986));
#66446=CARTESIAN_POINT('',(25.0330928170571,-5.57749036758178,9.98147628876456E-5));
#66447=CARTESIAN_POINT('',(16.5082437683087,-5.57784,5.11151866531329E-13));
#66448=CARTESIAN_POINT('Ctrl Pts',(24.7632437683088,-5.57751463566409,-0.000107372944178757));
#66449=CARTESIAN_POINT('Ctrl Pts',(24.7752601722703,-5.57774565600241,-0.331758031377505));
#66450=CARTESIAN_POINT('Ctrl Pts',(24.820799879551,-5.46745062976281,-1.58849413899114));
#66451=CARTESIAN_POINT('Ctrl Pts',(24.899862890151,-4.53515675876486,-3.63681427938567));
#66452=CARTESIAN_POINT('Ctrl Pts',(25.0004328001089,-2.24948658571366,-5.36039877527861));
#66453=CARTESIAN_POINT('Ctrl Pts',(25.1010027100666,0.581682147950543,-5.78409118255149));
#66454=CARTESIAN_POINT('Ctrl Pts',(25.2015726200244,3.27179346146541,-4.80514645716718));
#66455=CARTESIAN_POINT('Ctrl Pts',(25.3021425299822,5.16849767702856,-2.66095785232772));
#66456=CARTESIAN_POINT('Ctrl Pts',(25.40271243994,5.81184565510331,0.128510741072388));
#66457=CARTESIAN_POINT('Ctrl Pts',(25.5032823498978,5.04582606481892,2.88681559038817));
#66458=CARTESIAN_POINT('Ctrl Pts',(25.6038522598556,3.05619799740772,4.94507014408847));
#66459=CARTESIAN_POINT('Ctrl Pts',(25.7044221698135,0.325444546488037,5.80414944470552));
#66460=CARTESIAN_POINT('Ctrl Pts',(25.8049920797712,-2.484228926803,5.25572750135977));
#66461=CARTESIAN_POINT('Ctrl Pts',(25.9055619897291,-4.69147902383981,3.43279616321523));
#66462=CARTESIAN_POINT('Ctrl Pts',(25.9816458859082,-5.50063843152049,1.42392723963565));
#66463=CARTESIAN_POINT('Ctrl Pts',(26.0242064787681,-5.57797113570129,0.249540833763626));
#66464=CARTESIAN_POINT('Ctrl Pts',(26.0332437683088,-5.57772954743397,0.000140791171212053));
#66465=CARTESIAN_POINT('Ctrl Pts',(25.0330928170571,-5.57749036758178,9.9814762887715E-5));
#66466=CARTESIAN_POINT('Ctrl Pts',(25.0541742155912,-5.57711581138055,-0.58175037250084));
#66467=CARTESIAN_POINT('Ctrl Pts',(25.1087789174447,-5.34238951116529,-2.08914466751173));
#66468=CARTESIAN_POINT('Ctrl Pts',(25.1969069226173,-4.00633332410426,-4.21228658690491));
#66469=CARTESIAN_POINT('Ctrl Pts',(25.2974768325751,-1.51012044812308,-5.61369764292733));
#66470=CARTESIAN_POINT('Ctrl Pts',(25.3980467425329,1.35229533657296,-5.65379185297181));
#66471=CARTESIAN_POINT('Ctrl Pts',(25.4986166524907,3.88678066624468,-4.32284640561678));
#66472=CARTESIAN_POINT('Ctrl Pts',(25.5991865624485,5.47872503020431,-1.94361442612985));
#66473=CARTESIAN_POINT('Ctrl Pts',(25.6997564724064,5.74208329058304,0.906942378574534));
#66474=CARTESIAN_POINT('Ctrl Pts',(25.8003263823641,4.61299129594534,3.53756643719661));
#66475=CARTESIAN_POINT('Ctrl Pts',(25.900896292322,2.3652528830361,5.31033368003713));
#66476=CARTESIAN_POINT('Ctrl Pts',(26.0014662022797,-0.456057317931881,
5.79534957675619));
#66477=CARTESIAN_POINT('Ctrl Pts',(26.1020361122375,-3.1667740118886,4.87499818991498));
#66478=CARTESIAN_POINT('Ctrl Pts',(26.2025783171634,-5.10901553723906,2.77304314538772));
#66479=CARTESIAN_POINT('Ctrl Pts',(26.2695972187698,-5.5783062520285,0.924089784394088));
#66480=CARTESIAN_POINT('Ctrl Pts',(26.3030928170571,-5.57831427096578,-8.04366799073348E-7));
#66481=CARTESIAN_POINT('Origin',(16.5082437683087,0.,0.));
#66482=CARTESIAN_POINT('',(23.4932437683088,-5.57831163277732,1.31347539625247E-5));
#66483=CARTESIAN_POINT('',(23.7630928170571,-5.57776496850477,-0.000142365144290002));
#66484=CARTESIAN_POINT('',(16.5082437683087,-5.57784,5.11151866531329E-13));
#66485=CARTESIAN_POINT('Ctrl Pts',(23.4932437683088,-5.57831163277732,1.31347539627179E-5));
#66486=CARTESIAN_POINT('Ctrl Pts',(23.5263138657724,-5.57818690513318,-0.912339814690282));
#66487=CARTESIAN_POINT('Ctrl Pts',(23.5929072665553,-5.11826294276396,-2.74967014419475));
#66488=CARTESIAN_POINT('Ctrl Pts',(23.6930239706574,-3.19749799998333,-4.85490179812288));
#66489=CARTESIAN_POINT('Ctrl Pts',(23.7935938806152,-0.492647672782865,
-5.79235385657815));
#66490=CARTESIAN_POINT('Ctrl Pts',(23.894163790573,2.33166929098219,-5.32516509103753));
#66491=CARTESIAN_POINT('Ctrl Pts',(23.9947337005308,4.59055845885185,-3.56662837497514));
#66492=CARTESIAN_POINT('Ctrl Pts',(24.0953036104886,5.73624115213431,-0.94318734823729));
#66493=CARTESIAN_POINT('Ctrl Pts',(24.1958735204464,5.49089030394512,1.90897579852541));
#66494=CARTESIAN_POINT('Ctrl Pts',(24.2964434304042,3.91400328376506,4.2982139574468));
#66495=CARTESIAN_POINT('Ctrl Pts',(24.397013340362,1.38797383655825,5.64513893171319));
#66496=CARTESIAN_POINT('Ctrl Pts',(24.4975832503198,-1.47463807120625,5.62312257453662));
#66497=CARTESIAN_POINT('Ctrl Pts',(24.5981531602776,-3.97965151611398,4.23750383358008));
#66498=CARTESIAN_POINT('Ctrl Pts',(24.6867066662739,-5.33560473957068,2.11263182982895));
#66499=CARTESIAN_POINT('Ctrl Pts',(24.741736868951,-5.57710115662481,0.593479307041815));
#66500=CARTESIAN_POINT('Ctrl Pts',(24.7632437683088,-5.57751463566409,-0.000107372944178757));
#66501=CARTESIAN_POINT('Ctrl Pts',(23.7630928170571,-5.57776496850477,-0.000142365144289967));
#66502=CARTESIAN_POINT('Ctrl Pts',(23.7717046057741,-5.57800034635737,-0.237795620494548));
#66503=CARTESIAN_POINT('Ctrl Pts',(23.8138396978104,-5.50506709041506,-1.40042358557772));
#66504=CARTESIAN_POINT('Ctrl Pts',(23.8894980931659,-4.71306465610696,-3.40309954914673));
#66505=CARTESIAN_POINT('Ctrl Pts',(23.9900680031237,-2.51737095653659,-5.23993401306099));
#66506=CARTESIAN_POINT('Ctrl Pts',(24.0906379130815,0.288783032968795,-5.80608898949342));
#66507=CARTESIAN_POINT('Ctrl Pts',(24.1912078230393,3.02490738557195,-4.9642723840216));
#66508=CARTESIAN_POINT('Ctrl Pts',(24.2917777329971,5.02749430110096,-2.91862399881259));
#66509=CARTESIAN_POINT('Ctrl Pts',(24.3923476429549,5.81091817642424,-0.165211806326761));
#66510=CARTESIAN_POINT('Ctrl Pts',(24.4929175529127,5.18519939616966,2.62826410697425));
#66511=CARTESIAN_POINT('Ctrl Pts',(24.5934874628705,3.30207422591229,4.78438823681912));
#66512=CARTESIAN_POINT('Ctrl Pts',(24.6940573728283,0.618198898391366,5.78030233777395));
#66513=CARTESIAN_POINT('Ctrl Pts',(24.7946272827861,-2.21558912982611,5.37449809766863));
#66514=CARTESIAN_POINT('Ctrl Pts',(24.895197192744,-4.51209870130343,3.66538269540076));
#66515=CARTESIAN_POINT('Ctrl Pts',(24.9746857041676,-5.46239669669542,1.61199939801417));
#66516=CARTESIAN_POINT('Ctrl Pts',(25.020650912272,-5.57771142467081,0.343498504248142));
#66517=CARTESIAN_POINT('Ctrl Pts',(25.0330928170571,-5.57749036758178,9.9814762887715E-5));
#66518=CARTESIAN_POINT('Origin',(16.5082437683087,0.,0.));
#66519=CARTESIAN_POINT('',(22.2232437683088,-5.57746529176104,9.05900862117445E-5));
#66520=CARTESIAN_POINT('',(22.4930928170571,-5.57815907267454,9.96846322134232E-5));
#66521=CARTESIAN_POINT('',(16.5082437683087,-5.57784,5.11151866531329E-13));
#66522=CARTESIAN_POINT('Ctrl Pts',(22.2232437683088,-5.57746529176104,9.05900862117892E-5));
#66523=CARTESIAN_POINT('Ctrl Pts',(22.2438442559552,-5.57713507809895,-0.568493695023154));
#66524=CARTESIAN_POINT('Ctrl Pts',(22.297968046921,-5.34995718351836,-2.06259671300443));
#66525=CARTESIAN_POINT('Ctrl Pts',(22.385615141206,-4.03629730435431,-4.18358327276709));
#66526=CARTESIAN_POINT('Ctrl Pts',(22.4861850511638,-1.5501508710191,-5.60277584830882));
#66527=CARTESIAN_POINT('Ctrl Pts',(22.5867549611216,1.31190581412394,-5.66330010366589));
#66528=CARTESIAN_POINT('Ctrl Pts',(22.6873248710794,3.85582646866807,-4.35047895901507));
#66529=CARTESIAN_POINT('Ctrl Pts',(22.7878947810372,5.46471252376619,-1.98267041182017));
#66530=CARTESIAN_POINT('Ctrl Pts',(22.888464690995,5.74841049603226,0.865934003501583));
#66531=CARTESIAN_POINT('Ctrl Pts',(22.9890346009528,4.63812387140712,3.50455016839501));
#66532=CARTESIAN_POINT('Ctrl Pts',(23.0896045109106,2.40309620059581,5.29331593426996));
#66533=CARTESIAN_POINT('Ctrl Pts',(23.1901744208684,-0.414680230205875,
5.79845714272258));
#66534=CARTESIAN_POINT('Ctrl Pts',(23.2907443308262,-3.13189706215126,4.89747748554319));
#66535=CARTESIAN_POINT('Ctrl Pts',(23.391314240784,-5.08963155255177,2.80886375400866));
#66536=CARTESIAN_POINT('Ctrl Pts',(23.4588140532782,-5.57522741043254,0.949874987164157));
#66537=CARTESIAN_POINT('Ctrl Pts',(23.4927905624531,-5.57831334209489,0.0125163848447095));
#66538=CARTESIAN_POINT('Ctrl Pts',(23.4932437683088,-5.57831163277732,1.31347539627179E-5));
#66539=CARTESIAN_POINT('Ctrl Pts',(22.4930928170571,-5.57815907267454,9.96846322134405E-5));
#66540=CARTESIAN_POINT('Ctrl Pts',(22.5227582992762,-5.57747866976091,-0.818390184172317));
#66541=CARTESIAN_POINT('Ctrl Pts',(22.5859470848146,-5.18899760582401,-2.56243426994159));
#66542=CARTESIAN_POINT('Ctrl Pts',(22.6826591736723,-3.43863942725612,-4.68719787115575));
#66543=CARTESIAN_POINT('Ctrl Pts',(22.7832290836301,-0.78459279653397,-5.7600763135287));
#66544=CARTESIAN_POINT('Ctrl Pts',(22.8837989935879,2.05971691194769,-5.4361412083098));
#66545=CARTESIAN_POINT('Ctrl Pts',(22.9843689035457,4.40454704234543,-3.79394653966204));
#66546=CARTESIAN_POINT('Ctrl Pts',(23.0849388135035,5.68127830653479,-1.2317231010842));
#66547=CARTESIAN_POINT('Ctrl Pts',(23.1855087234613,5.58030447199677,1.62919212920396));
#66548=CARTESIAN_POINT('Ctrl Pts',(23.2860786334191,4.12611160668567,4.09502967061549));
#66549=CARTESIAN_POINT('Ctrl Pts',(23.3866485433769,1.67134022862849,5.56782604202173));
#66550=CARTESIAN_POINT('Ctrl Pts',(23.4872184533347,-1.1887297161335,5.69042939118205));
#66551=CARTESIAN_POINT('Ctrl Pts',(23.5877883632925,-3.76053372802574,4.43310851146552));
#66552=CARTESIAN_POINT('Ctrl Pts',(23.6797464845333,-5.27827641947763,2.30048111746861));
#66553=CARTESIAN_POINT('Ctrl Pts',(23.7381813024548,-5.57708408570509,0.687322543190415));
#66554=CARTESIAN_POINT('Ctrl Pts',(23.7630928170571,-5.57776496850477,-0.000142365144289967));
#66555=CARTESIAN_POINT('Origin',(16.5082437683087,0.,0.));
#66556=CARTESIAN_POINT('',(20.9532437683088,-5.5778058049599,-0.000143089372731608));
#66557=CARTESIAN_POINT('',(21.2230928170571,-5.57736899471967,1.10549737200594E-5));
#66558=CARTESIAN_POINT('',(16.5082437683087,-5.57784,5.11151866531329E-13));
#66559=CARTESIAN_POINT('Ctrl Pts',(20.9532437683088,-5.5778058049599,-0.000143089372731907));
#66560=CARTESIAN_POINT('Ctrl Pts',(20.9613746461381,-5.57803218064351,-0.224520272604914));
#66561=CARTESIAN_POINT('Ctrl Pts',(21.0030288272867,-5.50997940288581,-1.37385969881095));
#66562=CARTESIAN_POINT('Ctrl Pts',(21.0782063117546,-4.7372348978758,-3.36937241192321));
#66563=CARTESIAN_POINT('Ctrl Pts',(21.1787762217124,-2.5547079071865,-5.22183228757078));
#66564=CARTESIAN_POINT('Ctrl Pts',(21.2793461316702,0.247333551781491,-5.80800232805862));
#66565=CARTESIAN_POINT('Ctrl Pts',(21.379916041628,2.98939683737892,-4.98573680395642));
#66566=CARTESIAN_POINT('Ctrl Pts',(21.4804859515858,5.0065339632579,-2.95443439662243));
#66567=CARTESIAN_POINT('Ctrl Pts',(21.5810558615436,5.80959091282129,-0.206684191439672));
#66568=CARTESIAN_POINT('Ctrl Pts',(21.6816257715014,5.20382706708468,2.59118675228346));
#66569=CARTESIAN_POINT('Ctrl Pts',(21.7821956814592,3.33613963718532,4.76069713912736));
#66570=CARTESIAN_POINT('Ctrl Pts',(21.882765591417,0.659441217112314,5.77574256788688));
#66571=CARTESIAN_POINT('Ctrl Pts',(21.9833355013748,-2.17717113044407,5.39017539585389));
#66572=CARTESIAN_POINT('Ctrl Pts',(22.0839054113326,-4.48582135303932,3.69749533034633));
#66573=CARTESIAN_POINT('Ctrl Pts',(22.1638748336439,-5.45658946829869,1.63856553019077));
#66574=CARTESIAN_POINT('Ctrl Pts',(22.210320952636,-5.57767243687145,0.356767093915296));
#66575=CARTESIAN_POINT('Ctrl Pts',(22.2232437683088,-5.57746529176104,9.05900862117892E-5));
#66576=CARTESIAN_POINT('Ctrl Pts',(21.2230928170571,-5.57736899471967,1.10549737201288E-5));
#66577=CARTESIAN_POINT('Ctrl Pts',(21.2402886894591,-5.57733608158979,-0.47462751888798));
#66578=CARTESIAN_POINT('Ctrl Pts',(21.2910078651803,-5.40050874890991,-1.87459669199057));
#66579=CARTESIAN_POINT('Ctrl Pts',(21.3752503442208,-4.24245948454918,-3.97436819079288));
#66580=CARTESIAN_POINT('Ctrl Pts',(21.4758202541787,-1.83117047488202,-5.51732541055725));
#66581=CARTESIAN_POINT('Ctrl Pts',(21.5763901641365,1.02417579862052,-5.72233596772863));
#66582=CARTESIAN_POINT('Ctrl Pts',(21.6769600740943,3.6311603225972,-4.53968497867921));
#66583=CARTESIAN_POINT('Ctrl Pts',(21.7775299840521,5.35759159415115,-2.25616429018983));
#66584=CARTESIAN_POINT('Ctrl Pts',(21.8780998940099,5.78481151609187,0.574474296499018));
#66585=CARTESIAN_POINT('Ctrl Pts',(21.9786698039677,4.809219625112,3.26580336081112));
#66586=CARTESIAN_POINT('Ctrl Pts',(22.0792397139255,2.66739611495663,5.16517792142356));
#66587=CARTESIAN_POINT('Ctrl Pts',(22.1798096238833,-0.121268656904642,
5.81200128242416));
#66588=CARTESIAN_POINT('Ctrl Pts',(22.2803795338411,-2.88052588385809,5.04941933557423));
#66589=CARTESIAN_POINT('Ctrl Pts',(22.3809494437989,-4.94125806361523,3.06235754653254));
#66590=CARTESIAN_POINT('Ctrl Pts',(22.4518538715375,-5.54933006834121,1.13786085343053));
#66591=CARTESIAN_POINT('Ctrl Pts',(22.4892349959569,-5.57824755506284,0.10653946750165));
#66592=CARTESIAN_POINT('Ctrl Pts',(22.4930928170571,-5.57815907267454,9.96846322134405E-5));
#66593=CARTESIAN_POINT('Origin',(16.5082437683087,0.,0.));
#66594=CARTESIAN_POINT('',(19.6832437683088,-5.57812419168581,0.000109767319341423));
#66595=CARTESIAN_POINT('',(19.9530928170571,-5.57809442763664,-0.000115493386879661));
#66596=CARTESIAN_POINT('',(16.5082437683087,-5.57784,5.11151866531329E-13));
#66597=CARTESIAN_POINT('Ctrl Pts',(19.6832437683088,-5.57812419168581,0.000109767319341463));
#66598=CARTESIAN_POINT('Ctrl Pts',(19.7124283396402,-5.57741063147403,-0.805125894194631));
#66599=CARTESIAN_POINT('Ctrl Pts',(19.775136214291,-5.19852697588659,-2.5359603525814));
#66600=CARTESIAN_POINT('Ctrl Pts',(19.8713673922609,-3.4720077142605,-4.66253371853033));
#66601=CARTESIAN_POINT('Ctrl Pts',(19.9719373022187,-0.825686473140719,
-5.75432978220954));
#66602=CARTESIAN_POINT('Ctrl Pts',(20.0725072121766,2.02086287490732,-5.45070416604466));
#66603=CARTESIAN_POINT('Ctrl Pts',(20.1730771221344,4.37735479309912,-3.82528833061492));
#66604=CARTESIAN_POINT('Ctrl Pts',(20.2736470320921,5.67234190241483,-1.27224293413637));
#66605=CARTESIAN_POINT('Ctrl Pts',(20.37421694205,5.59179100359806,1.58932005701102));
#66606=CARTESIAN_POINT('Ctrl Pts',(20.4747868520077,4.15523558961498,4.06547441574607));
#66607=CARTESIAN_POINT('Ctrl Pts',(20.5753567619656,1.71103912739439,5.55575467045122));
#66608=CARTESIAN_POINT('Ctrl Pts',(20.6759266719234,-1.14808285301524,5.69876922970695));
#66609=CARTESIAN_POINT('Ctrl Pts',(20.7764965818812,-3.72879572848776,4.45983714130576));
#66610=CARTESIAN_POINT('Ctrl Pts',(20.8689356140096,-5.26973851376936,2.32700126529614));
#66611=CARTESIAN_POINT('Ctrl Pts',(20.9278513428188,-5.57709884221868,0.700578410378731));
#66612=CARTESIAN_POINT('Ctrl Pts',(20.9532437683088,-5.5778058049599,-0.000143089372731907));
#66613=CARTESIAN_POINT('Ctrl Pts',(19.9530928170571,-5.57809442763664,-0.000115493386879852));
#66614=CARTESIAN_POINT('Ctrl Pts',(19.9578190796419,-5.57821483639134,-0.130520510715282));
#66615=CARTESIAN_POINT('Ctrl Pts',(19.9960686455461,-5.54195387079495,-1.18581934554418));
#66616=CARTESIAN_POINT('Ctrl Pts',(20.0678415147694,-4.90137626234256,-3.12579203238712));
#66617=CARTESIAN_POINT('Ctrl Pts',(20.1684114247273,-2.81520362818565,-5.08612754957154));
#66618=CARTESIAN_POINT('Ctrl Pts',(20.268981334685,-0.0463465410280725,
-5.81308154368905));
#66619=CARTESIAN_POINT('Ctrl Pts',(20.3695512446429,2.73374954418304,-5.13036825249749));
#66620=CARTESIAN_POINT('Ctrl Pts',(20.4701211546007,4.85091371732528,-3.20354508412377));
#66621=CARTESIAN_POINT('Ctrl Pts',(20.5706910645585,5.79173549027881,-0.499864986629304));
#66622=CARTESIAN_POINT('Ctrl Pts',(20.6712609745162,5.32806639229823,2.32503193781961));
#66623=CARTESIAN_POINT('Ctrl Pts',(20.7718308844741,3.57234578085699,4.58611061982589));
#66624=CARTESIAN_POINT('Ctrl Pts',(20.8724007944319,0.950334392674663,5.73506142385651));
#66625=CARTESIAN_POINT('Ctrl Pts',(20.9729707043897,-1.90213226762502,5.4932647697747));
#66626=CARTESIAN_POINT('Ctrl Pts',(21.0735406143475,-4.29333349045155,3.91935613764576));
#66627=CARTESIAN_POINT('Ctrl Pts',(21.1569146519033,-5.41256404288243,1.82663100194757));
#66628=CARTESIAN_POINT('Ctrl Pts',(21.2067653861398,-5.57740024564094,0.450679002736854));
#66629=CARTESIAN_POINT('Ctrl Pts',(21.2230928170571,-5.57736899471967,1.10549737201288E-5));
#66630=CARTESIAN_POINT('Origin',(55.8232233047034,0.,-1.80744194084639E-16));
#66631=CARTESIAN_POINT('',(56.,5.05,-6.18446633569413E-16));
#66632=CARTESIAN_POINT('Origin',(56.,0.,0.));
#66633=CARTESIAN_POINT('',(55.6464466094067,5.90355339059328,7.22976776338556E-16));
#66634=CARTESIAN_POINT('',(55.8232233047034,5.47677669529664,6.70711704953985E-16));
#66635=CARTESIAN_POINT('',(55.6464466094067,-5.90355339059328,-7.22976776338556E-16));
#66636=CARTESIAN_POINT('Origin',(55.6464466094067,0.,-3.61488388169278E-16));
#66637=CARTESIAN_POINT('Origin',(55.6464466094067,0.,-3.61488388169278E-16));
#66638=CARTESIAN_POINT('Origin',(55.6,0.,0.));
#66639=CARTESIAN_POINT('',(55.26731,-6.28269,-7.69407619853509E-16));
#66640=CARTESIAN_POINT('',(55.6,-5.95,-7.28664845492675E-16));
#66641=CARTESIAN_POINT('',(55.26731,3.34571636511773,-5.31774159209371));
#66642=CARTESIAN_POINT('Origin',(55.26731,0.,0.));
#66643=CARTESIAN_POINT('',(55.26731,6.25879749617516,-0.55033779021994));
#66644=CARTESIAN_POINT('Origin',(55.26731,0.,0.));
#66645=CARTESIAN_POINT('Origin',(55.26731,0.,0.));
#66646=CARTESIAN_POINT('Origin',(56.,0.,0.));
#66647=CARTESIAN_POINT('Origin',(-0.25,7.95,-6.));
#66648=CARTESIAN_POINT('',(-0.379994381348751,8.07999438134875,7.13596312065045));
#66649=CARTESIAN_POINT('',(0.,7.7,6.99070811863863));
#66650=CARTESIAN_POINT('Ctrl Pts',(-0.379994381348751,8.07999438134875,
7.13596312065045));
#66651=CARTESIAN_POINT('Ctrl Pts',(-0.188043578117705,7.88804357811771,
7.06333561964445));
#66652=CARTESIAN_POINT('Ctrl Pts',(-1.38777878078145E-16,7.7,6.99070811863862));
#66653=CARTESIAN_POINT('',(0.,7.7,-6.99070811863863));
#66654=CARTESIAN_POINT('',(0.,7.7,-6.));
#66655=CARTESIAN_POINT('',(-0.37999438134875,8.07999438134875,-7.13596312065045));
#66656=CARTESIAN_POINT('Ctrl Pts',(-1.38777878078145E-16,7.7,-6.99070811863862));
#66657=CARTESIAN_POINT('Ctrl Pts',(-0.188043578117704,7.8880435781177,-7.06333561964445));
#66658=CARTESIAN_POINT('Ctrl Pts',(-0.37999438134875,8.07999438134875,-7.13596312065045));
#66659=CARTESIAN_POINT('',(-0.5,8.2,-6.83212111192935));
#66660=CARTESIAN_POINT('',(-0.686724551909448,8.38672455190945,-6.3593535568152));
#66661=CARTESIAN_POINT('',(-0.5,8.2,6.83212111192935));
#66662=CARTESIAN_POINT('',(-0.5,8.2,-6.));
#66663=CARTESIAN_POINT('',(-2.49296364416094,10.1929636441609,1.78614006741046));
#66664=CARTESIAN_POINT('Origin',(0.,7.17,0.));
#66665=CARTESIAN_POINT('Origin',(0.,0.,0.));
#66666=CARTESIAN_POINT('',(0.,-7.17,-8.78071754988652E-16));
#66667=CARTESIAN_POINT('Origin',(0.,0.,0.));
#66668=CARTESIAN_POINT('Origin',(-3.3,8.02916838915042,7.26464935833121));
#66669=CARTESIAN_POINT('',(-6.,8.2,6.83212111192935));
#66670=CARTESIAN_POINT('',(-3.3,8.2,6.83212111192935));
#66671=CARTESIAN_POINT('',(-6.15556461521625,8.04443538478375,7.22599487971177));
#66672=CARTESIAN_POINT('',(-4.01298129963321,10.1870187003668,1.80119205984589));
#66673=CARTESIAN_POINT('',(-6.,7.85833677830084,7.69717760473307));
#66674=CARTESIAN_POINT('Ctrl Pts',(-6.15556461521625,8.04443538478375,7.22599487971177));
#66675=CARTESIAN_POINT('Ctrl Pts',(-6.08268462231632,7.95218239374537,7.45957006079633));
#66676=CARTESIAN_POINT('Ctrl Pts',(-6.,7.85833677830084,7.69717760473307));
#66677=CARTESIAN_POINT('',(-0.599999999999996,7.85833677830084,7.69717760473307));
#66678=CARTESIAN_POINT('',(-3.3,7.85833677830084,7.69717760473307));
#66679=CARTESIAN_POINT('Ctrl Pts',(-0.6,7.85833677830085,7.69717760473306));
#66680=CARTESIAN_POINT('Ctrl Pts',(-0.481638745218463,7.97028509154812,
7.41373587298517));
#66681=CARTESIAN_POINT('Ctrl Pts',(-0.37999438134875,8.07999438134875,7.13596312065045));
#66682=CARTESIAN_POINT('Origin',(-3.3,0.,0.));
#66683=CARTESIAN_POINT('',(-6.,7.85833677830084,-7.69717760473307));
#66684=CARTESIAN_POINT('Origin',(-6.,0.,0.));
#66685=CARTESIAN_POINT('',(-0.599999999999996,7.85833677830084,-7.69717760473307));
#66686=CARTESIAN_POINT('',(-3.3,7.85833677830084,-7.69717760473307));
#66687=CARTESIAN_POINT('Origin',(-0.599999999999996,0.,0.));
#66688=CARTESIAN_POINT('Origin',(-6.25,0.,0.));
#66689=CARTESIAN_POINT('',(-6.5,7.7,6.99070811863863));
#66690=CARTESIAN_POINT('Ctrl Pts',(-6.5,7.7,6.99070811863863));
#66691=CARTESIAN_POINT('Ctrl Pts',(-6.33063251438461,7.86936748561539,7.10651564020904));
#66692=CARTESIAN_POINT('Ctrl Pts',(-6.15556461521625,8.04443538478376,7.22599487971177));
#66693=CARTESIAN_POINT('',(-6.5,7.7,-6.99070811863863));
#66694=CARTESIAN_POINT('Origin',(-6.5,0.,0.));
#66695=CARTESIAN_POINT('',(-6.15556461521625,8.04443538478375,-7.22599487971178));
#66696=CARTESIAN_POINT('Ctrl Pts',(-6.15556461521625,8.04443538478375,-7.22599487971178));
#66697=CARTESIAN_POINT('Ctrl Pts',(-6.33063251438454,7.86936748561546,-7.1065156402091));
#66698=CARTESIAN_POINT('Ctrl Pts',(-6.5,7.7,-6.99070811863863));
#66699=CARTESIAN_POINT('Ctrl Pts',(-6.,7.85833677830084,-7.69717760473307));
#66700=CARTESIAN_POINT('Ctrl Pts',(-6.08268462231633,7.95218239374537,-7.45957006079634));
#66701=CARTESIAN_POINT('Ctrl Pts',(-6.15556461521625,8.04443538478375,-7.22599487971178));
#66702=CARTESIAN_POINT('Origin',(-6.25,7.95,-6.));
#66703=CARTESIAN_POINT('',(-6.,8.2,-6.83212111192935));
#66704=CARTESIAN_POINT('',(-6.,8.2,-6.));
#66705=CARTESIAN_POINT('',(-5.8192203918847,8.3807796081153,-6.37440554925063));
#66706=CARTESIAN_POINT('',(-6.5,7.7,-6.));
#66707=CARTESIAN_POINT('Origin',(0.,8.2,-12.));
#66708=CARTESIAN_POINT('',(-3.3,8.2,-6.83212111192935));
#66709=CARTESIAN_POINT('Origin',(-6.5,10.4,0.));
#66710=CARTESIAN_POINT('Origin',(-3.3,8.02916838915042,-7.26464935833121));
#66711=CARTESIAN_POINT('Ctrl Pts',(-0.37999438134875,8.07999438134875,-7.13596312065045));
#66712=CARTESIAN_POINT('Ctrl Pts',(-0.481638745218464,7.97028509154812,
-7.41373587298517));
#66713=CARTESIAN_POINT('Ctrl Pts',(-0.6,7.85833677830085,-7.69717760473306));
#66714=CARTESIAN_POINT('Origin',(-0.300000000000002,0.,0.));
#66715=CARTESIAN_POINT('Origin',(55.26731,1.21203632162606E-15,2.67744564496562E-16));
#66716=CARTESIAN_POINT('Ctrl Pts',(55.26731,-5.53879749490421,-0.66264931684701));
#66717=CARTESIAN_POINT('Ctrl Pts',(55.26731,-5.53639098513788,-0.70561892266728));
#66718=CARTESIAN_POINT('Ctrl Pts',(55.26731,-5.53347920854467,-0.748545142165827));
#66719=CARTESIAN_POINT('Ctrl Pts',(55.26731,-5.53006164828575,-0.79141917993666));
#66720=CARTESIAN_POINT('Ctrl Pts',(55.26731,-5.51741046348254,-0.950131048639964));
#66721=CARTESIAN_POINT('Ctrl Pts',(55.26731,-5.49783241559118,-1.10812730197615));
#66722=CARTESIAN_POINT('Ctrl Pts',(55.26731,-5.47155417770622,-1.26500836420001));
#66723=CARTESIAN_POINT('Ctrl Pts',(55.26731,-5.44498168391539,-1.42364613398091));
#66724=CARTESIAN_POINT('Ctrl Pts',(55.26731,-5.4115580176756,-1.58114430079878));
#66725=CARTESIAN_POINT('Ctrl Pts',(55.26731,-5.37146426041803,-1.73709118451399));
#66726=CARTESIAN_POINT('Ctrl Pts',(55.26731,-5.35511257576213,-1.80069196528392));
#66727=CARTESIAN_POINT('Ctrl Pts',(55.26731,-5.33765084923196,-1.86403467739513));
#66728=CARTESIAN_POINT('Ctrl Pts',(55.26731,-5.31908891537725,-1.927091041383));
#66729=CARTESIAN_POINT('Ctrl Pts',(55.26731,-5.31157503508314,-1.95261628969471));
#66730=CARTESIAN_POINT('Ctrl Pts',(55.26731,-5.30388243230773,-1.97808913032777));
#66731=CARTESIAN_POINT('Ctrl Pts',(55.26731,-5.29601425645973,-2.00350056357598));
#66732=CARTESIAN_POINT('Ctrl Pts',(55.26731,-5.24778551413657,-2.15926239323839));
#66733=CARTESIAN_POINT('Ctrl Pts',(55.26731,-5.19294007214862,-2.31280035724505));
#66734=CARTESIAN_POINT('Ctrl Pts',(55.26731,-5.13168699340163,-2.46369615505792));
#66735=CARTESIAN_POINT('Ctrl Pts',(55.26731,-5.07029795396065,-2.6149268894619));
#66736=CARTESIAN_POINT('Ctrl Pts',(55.26731,-5.00247261475932,-2.76350446256005));
#66737=CARTESIAN_POINT('Ctrl Pts',(55.26731,-4.92836992148161,-2.90899887332677));
#66738=CARTESIAN_POINT('Ctrl Pts',(55.26731,-4.90394573253089,-2.9569537157577));
#66739=CARTESIAN_POINT('Ctrl Pts',(55.26731,-4.87883919629439,-3.00457349651584));
#66740=CARTESIAN_POINT('Ctrl Pts',(55.26731,-4.85305483416844,-3.05184239250323));
#66741=CARTESIAN_POINT('Ctrl Pts',(55.26731,-4.83800368980644,-3.0794347360277));
#66742=CARTESIAN_POINT('Ctrl Pts',(55.26731,-4.82272157071552,-3.10690751352349));
#66743=CARTESIAN_POINT('Ctrl Pts',(55.26731,-4.80720928755211,-3.13425753405247));
#66744=CARTESIAN_POINT('Ctrl Pts',(55.26731,-4.79564225862179,-3.15465159696193));
#66745=CARTESIAN_POINT('Ctrl Pts',(55.26731,-4.78394939219416,-3.1749735513043));
#66746=CARTESIAN_POINT('Ctrl Pts',(55.26731,-4.7721359879562,-3.19521407307116));
#66747=CARTESIAN_POINT('Ctrl Pts',(55.26731,-4.72395212555498,-3.27776999819641));
#66748=CARTESIAN_POINT('Ctrl Pts',(55.26731,-4.67374052959922,-3.3590117700535));
#66749=CARTESIAN_POINT('Ctrl Pts',(55.26731,-4.6215443815017,-3.43885946673828));
#66750=CARTESIAN_POINT('Ctrl Pts',(55.26731,-4.5328034432177,-3.57461200369533));
#66751=CARTESIAN_POINT('Ctrl Pts',(55.26731,-4.43832903291709,-3.70633616772238));
#66752=CARTESIAN_POINT('Ctrl Pts',(55.26731,-4.33852183698003,-3.8338008634785));
#66753=CARTESIAN_POINT('Ctrl Pts',(55.26731,-4.23736781566362,-3.96298560241993));
#66754=CARTESIAN_POINT('Ctrl Pts',(55.26731,-4.13073572754274,-4.08779570010757));
#66755=CARTESIAN_POINT('Ctrl Pts',(55.26731,-4.01899373500795,-4.20796867396684));
#66756=CARTESIAN_POINT('Ctrl Pts',(55.26731,-3.909336498848,-4.32589959568748));
#66757=CARTESIAN_POINT('Ctrl Pts',(55.26731,-3.79475765651907,-4.43936521884963));
#66758=CARTESIAN_POINT('Ctrl Pts',(55.26731,-3.67556598183449,-4.54808950467785));
#66759=CARTESIAN_POINT('Ctrl Pts',(55.26731,-3.58617222582106,-4.62963271904902));
#66760=CARTESIAN_POINT('Ctrl Pts',(55.26731,-3.49418291445617,-4.70850841060584));
#66761=CARTESIAN_POINT('Ctrl Pts',(55.26731,-3.39971633932651,-4.7845873566953));
#66762=CARTESIAN_POINT('Ctrl Pts',(55.26731,-3.37842810366135,-4.80173190259724));
#66763=CARTESIAN_POINT('Ctrl Pts',(55.26731,-3.35701402694704,-4.81873437102781));
#66764=CARTESIAN_POINT('Ctrl Pts',(55.26731,-3.3354754008909,-4.83559319542517));
#66765=CARTESIAN_POINT('Ctrl Pts',(55.26731,-3.31814813154819,-4.84915568499034));
#66766=CARTESIAN_POINT('Ctrl Pts',(55.26731,-3.3007467856717,-4.8626200729148));
#66767=CARTESIAN_POINT('Ctrl Pts',(55.26731,-3.28327672842942,-4.87598236089846));
#66768=CARTESIAN_POINT('Ctrl Pts',(55.26731,-3.14959090197206,-4.97823437345244));
#66769=CARTESIAN_POINT('Ctrl Pts',(55.26731,-3.01180300905512,-5.07457437893082));
#66770=CARTESIAN_POINT('Ctrl Pts',(55.26731,-2.87031200820997,-5.1647462198623));
#66771=CARTESIAN_POINT('Ctrl Pts',(55.26731,-2.74730242599433,-5.24313990154057));
#66772=CARTESIAN_POINT('Ctrl Pts',(55.26731,-2.62149298241495,-5.31687137958735));
#66773=CARTESIAN_POINT('Ctrl Pts',(55.26731,-2.49312065219561,-5.38575260253262));
#66774=CARTESIAN_POINT('Ctrl Pts',(55.26731,-2.34617012834124,-5.46460239655165));
#66775=CARTESIAN_POINT('Ctrl Pts',(55.26731,-2.19586150139362,-5.53709781451365));
#66776=CARTESIAN_POINT('Ctrl Pts',(55.26731,-2.04264539888495,-5.60318412837367));
#66777=CARTESIAN_POINT('Ctrl Pts',(55.26731,-1.88854421239906,-5.66965220326634));
#66778=CARTESIAN_POINT('Ctrl Pts',(55.26731,-1.73150118930178,-5.72963719159267));
#66779=CARTESIAN_POINT('Ctrl Pts',(55.26731,-1.57194996293008,-5.78303699335734));
#66780=CARTESIAN_POINT('Ctrl Pts',(55.26731,-1.4929835329537,-5.80946607073076));
#66781=CARTESIAN_POINT('Ctrl Pts',(55.26731,-1.41340238971528,-5.83428134027811));
#66782=CARTESIAN_POINT('Ctrl Pts',(55.26731,-1.33325765941392,-5.85746592651278));
#66783=CARTESIAN_POINT('Ctrl Pts',(55.26731,-1.31267842894026,-5.86341916812661));
#66784=CARTESIAN_POINT('Ctrl Pts',(55.26731,-1.2920594397503,-5.86926559490217));
#66785=CARTESIAN_POINT('Ctrl Pts',(55.26731,-1.27141013285999,-5.87500251293336));
#66786=CARTESIAN_POINT('Ctrl Pts',(55.26731,-1.10752825083565,-5.92053319001446));
#66787=CARTESIAN_POINT('Ctrl Pts',(55.26731,-0.942046179526727,-5.95908657120551));
#66788=CARTESIAN_POINT('Ctrl Pts',(55.26731,-0.775444606041624,-5.99064537269145));
#66789=CARTESIAN_POINT('Ctrl Pts',(55.26731,-0.607515220055868,-6.0224556974388));
#66790=CARTESIAN_POINT('Ctrl Pts',(55.26731,-0.438447729379715,-6.04715977389526));
#66791=CARTESIAN_POINT('Ctrl Pts',(55.26731,-0.268707779413495,-6.0646939791095));
#66792=CARTESIAN_POINT('Ctrl Pts',(55.26731,-0.0990952702397115,-6.08221501963854));
#66793=CARTESIAN_POINT('Ctrl Pts',(55.26731,0.0711894188729789,-6.09257716755982));
#66794=CARTESIAN_POINT('Ctrl Pts',(55.26731,0.241697465736731,-6.09566772239982));
#66795=CARTESIAN_POINT('Ctrl Pts',(55.26731,0.291425473729497,-6.09656907068579));
#66796=CARTESIAN_POINT('Ctrl Pts',(55.26731,0.341172543128352,-6.0968515846414));
#66797=CARTESIAN_POINT('Ctrl Pts',(55.26731,0.390927654735083,-6.09651163725333));
#66798=CARTESIAN_POINT('Ctrl Pts',(55.26731,0.519364571915785,-6.09563410340571));
#66799=CARTESIAN_POINT('Ctrl Pts',(55.26731,0.647855132112174,-6.09060997358755));
#66800=CARTESIAN_POINT('Ctrl Pts',(55.26731,0.776220742198477,-6.08149242407852));
#66801=CARTESIAN_POINT('Ctrl Pts',(55.26731,0.832380696611235,-6.07750349616832));
#66802=CARTESIAN_POINT('Ctrl Pts',(55.26731,0.888516726202931,-6.07273084466002));
#66803=CARTESIAN_POINT('Ctrl Pts',(55.26731,0.94461377786397,-6.06717791703778));
#66804=CARTESIAN_POINT('Ctrl Pts',(55.26731,0.979456538284439,-6.06372890642056));
#66805=CARTESIAN_POINT('Ctrl Pts',(55.26731,1.01428425996497,-6.05997886518406));
#66806=CARTESIAN_POINT('Ctrl Pts',(55.26731,1.04909331400685,-6.05592850219243));
#66807=CARTESIAN_POINT('Ctrl Pts',(55.26731,1.07028621757498,-6.053462507219));
#66808=CARTESIAN_POINT('Ctrl Pts',(55.26731,1.09146790447692,-6.05088565499255));
#66809=CARTESIAN_POINT('Ctrl Pts',(55.26731,1.11262823854904,-6.04819950667145));
#66810=CARTESIAN_POINT('Ctrl Pts',(55.26731,1.28221027526524,-6.02667231803342));
#66811=CARTESIAN_POINT('Ctrl Pts',(55.26731,1.45059848057761,-5.99810910051797));
#66812=CARTESIAN_POINT('Ctrl Pts',(55.26731,1.61737767416904,-5.96273158735447));
#66813=CARTESIAN_POINT('Ctrl Pts',(55.26731,1.78721861570122,-5.92670461051541));
#66814=CARTESIAN_POINT('Ctrl Pts',(55.26731,1.95539160952368,-5.88361085063995));
#66815=CARTESIAN_POINT('Ctrl Pts',(55.26731,2.12146398918322,-5.83363090017481));
#66816=CARTESIAN_POINT('Ctrl Pts',(55.26731,2.28786991126281,-5.7835505691788));
#66817=CARTESIAN_POINT('Ctrl Pts',(55.26731,2.45216750385921,-5.72655622517196));
#66818=CARTESIAN_POINT('Ctrl Pts',(55.26731,2.61391653842935,-5.66277744479735));
#66819=CARTESIAN_POINT('Ctrl Pts',(55.26731,2.7740105837354,-5.59965123831338));
#66820=CARTESIAN_POINT('Ctrl Pts',(55.26731,2.93160864878227,-5.52987849972489));
#66821=CARTESIAN_POINT('Ctrl Pts',(55.26731,3.08626846857654,-5.45353667014268));
#66822=CARTESIAN_POINT('Ctrl Pts',(55.26731,3.17371866150044,-5.41037026962568));
#66823=CARTESIAN_POINT('Ctrl Pts',(55.26731,3.26022910922655,-5.36510275759276));
#66824=CARTESIAN_POINT('Ctrl Pts',(55.26731,3.34571636511758,-5.31774159209381));
#66825=CARTESIAN_POINT('Ctrl Pts',(55.26731,6.259054959814,-0.550339049542366));
#66826=CARTESIAN_POINT('Ctrl Pts',(55.26731,6.26062435353154,-0.501976787317531));
#66827=CARTESIAN_POINT('Ctrl Pts',(55.26731,6.26162468980508,-0.453612950749968));
#66828=CARTESIAN_POINT('Ctrl Pts',(55.26731,6.26205307910451,-0.405256685636834));
#66829=CARTESIAN_POINT('Ctrl Pts',(55.26731,6.26359989997391,-0.230652697762518));
#66830=CARTESIAN_POINT('Ctrl Pts',(55.26731,6.25769385372729,-0.0561469830970189));
#66831=CARTESIAN_POINT('Ctrl Pts',(55.26731,6.24446672156915,0.117807872010252));
#66832=CARTESIAN_POINT('Ctrl Pts',(55.26731,6.2312217581332,0.291997232776786));
#66833=CARTESIAN_POINT('Ctrl Pts',(55.26731,6.21063574375413,0.465634978729183));
#66834=CARTESIAN_POINT('Ctrl Pts',(55.26731,6.18279028992183,0.638254810814217));
#66835=CARTESIAN_POINT('Ctrl Pts',(55.26731,6.17518420463392,0.685406535226076));
#66836=CARTESIAN_POINT('Ctrl Pts',(55.26731,6.16703619046129,0.732482206629567));
#66837=CARTESIAN_POINT('Ctrl Pts',(55.26731,6.15834728588605,0.77947205650192));
#66838=CARTESIAN_POINT('Ctrl Pts',(55.26731,6.15200415638981,0.813775886192789));
#66839=CARTESIAN_POINT('Ctrl Pts',(55.26731,6.1453727600719,0.848033975717414));
#66840=CARTESIAN_POINT('Ctrl Pts',(55.26731,6.13845341352662,0.882242476691098));
#66841=CARTESIAN_POINT('Ctrl Pts',(55.26731,6.13310876166636,0.908665857449567));
#66842=CARTESIAN_POINT('Ctrl Pts',(55.26731,6.12759420574721,0.935050245759139));
#66843=CARTESIAN_POINT('Ctrl Pts',(55.26731,6.12191042011715,0.961393081297173));
#66844=CARTESIAN_POINT('Ctrl Pts',(55.26731,6.08539362493502,1.13063872011406));
#66845=CARTESIAN_POINT('Ctrl Pts',(55.26731,6.04189304342002,1.29818273238435));
#66846=CARTESIAN_POINT('Ctrl Pts',(55.26731,5.99151057004913,1.46357572936354));
#66847=CARTESIAN_POINT('Ctrl Pts',(55.26731,5.94147782389488,1.62782065979071));
#66848=CARTESIAN_POINT('Ctrl Pts',(55.26731,5.88465812170642,1.78994500032788));
#66849=CARTESIAN_POINT('Ctrl Pts',(55.26731,5.82110503590125,1.94948687666254));
#66850=CARTESIAN_POINT('Ctrl Pts',(55.26731,5.79867983920363,2.00578245874144));
#66851=CARTESIAN_POINT('Ctrl Pts',(55.26731,5.77541587560676,2.06175625579524));
#66852=CARTESIAN_POINT('Ctrl Pts',(55.26731,5.75131420661106,2.11738708461132));
#66853=CARTESIAN_POINT('Ctrl Pts',(55.26731,5.73724476762827,2.14986178799096));
#66854=CARTESIAN_POINT('Ctrl Pts',(55.26731,5.72288985275387,2.18221960906239));
#66855=CARTESIAN_POINT('Ctrl Pts',(55.26731,5.70824957074237,2.21445624811616));
#66856=CARTESIAN_POINT('Ctrl Pts',(55.26731,5.69864542930337,2.23560373972508));
#66857=CARTESIAN_POINT('Ctrl Pts',(55.26731,5.68891860432664,2.25669867882069));
#66858=CARTESIAN_POINT('Ctrl Pts',(55.26731,5.67907503084032,2.27772758874302));
#66859=CARTESIAN_POINT('Ctrl Pts',(55.26731,5.63447921087121,2.37299801897305));
#66860=CARTESIAN_POINT('Ctrl Pts',(55.26731,5.58745815531255,2.46697904036293));
#66861=CARTESIAN_POINT('Ctrl Pts',(55.26731,5.53803781346215,2.55957253982886));
#66862=CARTESIAN_POINT('Ctrl Pts',(55.26731,5.45804813929303,2.70944046010506));
#66863=CARTESIAN_POINT('Ctrl Pts',(55.26731,5.37177526959653,2.85567505990725));
#66864=CARTESIAN_POINT('Ctrl Pts',(55.26731,5.27955684762645,2.99796478200937));
#66865=CARTESIAN_POINT('Ctrl Pts',(55.26731,5.18687973109493,3.14096225339068));
#66866=CARTESIAN_POINT('Ctrl Pts',(55.26731,5.08819724887706,3.27997606150962));
#66867=CARTESIAN_POINT('Ctrl Pts',(55.26731,4.98381076759098,3.41465759654846));
#66868=CARTESIAN_POINT('Ctrl Pts',(55.26731,4.88303664984125,3.54467838758864));
#66869=CARTESIAN_POINT('Ctrl Pts',(55.26731,4.77694582819166,3.6706618191179));
#66870=CARTESIAN_POINT('Ctrl Pts',(55.26731,4.66578001467949,3.79225854630936));
#66871=CARTESIAN_POINT('Ctrl Pts',(55.26731,4.58240565454537,3.88345609170295));
#66872=CARTESIAN_POINT('Ctrl Pts',(55.26731,4.49617597963476,3.97218543802049));
#66873=CARTESIAN_POINT('Ctrl Pts',(55.26731,4.40718462220901,4.05828393055008));
#66874=CARTESIAN_POINT('Ctrl Pts',(55.26731,4.386430352664,4.07836353572824));
#66875=CARTESIAN_POINT('Ctrl Pts',(55.26731,4.36552584907783,4.09829998793731));
#66876=CARTESIAN_POINT('Ctrl Pts',(55.26731,4.34447225403319,4.118091110524));
#66877=CARTESIAN_POINT('Ctrl Pts',(55.26731,4.32939733162735,4.13226206976808));
#66878=CARTESIAN_POINT('Ctrl Pts',(55.26731,4.314246538133,4.14635792301651));
#66879=CARTESIAN_POINT('Ctrl Pts',(55.26731,4.29903007439866,4.16036906530759));
#66880=CARTESIAN_POINT('Ctrl Pts',(55.26731,4.17560888326235,4.2740138582724));
#66881=CARTESIAN_POINT('Ctrl Pts',(55.26731,4.04770434386886,4.3822455413649));
#66882=CARTESIAN_POINT('Ctrl Pts',(55.26731,3.91561946318572,4.48475177730016));
#66883=CARTESIAN_POINT('Ctrl Pts',(55.26731,3.79417535715088,4.57900009793888));
#66884=CARTESIAN_POINT('Ctrl Pts',(55.26731,3.66919656977907,4.66840821575284));
#66885=CARTESIAN_POINT('Ctrl Pts',(55.26731,3.54089521629959,4.75270229533564));
#66886=CARTESIAN_POINT('Ctrl Pts',(55.26731,3.40098928201791,4.84462059267715));
#66887=CARTESIAN_POINT('Ctrl Pts',(55.26731,3.2571322026833,4.93045873435785));
#66888=CARTESIAN_POINT('Ctrl Pts',(55.26731,3.10975766305844,5.01005242618096));
#66889=CARTESIAN_POINT('Ctrl Pts',(55.26731,2.96307989452868,5.08926980752361));
#66890=CARTESIAN_POINT('Ctrl Pts',(55.26731,2.81291710565447,5.16230182142269));
#66891=CARTESIAN_POINT('Ctrl Pts',(55.26731,2.65968537241045,5.22893643335111));
#66892=CARTESIAN_POINT('Ctrl Pts',(55.26731,2.5865649781927,5.26073369224521));
#66893=CARTESIAN_POINT('Ctrl Pts',(55.26731,2.51274565898121,5.29107345515416));
#66894=CARTESIAN_POINT('Ctrl Pts',(55.26731,2.43827244344798,5.31992845289072));
#66895=CARTESIAN_POINT('Ctrl Pts',(55.26731,2.41937185972979,5.32725157297495));
#66896=CARTESIAN_POINT('Ctrl Pts',(55.26731,2.40042679525609,5.33447993108298));
#66897=CARTESIAN_POINT('Ctrl Pts',(55.26731,2.38144583174371,5.34161011482402));
#66898=CARTESIAN_POINT('Ctrl Pts',(55.26731,2.22683096477766,5.39969106576447));
#66899=CARTESIAN_POINT('Ctrl Pts',(55.26731,2.07011540008946,5.45115874666631));
#66900=CARTESIAN_POINT('Ctrl Pts',(55.26731,1.911728292796,5.49589861617376));
#66901=CARTESIAN_POINT('Ctrl Pts',(55.26731,1.75351066848805,5.54059061154054));
#66902=CARTESIAN_POINT('Ctrl Pts',(55.26731,1.59362433851506,5.57856935937553));
#66903=CARTESIAN_POINT('Ctrl Pts',(55.26731,1.43248375220305,5.60967057749581));
#66904=CARTESIAN_POINT('Ctrl Pts',(55.26731,1.27339371223188,5.64037602636594));
#66905=CARTESIAN_POINT('Ctrl Pts',(55.26731,1.11308044188337,5.66437794116206));
#66906=CARTESIAN_POINT('Ctrl Pts',(55.26731,0.951940409530166,5.6814676859131));
#66907=CARTESIAN_POINT('Ctrl Pts',(55.26731,0.907459779355754,5.68618508980675));
#66908=CARTESIAN_POINT('Ctrl Pts',(55.26731,0.862916172292719,5.69037550710057));
#66909=CARTESIAN_POINT('Ctrl Pts',(55.26731,0.818318002073663,5.69403384682366));
#66910=CARTESIAN_POINT('Ctrl Pts',(55.26731,0.701153467936443,5.70364472698457));
#66911=CARTESIAN_POINT('Ctrl Pts',(55.26731,0.583612054961453,5.70958425773096));
#66912=CARTESIAN_POINT('Ctrl Pts',(55.26731,0.465862065703461,5.71186041381545));
#66913=CARTESIAN_POINT('Ctrl Pts',(55.26731,0.41434644540309,5.71285623210241));
#66914=CARTESIAN_POINT('Ctrl Pts',(55.26731,0.362790955096401,5.71315068969682));
#66915=CARTESIAN_POINT('Ctrl Pts',(55.26731,0.311209982030667,5.71274368078609));
#66916=CARTESIAN_POINT('Ctrl Pts',(55.26731,0.27708871341108,5.71247444080188));
#66917=CARTESIAN_POINT('Ctrl Pts',(55.26731,0.242956297684031,5.71189823375274));
#66918=CARTESIAN_POINT('Ctrl Pts',(55.26731,0.208816953097745,5.71101491794674));
#66919=CARTESIAN_POINT('Ctrl Pts',(55.26731,0.188374788502713,5.71048600073071));
#66920=CARTESIAN_POINT('Ctrl Pts',(55.26731,0.167930440883001,5.70984692698787));
#66921=CARTESIAN_POINT('Ctrl Pts',(55.26731,0.147498859806081,5.70909832637494));
#66922=CARTESIAN_POINT('Ctrl Pts',(55.26731,-0.0137838547239354,5.70318902652697));
#66923=CARTESIAN_POINT('Ctrl Pts',(55.26731,-0.174494943653233,5.69045414521296));
#66924=CARTESIAN_POINT('Ctrl Pts',(55.26731,-0.33421189439968,5.67101179972101));
#66925=CARTESIAN_POINT('Ctrl Pts',(55.26731,-0.494670179165839,5.65147921163383));
#66926=CARTESIAN_POINT('Ctrl Pts',(55.26731,-0.654125821445795,5.62517659128013));
#66927=CARTESIAN_POINT('Ctrl Pts',(55.26731,-0.81214282132803,5.59217212346982));
#66928=CARTESIAN_POINT('Ctrl Pts',(55.26731,-0.969071547367172,5.55939495967776));
#66929=CARTESIAN_POINT('Ctrl Pts',(55.26731,-1.12458207397616,5.52000770889059));
#66930=CARTESIAN_POINT('Ctrl Pts',(55.26731,-1.27822915468614,5.4740294698342));
#66931=CARTESIAN_POINT('Ctrl Pts',(55.26731,-1.42877972365552,5.42897784881958));
#66932=CARTESIAN_POINT('Ctrl Pts',(55.26731,-1.57754176552956,5.37759792723356));
#66933=CARTESIAN_POINT('Ctrl Pts',(55.26731,-1.72406969420736,5.31986579039788));
#66934=CARTESIAN_POINT('Ctrl Pts',(55.26731,-1.79587686650099,5.29157369936754));
#66935=CARTESIAN_POINT('Ctrl Pts',(55.26731,-1.86714703849359,5.26175546467072));
#66936=CARTESIAN_POINT('Ctrl Pts',(55.26731,-1.93782473268728,5.23040479991611));
#66937=CARTESIAN_POINT('Ctrl Pts',(18.4587229554446,-2.48002491540308,4.99617608622634));
#66938=CARTESIAN_POINT('Ctrl Pts',(18.4922462587639,-3.30865498737451,4.58485687155599));
#66939=CARTESIAN_POINT('Ctrl Pts',(18.5592928654024,-4.7565022034365,3.3424227331334));
#66940=CARTESIAN_POINT('Ctrl Pts',(18.6598627753602,-5.77493526257405,0.666469965513239));
#66941=CARTESIAN_POINT('Ctrl Pts',(18.760432685318,-5.39287434860188,-2.17036838028292));
#66942=CARTESIAN_POINT('Ctrl Pts',(18.8610025952758,-3.7030871350563,-4.48125359415228));
#66943=CARTESIAN_POINT('Ctrl Pts',(18.9615725052336,-1.1152833298924,-5.70525647060629));
#66944=CARTESIAN_POINT('Ctrl Pts',(19.0621424151914,1.74296490233074,-5.54583252750879));
#66945=CARTESIAN_POINT('Ctrl Pts',(19.1627123251492,4.17855117605108,-4.04150148361096));
#66946=CARTESIAN_POINT('Ctrl Pts',(19.263282235107,5.60083956100377,-1.55713407092352));
#66947=CARTESIAN_POINT('Ctrl Pts',(19.3638521450648,5.66493061750189,1.30484940988588));
#66948=CARTESIAN_POINT('Ctrl Pts',(19.4644220550226,4.35528013812923,3.85040169824184));
#66949=CARTESIAN_POINT('Ctrl Pts',(19.5649919649805,1.98947835131264,5.4622381255191));
#66950=CARTESIAN_POINT('Ctrl Pts',(19.6655618749382,-0.858770415672562,
5.74948485589373));
#66951=CARTESIAN_POINT('Ctrl Pts',(19.766131784896,-3.49876799771652,4.64248730288639));
#66952=CARTESIAN_POINT('Ctrl Pts',(19.8667016948538,-5.29031740242813,2.40969014364539));
#66953=CARTESIAN_POINT('Ctrl Pts',(19.9672716048116,-5.79896936542072,-0.407454580540862));
#66954=CARTESIAN_POINT('Ctrl Pts',(20.0678415147694,-4.90137626234256,-3.12579203238712));
#66955=CARTESIAN_POINT('Ctrl Pts',(20.1684114247273,-2.81520362818565,-5.08612754957154));
#66956=CARTESIAN_POINT('Ctrl Pts',(20.268981334685,-0.0463465410280725,
-5.81308154368905));
#66957=CARTESIAN_POINT('Ctrl Pts',(20.3695512446429,2.73374954418304,-5.13036825249749));
#66958=CARTESIAN_POINT('Ctrl Pts',(20.4701211546007,4.85091371732528,-3.20354508412377));
#66959=CARTESIAN_POINT('Ctrl Pts',(20.5706910645585,5.79173549027881,-0.499864986629304));
#66960=CARTESIAN_POINT('Ctrl Pts',(20.6712609745162,5.32806639229823,2.32503193781961));
#66961=CARTESIAN_POINT('Ctrl Pts',(20.7718308844741,3.57234578085699,4.58611061982589));
#66962=CARTESIAN_POINT('Ctrl Pts',(20.8724007944319,0.950334392674663,5.73506142385651));
#66963=CARTESIAN_POINT('Ctrl Pts',(20.9729707043897,-1.90213226762502,5.4932647697747));
#66964=CARTESIAN_POINT('Ctrl Pts',(21.0735406143475,-4.29333349045155,3.91935613764576));
#66965=CARTESIAN_POINT('Ctrl Pts',(21.1741105243052,-5.64340503766005,1.39500701610168));
#66966=CARTESIAN_POINT('Ctrl Pts',(21.2746804342631,-5.62495572124505,-1.46763010602068));
#66967=CARTESIAN_POINT('Ctrl Pts',(21.3752503442208,-4.24245948454918,-3.97436819079288));
#66968=CARTESIAN_POINT('Ctrl Pts',(21.4758202541787,-1.83117047488202,-5.51732541055725));
#66969=CARTESIAN_POINT('Ctrl Pts',(21.5763901641365,1.02417579862052,-5.72233596772863));
#66970=CARTESIAN_POINT('Ctrl Pts',(21.6769600740943,3.6311603225972,-4.53968497867921));
#66971=CARTESIAN_POINT('Ctrl Pts',(21.7775299840521,5.35759159415115,-2.25616429018983));
#66972=CARTESIAN_POINT('Ctrl Pts',(21.8780998940099,5.78481151609187,0.574474296499018));
#66973=CARTESIAN_POINT('Ctrl Pts',(21.9786698039677,4.809219625112,3.26580336081112));
#66974=CARTESIAN_POINT('Ctrl Pts',(22.0792397139255,2.66739611495663,5.16517792142356));
#66975=CARTESIAN_POINT('Ctrl Pts',(22.1798096238833,-0.121268656904642,
5.81200128242416));
#66976=CARTESIAN_POINT('Ctrl Pts',(22.2803795338411,-2.88052588385809,5.04941933557423));
#66977=CARTESIAN_POINT('Ctrl Pts',(22.3809494437989,-4.94125806361523,3.06235754653254));
#66978=CARTESIAN_POINT('Ctrl Pts',(22.4815193537567,-5.80373941652232,0.332676688621903));
#66979=CARTESIAN_POINT('Ctrl Pts',(22.5820892637145,-5.25881895694809,-2.4776779799019));
#66980=CARTESIAN_POINT('Ctrl Pts',(22.6826591736723,-3.43863942725612,-4.68719787115575));
#66981=CARTESIAN_POINT('Ctrl Pts',(22.7832290836301,-0.78459279653397,-5.7600763135287));
#66982=CARTESIAN_POINT('Ctrl Pts',(22.8837989935879,2.05971691194769,-5.4361412083098));
#66983=CARTESIAN_POINT('Ctrl Pts',(22.9843689035457,4.40454704234543,-3.79394653966204));
#66984=CARTESIAN_POINT('Ctrl Pts',(23.0849388135035,5.68127830653479,-1.2317231010842));
#66985=CARTESIAN_POINT('Ctrl Pts',(23.1855087234613,5.58030447199677,1.62919212920396));
#66986=CARTESIAN_POINT('Ctrl Pts',(23.2860786334191,4.12611160668567,4.09502967061549));
#66987=CARTESIAN_POINT('Ctrl Pts',(23.3866485433769,1.67134022862849,5.56782604202173));
#66988=CARTESIAN_POINT('Ctrl Pts',(23.4872184533347,-1.1887297161335,5.69042939118205));
#66989=CARTESIAN_POINT('Ctrl Pts',(23.5877883632925,-3.76053372802574,4.43310851146552));
#66990=CARTESIAN_POINT('Ctrl Pts',(23.6883582732503,-5.42041154804703,2.10076263386556));
#66991=CARTESIAN_POINT('Ctrl Pts',(23.7889281832081,-5.76584423371262,-0.741016374050092));
#66992=CARTESIAN_POINT('Ctrl Pts',(23.8894980931659,-4.71306465610696,-3.40309954914673));
#66993=CARTESIAN_POINT('Ctrl Pts',(23.9900680031237,-2.51737095653659,-5.23993401306099));
#66994=CARTESIAN_POINT('Ctrl Pts',(24.0906379130815,0.288783032968795,-5.80608898949342));
#66995=CARTESIAN_POINT('Ctrl Pts',(24.1912078230393,3.02490738557195,-4.9642723840216));
#66996=CARTESIAN_POINT('Ctrl Pts',(24.2917777329971,5.02749430110096,-2.91862399881259));
#66997=CARTESIAN_POINT('Ctrl Pts',(24.3923476429549,5.81091817642424,-0.165211806326761));
#66998=CARTESIAN_POINT('Ctrl Pts',(24.4929175529127,5.18519939616966,2.62826410697425));
#66999=CARTESIAN_POINT('Ctrl Pts',(24.5934874628705,3.30207422591229,4.78438823681912));
#67000=CARTESIAN_POINT('Ctrl Pts',(24.6940573728283,0.618198898391366,5.78030233777395));
#67001=CARTESIAN_POINT('Ctrl Pts',(24.7946272827861,-2.21558912982611,5.37449809766863));
#67002=CARTESIAN_POINT('Ctrl Pts',(24.895197192744,-4.51209870130343,3.66538269540076));
#67003=CARTESIAN_POINT('Ctrl Pts',(24.9957671027017,-5.71442822185861,1.06741514476474));
#67004=CARTESIAN_POINT('Ctrl Pts',(25.0963370126596,-5.53101381775679,-1.78939965961516));
#67005=CARTESIAN_POINT('Ctrl Pts',(25.1969069226173,-4.00633332410426,-4.21228658690491));
#67006=CARTESIAN_POINT('Ctrl Pts',(25.2974768325751,-1.51012044812308,-5.61369764292733));
#67007=CARTESIAN_POINT('Ctrl Pts',(25.3980467425329,1.35229533657296,-5.65379185297181));
#67008=CARTESIAN_POINT('Ctrl Pts',(25.4986166524907,3.88678066624468,-4.32284640561678));
#67009=CARTESIAN_POINT('Ctrl Pts',(25.5991865624485,5.47872503020431,-1.94361442612985));
#67010=CARTESIAN_POINT('Ctrl Pts',(25.6997564724064,5.74208329058304,0.906942378574534));
#67011=CARTESIAN_POINT('Ctrl Pts',(25.8003263823641,4.61299129594534,3.53756643719661));
#67012=CARTESIAN_POINT('Ctrl Pts',(25.900896292322,2.3652528830361,5.31033368003713));
#67013=CARTESIAN_POINT('Ctrl Pts',(26.0014662022797,-0.456057317931881,
5.79534957675619));
#67014=CARTESIAN_POINT('Ctrl Pts',(26.1020361122375,-3.1667740118886,4.87499818991498));
#67015=CARTESIAN_POINT('Ctrl Pts',(26.2026060221954,-5.10955073401222,2.77246393855764));
#67016=CARTESIAN_POINT('Ctrl Pts',(26.3031759321531,-5.81326580158569,-0.00239043128346468));
#67017=CARTESIAN_POINT('Ctrl Pts',(26.403745842111,-5.10726891650053,-2.77666512359608));
#67018=CARTESIAN_POINT('Ctrl Pts',(26.5043157520687,-3.16276371564756,-4.87760091366961));
#67019=CARTESIAN_POINT('Ctrl Pts',(26.6048856620266,-0.451291036347756,
-5.79572268095701));
#67020=CARTESIAN_POINT('Ctrl Pts',(26.7054555719843,2.36961933078211,-5.30838668723663));
#67021=CARTESIAN_POINT('Ctrl Pts',(26.8060254819422,4.61589905003359,-3.53377149147286));
#67022=CARTESIAN_POINT('Ctrl Pts',(26.9065953918999,5.74282722315021,-0.902219750998773));
#67023=CARTESIAN_POINT('Ctrl Pts',(27.0071653018578,5.47712473824325,1.94811950243589));
#67024=CARTESIAN_POINT('Ctrl Pts',(27.1077352118156,3.88322421917838,4.32604145352698));
#67025=CARTESIAN_POINT('Ctrl Pts',(27.2083051217733,1.34764516975351,5.65490207611833));
#67026=CARTESIAN_POINT('Ctrl Pts',(27.3088750317312,-1.51473667324498,5.61245381315286));
#67027=CARTESIAN_POINT('Ctrl Pts',(27.409444941689,-4.00979617691032,4.20899033185902));
#67028=CARTESIAN_POINT('Ctrl Pts',(27.5100148516468,-5.53248355942245,1.78485031830896));
#67029=CARTESIAN_POINT('Ctrl Pts',(27.6105847616046,-5.71354844129516,-1.07211436098069));
#67030=CARTESIAN_POINT('Ctrl Pts',(27.7111546715624,-4.50908274454013,-3.66909223063931));
#67031=CARTESIAN_POINT('Ctrl Pts',(27.8117245815202,-2.21116836378188,-5.3763183928277));
#67032=CARTESIAN_POINT('Ctrl Pts',(27.912294491478,0.622952441756332,-5.77979197284445));
#67033=CARTESIAN_POINT('Ctrl Pts',(28.0128644014358,3.30600781642397,-4.78167097485711));
#67034=CARTESIAN_POINT('Ctrl Pts',(28.1134343113936,5.18735914151516,-2.62399888166641));
#67035=CARTESIAN_POINT('Ctrl Pts',(28.2140042213514,5.8107803402164,0.169990681514914));
#67036=CARTESIAN_POINT('Ctrl Pts',(28.3145741313092,5.02509230850153,2.92275765076171));
#67037=CARTESIAN_POINT('Ctrl Pts',(28.415144041267,3.02082371771862,4.96675840569238));
#67038=CARTESIAN_POINT('Ctrl Pts',(28.5157139512248,0.284007975800641,5.80632452277075));
#67039=CARTESIAN_POINT('Ctrl Pts',(28.6162838611826,-2.5216794557668,5.23786194132788));
#67040=CARTESIAN_POINT('Ctrl Pts',(28.7168537711404,-4.71586179004478,3.39922234801476));
#67041=CARTESIAN_POINT('Ctrl Pts',(28.8174236810982,-5.76645169978597,0.736274261456154));
#67042=CARTESIAN_POINT('Ctrl Pts',(28.917993591056,-5.41868203625607,-2.10521969969957));
#67043=CARTESIAN_POINT('Ctrl Pts',(29.0185635010138,-3.75688664349095,-4.43619969591165));
#67044=CARTESIAN_POINT('Ctrl Pts',(29.1191334109716,-1.18404947371506,-5.69140508467306));
#67045=CARTESIAN_POINT('Ctrl Pts',(29.2197033209294,1.67591867417301,-5.56644963972599));
#67046=CARTESIAN_POINT('Ctrl Pts',(29.3202732308872,4.12947798625297,-4.09163494890484));
#67047=CARTESIAN_POINT('Ctrl Pts',(29.420843140845,5.58164244143966,-1.62460230517097));
#67048=CARTESIAN_POINT('Ctrl Pts',(29.5214130508028,5.68026340941513,1.2363949990626));
#67049=CARTESIAN_POINT('Ctrl Pts',(29.6219829607606,4.40142539034105,3.79756758034778));
#67050=CARTESIAN_POINT('Ctrl Pts',(29.7225528707184,2.05524550298248,5.43783329245368));
#67051=CARTESIAN_POINT('Ctrl Pts',(29.8231227806762,-0.789329649635071,
5.75942911218241));
#67052=CARTESIAN_POINT('Ctrl Pts',(29.923692690634,-3.44249304169372,4.68436833008867));
#67053=CARTESIAN_POINT('Ctrl Pts',(30.0242626005918,-5.26085483453837,2.47335226038701));
#67054=CARTESIAN_POINT('Ctrl Pts',(30.1248325105496,-5.80346385870219,-0.337449603325932));
#67055=CARTESIAN_POINT('Ctrl Pts',(30.2254024205074,-4.93873789291885,-3.06642022871864));
#67056=CARTESIAN_POINT('Ctrl Pts',(30.3259723304652,-2.87637223950989,-5.05178658830954));
#67057=CARTESIAN_POINT('Ctrl Pts',(30.426542240423,-0.116488794083507,-5.81209904895815));
#67058=CARTESIAN_POINT('Ctrl Pts',(30.5271121503808,2.67164308363124,-5.16298249345597));
#67059=CARTESIAN_POINT('Ctrl Pts',(30.6276820603386,4.81190381339239,-3.26184712773408));
#67060=CARTESIAN_POINT('Ctrl Pts',(30.7282519702964,5.78528201063068,-0.569716641428254));
#67061=CARTESIAN_POINT('Ctrl Pts',(30.8288218802542,5.35573430042772,2.26056963999551));
#67062=CARTESIAN_POINT('Ctrl Pts',(30.929391790212,3.62742563274069,4.54266972968354));
#67063=CARTESIAN_POINT('Ctrl Pts',(31.0299617001698,1.01946937170607,5.72317632038368));
#67064=CARTESIAN_POINT('Ctrl Pts',(31.1305316101276,-1.8357073343788,5.51581758006511));
#67065=CARTESIAN_POINT('Ctrl Pts',(31.2311015200854,-4.24572659210633,3.97087782475468));
#67066=CARTESIAN_POINT('Ctrl Pts',(31.3316714300432,-5.62616080609128,1.46300361518679));
#67067=CARTESIAN_POINT('Ctrl Pts',(31.4322413400011,-5.64225586775969,-1.39964771166842));
#67068=CARTESIAN_POINT('Ctrl Pts',(31.5328112499588,-4.29010873851205,-3.92288567330096));
#67069=CARTESIAN_POINT('Ctrl Pts',(31.6333811599166,-1.89761393322384,-5.49482723609051));
#67070=CARTESIAN_POINT('Ctrl Pts',(31.7339510698744,0.955050617350668,-5.73427792423296));
#67071=CARTESIAN_POINT('Ctrl Pts',(31.8345209798323,3.57611621535257,-4.58317115197979));
#67072=CARTESIAN_POINT('Ctrl Pts',(31.93509088979,5.32997670955485,-2.32064932069671));
#67073=CARTESIAN_POINT('Ctrl Pts',(32.0356607997479,5.79132243988692,0.504627973173819));
#67074=CARTESIAN_POINT('Ctrl Pts',(32.1362307097056,4.84827746388286,3.20753341794796));
#67075=CARTESIAN_POINT('Ctrl Pts',(32.2368006196635,2.72952937642347,5.13261477000649));
#67076=CARTESIAN_POINT('Ctrl Pts',(32.3373705296212,-0.051127235161469,
5.8130414586404));
#67077=CARTESIAN_POINT('Ctrl Pts',(32.4379404395791,-2.81938553623152,5.0838105975868));
#67078=CARTESIAN_POINT('Ctrl Pts',(32.5385103495368,-4.90394527177332,3.12176004290838));
#67079=CARTESIAN_POINT('Ctrl Pts',(32.6390802594946,-5.79930250036685,0.402685365125275));
#67080=CARTESIAN_POINT('Ctrl Pts',(32.7396501694525,-5.28833386482735,-2.41404016705763));
#67081=CARTESIAN_POINT('Ctrl Pts',(32.8402200794103,-3.49494881941665,-4.64536303680407));
#67082=CARTESIAN_POINT('Ctrl Pts',(32.940789989368,-0.854041693849599,-5.75018936898723));
#67083=CARTESIAN_POINT('Ctrl Pts',(33.0413598993259,1.99396980729241,-5.46059972911893));
#67084=CARTESIAN_POINT('Ctrl Pts',(33.1419298092837,4.35844534663238,-3.8468193555801));
#67085=CARTESIAN_POINT('Ctrl Pts',(33.2424997192414,5.66600164128877,-1.30018859976555));
#67086=CARTESIAN_POINT('Ctrl Pts',(33.3430696291993,5.59955741538933,1.56173677225253));
#67087=CARTESIAN_POINT('Ctrl Pts',(33.443639539157,4.17522533651758,4.04494232138717));
#67088=CARTESIAN_POINT('Ctrl Pts',(33.5442094491149,1.73840470769403,5.54725283958776));
#67089=CARTESIAN_POINT('Ctrl Pts',(33.6447793590727,-1.1199775662767,5.70435931942268));
#67090=CARTESIAN_POINT('Ctrl Pts',(33.7453492690304,-3.70676624453413,4.47816357477366));
#67091=CARTESIAN_POINT('Ctrl Pts',(33.8459191789883,-5.39466729938273,2.16601701817368));
#67092=CARTESIAN_POINT('Ctrl Pts',(33.9464890889461,-5.77436617801534,-0.67138680076386));
#67093=CARTESIAN_POINT('Ctrl Pts',(34.0470589989039,-4.75378622921922,-3.34597989846517));
#67094=CARTESIAN_POINT('Ctrl Pts',(34.1476289088617,-2.58041721203297,-5.20917575110413));
#67095=CARTESIAN_POINT('Ctrl Pts',(34.2481988188195,0.218700757774141,-5.80915096830823));
#67096=CARTESIAN_POINT('Ctrl Pts',(34.3487687287773,2.96478398208491,-5.00041207638131));
#67097=CARTESIAN_POINT('Ctrl Pts',(34.4493386387351,4.99190964291116,-2.97907756043006));
#67098=CARTESIAN_POINT('Ctrl Pts',(34.5499085486929,5.80850151251044,-0.235319300549913));
#67099=CARTESIAN_POINT('Ctrl Pts',(34.6504784586507,5.21653676545061,2.56550368714399));
#67100=CARTESIAN_POINT('Ctrl Pts',(34.7510483686085,3.35956634331347,4.74419423916461));
#67101=CARTESIAN_POINT('Ctrl Pts',(34.8516182785663,0.687903974933855,5.7724217721263));
#67102=CARTESIAN_POINT('Ctrl Pts',(34.952188188524,-2.15057451519974,5.40084199441352));
#67103=CARTESIAN_POINT('Ctrl Pts',(35.0527580984819,-4.46754053667362,3.71956268225518));
#67104=CARTESIAN_POINT('Ctrl Pts',(35.1533280084396,-5.70113182379116,1.13629262155616));
#67105=CARTESIAN_POINT('Ctrl Pts',(35.2538979183975,-5.55220355133712,-1.72252742171694));
#67106=CARTESIAN_POINT('Ctrl Pts',(35.3544678283553,-4.05687069717986,-4.16363604802468));
#67107=CARTESIAN_POINT('Ctrl Pts',(35.4550377383131,-1.57775019122715,-5.59506651686378));
#67108=CARTESIAN_POINT('Ctrl Pts',(35.5556076482709,1.28397337792556,-5.66969817175709));
#67109=CARTESIAN_POINT('Ctrl Pts',(35.6561775582287,3.83433450821241,-4.36943290063812));
#67110=CARTESIAN_POINT('Ctrl Pts',(35.7567474681865,5.45487282096287,-2.00958391244754));
#67111=CARTESIAN_POINT('Ctrl Pts',(35.8573173781443,5.75260917034078,0.837587444604104));
#67112=CARTESIAN_POINT('Ctrl Pts',(35.9578872881021,4.65534274792201,3.48164456735854));
#67113=CARTESIAN_POINT('Ctrl Pts',(36.05845719806,2.4291597165847,5.28140587962803));
#67114=CARTESIAN_POINT('Ctrl Pts',(36.1590271080177,-0.386092454934063,
5.80043081247336));
#67115=CARTESIAN_POINT('Ctrl Pts',(36.2595970179756,-3.10771753849076,4.91285626647109));
#67116=CARTESIAN_POINT('Ctrl Pts',(36.3601669279333,-5.07572379417585,2.83391830497715));
#67117=CARTESIAN_POINT('Ctrl Pts',(36.4607368378912,-5.81287139910188,0.0677575940443941));
#67118=CARTESIAN_POINT('Ctrl Pts',(36.5613067478488,-5.14040269363212,-2.71483427511641));
#67119=CARTESIAN_POINT('Ctrl Pts',(36.6618766578068,-3.22139075996267,-4.83908116956871));
#67120=CARTESIAN_POINT('Ctrl Pts',(36.7624465677644,-0.5211943400678,-5.78985504602047));
#67121=CARTESIAN_POINT('Ctrl Pts',(36.8630164777224,2.30539125863451,-5.33659405788552));
#67122=CARTESIAN_POINT('Ctrl Pts',(36.9635863876801,4.57292146166484,-3.58921360460651));
#67123=CARTESIAN_POINT('Ctrl Pts',(37.064156297638,5.73152214674337,-0.97145194190844));
#67124=CARTESIAN_POINT('Ctrl Pts',(37.1647262075957,5.50023364509525,1.88188598044871));
#67125=CARTESIAN_POINT('Ctrl Pts',(37.2652961175536,3.93514321927045,4.27886817252847));
#67126=CARTESIAN_POINT('Ctrl Pts',(37.3658660275113,1.41578395025668,5.63822851614255));
#67127=CARTESIAN_POINT('Ctrl Pts',(37.4664359374691,-1.44690170794694,5.63032329814084));
#67128=CARTESIAN_POINT('Ctrl Pts',(37.5670058474269,-3.9587149475079,4.25706952708373));
#67129=CARTESIAN_POINT('Ctrl Pts',(37.6675757573847,-5.51054322007353,1.85148006031634));
#67130=CARTESIAN_POINT('Ctrl Pts',(37.7681456673425,-5.72606950540495,-1.00309172727058));
#67131=CARTESIAN_POINT('Ctrl Pts',(37.8687155773003,-4.55302886484057,-3.61441463448453));
#67132=CARTESIAN_POINT('Ctrl Pts',(37.9692854872581,-2.27588264393015,-5.34924510422778));
#67133=CARTESIAN_POINT('Ctrl Pts',(38.0698553972159,0.553163158988311,-5.78688824097939));
#67134=CARTESIAN_POINT('Ctrl Pts',(38.1704253071738,3.24806737203082,-4.82121596081281));
#67135=CARTESIAN_POINT('Ctrl Pts',(38.2709952171315,5.15531804338536,-2.6864029603901));
#67136=CARTESIAN_POINT('Ctrl Pts',(38.3715651270894,5.81240852706456,0.0998604453944716));
#67137=CARTESIAN_POINT('Ctrl Pts',(38.4721350370471,5.0599949464186,2.86190777913362));
#67138=CARTESIAN_POINT('Ctrl Pts',(38.572704947005,3.08053694705489,4.92994494004518));
#67139=CARTESIAN_POINT('Ctrl Pts',(38.6732748569627,0.354051389844875,5.80247469683378));
#67140=CARTESIAN_POINT('Ctrl Pts',(38.7738447669205,-2.45829132462492,5.26790933457678));
#67141=CARTESIAN_POINT('Ctrl Pts',(38.8744146768784,-4.67450050904083,3.45588049345234));
#67142=CARTESIAN_POINT('Ctrl Pts',(38.9749845868361,-5.75714734395841,0.80580360758677));
#67143=CARTESIAN_POINT('Ctrl Pts',(39.075554496794,-5.44369090388365,-2.03967995945972));
#67144=CARTESIAN_POINT('Ctrl Pts',(39.1761244067517,-3.81014410570237,-4.39054289215228));
#67145=CARTESIAN_POINT('Ctrl Pts',(39.2766943167096,-1.25264064176956,-5.67670295300313));
#67146=CARTESIAN_POINT('Ctrl Pts',(39.3772642266673,1.60862709948338,-5.58626743441943));
#67147=CARTESIAN_POINT('Ctrl Pts',(39.4778341366252,4.07980415386393,-4.14116687180823));
#67148=CARTESIAN_POINT('Ctrl Pts',(39.578404046583,5.5616322129449,-1.69183690761873));
#67149=CARTESIAN_POINT('Ctrl Pts',(39.6789739565408,5.69476924799924,1.16776205028657));
#67150=CARTESIAN_POINT('Ctrl Pts',(39.7795438664986,4.44692964263445,3.74417971624045));
#67151=CARTESIAN_POINT('Ctrl Pts',(39.8801137764563,2.12071342697536,5.41263702410329));
#67152=CARTESIAN_POINT('Ctrl Pts',(39.9806836864142,-0.719773969154297,
5.76853451297425));
#67153=CARTESIAN_POINT('Ctrl Pts',(40.081253596372,-3.38571679736614,4.72556734816892));
#67154=CARTESIAN_POINT('Ctrl Pts',(40.1818235063298,-5.23062621673878,2.5366541693365));
#67155=CARTESIAN_POINT('Ctrl Pts',(40.2823934162876,-5.80711328122534,-0.267395461935357));
#67156=CARTESIAN_POINT('Ctrl Pts',(40.3829633262454,-4.9753803739444,-3.00660192386958));
#67157=CARTESIAN_POINT('Ctrl Pts',(40.4835332362031,-2.93712200893205,-5.01671000743458));
#67158=CARTESIAN_POINT('Ctrl Pts',(40.584103146161,-0.186614085112543,-5.81027023272455));
#67159=CARTESIAN_POINT('Ctrl Pts',(40.6846730561188,2.609147593704,-5.19484492822605));
#67160=CARTESIAN_POINT('Ctrl Pts',(40.7852429660765,4.7721932270764,-3.31967420050424));
#67161=CARTESIAN_POINT('Ctrl Pts',(40.8858128760344,5.77798611092356,-0.639485336830895));
#67162=CARTESIAN_POINT('Ctrl Pts',(40.9863827859921,5.38262233672791,2.19577817053662));
#67163=CARTESIAN_POINT('Ctrl Pts',(41.08695269595,3.6819772793914,4.49856736173782));
#67164=CARTESIAN_POINT('Ctrl Pts',(41.1875226059078,1.08845590135412,5.7104578402134));
#67165=CARTESIAN_POINT('Ctrl Pts',(41.2880925158656,-1.76901509578748,5.53756720816311));
#67166=CARTESIAN_POINT('Ctrl Pts',(41.3886624258233,-4.19750145501954,4.02182129502992));
#67167=CARTESIAN_POINT('Ctrl Pts',(41.4892323357812,-5.608097324739,1.53078717995108));
#67168=CARTESIAN_POINT('Ctrl Pts',(41.589802245739,-5.65873442082026,-1.33146150852038));
#67169=CARTESIAN_POINT('Ctrl Pts',(41.6903721556968,-4.33713329105347,-3.87083192733591));
#67170=CARTESIAN_POINT('Ctrl Pts',(41.7909420656546,-1.96378107173494,-5.4715289358956));
#67171=CARTESIAN_POINT('Ctrl Pts',(41.8915119756124,0.88578636700025,-5.74538488754965));
#67172=CARTESIAN_POINT('Ctrl Pts',(41.9920818855702,3.52055137424819,-4.62598994976497));
#67173=CARTESIAN_POINT('Ctrl Pts',(42.0926517955281,5.30158570383253,-2.38479643134711));
#67174=CARTESIAN_POINT('Ctrl Pts',(42.1932217054858,5.7969900639945,0.434708168771271));
#67175=CARTESIAN_POINT('Ctrl Pts',(42.2937916154436,4.88662932385308,3.14879641217187));
#67176=CARTESIAN_POINT('Ctrl Pts',(42.3943615254014,2.79126517922797,5.09930423619505));
#67177=CARTESIAN_POINT('Ctrl Pts',(42.4949314353592,0.0190216314411856,
5.81323517256825));
#67178=CARTESIAN_POINT('Ctrl Pts',(42.595501345317,-2.75783464559572,5.11746158379321));
#67179=CARTESIAN_POINT('Ctrl Pts',(42.6960712552748,-4.86591839509884,3.18070796620598));
#67180=CARTESIAN_POINT('Ctrl Pts',(42.7966411652326,-5.79402112251256,0.472635404858439));
#67181=CARTESIAN_POINT('Ctrl Pts',(42.8972110751905,-5.31707871537652,-2.35005083530915));
#67182=CARTESIAN_POINT('Ctrl Pts',(42.9977809851481,-3.55074929685554,-4.60285177090544));
#67183=CARTESIAN_POINT('Ctrl Pts',(43.0983508951061,-0.923366230433899,
-5.73946511432395));
#67184=CARTESIAN_POINT('Ctrl Pts',(43.1989208050638,1.92793235200782,-5.48426310821507));
#67185=CARTESIAN_POINT('Ctrl Pts',(43.2994907150216,4.31170899870712,-3.89913201937502));
#67186=CARTESIAN_POINT('Ctrl Pts',(43.4000606249794,5.64989992486267,-1.36846477232117));
#67187=CARTESIAN_POINT('Ctrl Pts',(43.5006305349373,5.61799498283493,1.49405400400684));
#67188=CARTESIAN_POINT('Ctrl Pts',(43.601200444895,4.22373109360091,3.99426597048771));
#67189=CARTESIAN_POINT('Ctrl Pts',(43.7017703548528,1.80521605007753,5.52587187750403));
#67190=CARTESIAN_POINT('Ctrl Pts',(43.8023402648106,-1.05106233160792,5.71745861105458));
#67191=CARTESIAN_POINT('Ctrl Pts',(43.9029101747684,-3.65245900266303,4.52256655317676));
#67192=CARTESIAN_POINT('Ctrl Pts',(44.0034800847262,-5.36813750971383,2.23095599930855));
#67193=CARTESIAN_POINT('Ctrl Pts',(44.104049994684,-5.78204729170571,-0.601659463921077));
#67194=CARTESIAN_POINT('Ctrl Pts',(44.2046199046419,-4.79381558281113,-3.28837302507556));
#67195=CARTESIAN_POINT('Ctrl Pts',(44.3051898145996,-2.64308772173875,-5.17765895837504));
#67196=CARTESIAN_POINT('Ctrl Pts',(44.4057597245574,0.148586636609559,-5.81136705134586));
#67197=CARTESIAN_POINT('Ctrl Pts',(44.5063296345153,2.90422886348763,-5.03582363695677));
#67198=CARTESIAN_POINT('Ctrl Pts',(44.606899544473,4.95559809101348,-3.03909732558712));
#67199=CARTESIAN_POINT('Ctrl Pts',(44.7074694544309,5.80523904738957,-0.305392528904701));
#67200=CARTESIAN_POINT('Ctrl Pts',(44.8080393643886,5.24711453208993,2.50236969314653));
#67201=CARTESIAN_POINT('Ctrl Pts',(44.9086092743465,3.41656925962507,4.70330941872129));
#67202=CARTESIAN_POINT('Ctrl Pts',(45.0091791843043,0.757508882781974,5.76370065899971));
#67203=CARTESIAN_POINT('Ctrl Pts',(45.109749094262,-2.08524674605032,5.42639945102955));
#67204=CARTESIAN_POINT('Ctrl Pts',(45.2103190042198,-4.42233183400564,3.77320104738504));
#67205=CARTESIAN_POINT('Ctrl Pts',(45.3108889141777,-5.68700525908472,1.20500463782932));
#67206=CARTESIAN_POINT('Ctrl Pts',(45.4114588241355,-5.57258480437296,-1.65540435909754));
#67207=CARTESIAN_POINT('Ctrl Pts',(45.5120287340932,-4.1068173316415,-4.11437922396275));
#67208=CARTESIAN_POINT('Ctrl Pts',(45.6125986440511,-1.64515019125313,-5.57562066879259));
#67209=CARTESIAN_POINT('Ctrl Pts',(45.7131685540088,1.21546445432158,-5.68477890109438));
#67210=CARTESIAN_POINT('Ctrl Pts',(45.8137384639667,3.78133001603,-4.41538314350158));
#67211=CARTESIAN_POINT('Ctrl Pts',(45.9143083739244,5.43022630392851,-2.07526077449805));
#67212=CARTESIAN_POINT('Ctrl Pts',(46.0148782838823,5.76229738761891,0.768110545877321));
#67213=CARTESIAN_POINT('Ctrl Pts',(46.11544819384,4.69701631516247,3.42521572008903));
#67214=CARTESIAN_POINT('Ctrl Pts',(46.2160181037979,2.4927128296055,5.25170903070299));
#67215=CARTESIAN_POINT('Ctrl Pts',(46.3165880137556,-0.316071371332041,
5.80466742219323));
#67216=CARTESIAN_POINT('Ctrl Pts',(46.4171579237135,-3.04820853680487,4.94999896062587));
#67217=CARTESIAN_POINT('Ctrl Pts',(46.5177278336712,-5.04115775608791,2.89496001220778));
#67218=CARTESIAN_POINT('Ctrl Pts',(46.6182977436291,-5.81163055909281,0.13789575289385));
#67219=CARTESIAN_POINT('Ctrl Pts',(46.7188676535869,-5.17278795433587,-2.65260810779222));
#67220=CARTESIAN_POINT('Ctrl Pts',(46.8194375635447,-3.27954872353672,-4.79985678577976));
#67221=CARTESIAN_POINT('Ctrl Pts',(46.9200074735025,-0.591021750409563,
-5.78314432507005));
#67222=CARTESIAN_POINT('Ctrl Pts',(47.0205773834603,2.24082748842343,-5.36402434382742));
#67223=CARTESIAN_POINT('Ctrl Pts',(47.1211472934181,4.52927799028237,-3.64413307671263));
#67224=CARTESIAN_POINT('Ctrl Pts',(47.2217172033759,5.71938247843022,-1.04054267546927));
#67225=CARTESIAN_POINT('Ctrl Pts',(47.3222871133337,5.52254163896719,1.8153784288464));
#67226=CARTESIAN_POINT('Ctrl Pts',(47.4228570232915,3.98648920601686,4.23107182689664));
#67227=CARTESIAN_POINT('Ctrl Pts',(47.5234269332493,1.48371657229165,5.62073394915242));
#67228=CARTESIAN_POINT('Ctrl Pts',(47.6239968432071,-1.37885605298849,5.64737292722768));
#67229=CARTESIAN_POINT('Ctrl Pts',(47.7245667531649,-3.90705727237777,4.30452883187085));
#67230=CARTESIAN_POINT('Ctrl Pts',(47.8251366631227,-5.48780046652238,1.91784020024717));
#67231=CARTESIAN_POINT('Ctrl Pts',(47.9257065730805,-5.73775677159133,-0.933923029004594));
#67232=CARTESIAN_POINT('Ctrl Pts',(48.0262764830383,-4.59631199877497,-3.55921072767047));
#67233=CARTESIAN_POINT('Ctrl Pts',(48.1268463929962,-2.34026552289286,-5.32139288874693));
#67234=CARTESIAN_POINT('Ctrl Pts',(48.2274163029538,0.483293327723093,-5.79314185510984));
#67235=CARTESIAN_POINT('Ctrl Pts',(48.3279862129118,3.18965396239895,-4.8600589085113));
#67236=CARTESIAN_POINT('Ctrl Pts',(48.4285561228695,5.12252625693867,-2.74841586027683));
#67237=CARTESIAN_POINT('Ctrl Pts',(48.5291260328273,5.81319034378827,0.0297156681595752));
#67238=CARTESIAN_POINT('Ctrl Pts',(48.629695942785,5.09416077643017,2.80064117264737));
#67239=CARTESIAN_POINT('Ctrl Pts',(48.730265852743,3.13980160598745,4.89241360364045));
#67240=CARTESIAN_POINT('Ctrl Pts',(48.8308357627007,0.424043248924028,5.79777994728061));
#67241=CARTESIAN_POINT('Ctrl Pts',(48.9314056726585,-2.39454523097487,5.29718964460052));
#67242=CARTESIAN_POINT('Ctrl Pts',(49.0319755826163,-4.63245855365558,3.51203541307753));
#67243=CARTESIAN_POINT('Ctrl Pts',(49.1325454925742,-5.74700466482796,0.875215617144052));
#67244=CARTESIAN_POINT('Ctrl Pts',(49.2331154025319,-5.46790709196603,-1.97384321253615));
#67245=CARTESIAN_POINT('Ctrl Pts',(49.3336853124898,-3.86284675623355,-4.3442467623172));
#67246=CARTESIAN_POINT('Ctrl Pts',(49.4342552224475,-1.3210494073637,-5.66117421188848));
#67247=CARTESIAN_POINT('Ctrl Pts',(49.5348251324054,1.54110128559463,-5.60527178837798));
#67248=CARTESIAN_POINT('Ctrl Pts',(49.6353950423631,4.02953624342044,-4.19009578136448));
#67249=CARTESIAN_POINT('Ctrl Pts',(49.735964952321,5.54081213095715,-1.75882515432473));
#67250=CARTESIAN_POINT('Ctrl Pts',(49.8365348622786,5.70844584642674,1.09895905859165));
#67251=CARTESIAN_POINT('Ctrl Pts',(49.9371047722366,4.49178635813174,3.69024664581502));
#67252=CARTESIAN_POINT('Ctrl Pts',(50.0376746821943,2.18587254464829,5.38665259809838));
#67253=CARTESIAN_POINT('Ctrl Pts',(50.1382445921522,-0.650113479250571,
5.77679993232794));
#67254=CARTESIAN_POINT('Ctrl Pts',(50.2388145021098,-3.32844754406752,4.76607825580302));
#67255=CARTESIAN_POINT('Ctrl Pts',(50.3393844120678,-5.19963594467117,2.5995867050227));
#67256=CARTESIAN_POINT('Ctrl Pts',(50.4399543220255,-5.80991710468783,-0.197302383926823));
#67257=CARTESIAN_POINT('Ctrl Pts',(50.5405242319834,-5.01129836816094,-2.94634581461765));
#67258=CARTESIAN_POINT('Ctrl Pts',(50.6410941419411,-2.99744409122436,-4.98090292156266));
#67259=CARTESIAN_POINT('Ctrl Pts',(50.7416640518989,-0.256712202451727,
-5.80759535773281));
#67260=CARTESIAN_POINT('Ctrl Pts',(50.8422339618567,2.54627217443023,-5.2259509189974));
#67261=CARTESIAN_POINT('Ctrl Pts',(50.9428038718146,4.73178774091697,-3.37701788105352));
#67262=CARTESIAN_POINT('Ctrl Pts',(51.0433737817723,5.76984885348993,-0.709160913988021));
#67263=CARTESIAN_POINT('Ctrl Pts',(51.1439436917302,5.40872658594295,2.13066696425354));
#67264=CARTESIAN_POINT('Ctrl Pts',(51.2445136016879,3.73599277729174,4.45380993780282));
#67265=CARTESIAN_POINT('Ctrl Pts',(51.3450835116458,1.15728393619704,5.69690783540226));
#67266=CARTESIAN_POINT('Ctrl Pts',(51.4456534216035,-1.70206526320226,5.55851048697829));
#67267=CARTESIAN_POINT('Ctrl Pts',(51.5462233315614,-4.14866510146161,4.07217913038731));
#67268=CARTESIAN_POINT('Ctrl Pts',(51.6467932415191,-5.58921722390637,1.59834784012599));
#67269=CARTESIAN_POINT('Ctrl Pts',(51.747363151477,-5.67438898091241,-1.2630814254622));
#67270=CARTESIAN_POINT('Ctrl Pts',(51.8479330614348,-4.38352629472378,-3.81821453267259));
#67271=CARTESIAN_POINT('Ctrl Pts',(51.9485029713925,-2.02966225553008,-5.44743390253828));
#67272=CARTESIAN_POINT('Ctrl Pts',(52.0490728813504,0.816393133438721,-5.75565524034613));
#67273=CARTESIAN_POINT('Ctrl Pts',(52.1496427913082,3.46447389032224,-4.66813513700239));
#67274=CARTESIAN_POINT('Ctrl Pts',(52.250212701266,5.27242271112307,-2.44859628140164));
#67275=CARTESIAN_POINT('Ctrl Pts',(52.3507826112238,5.80181356312538,0.364725064619975));
#67276=CARTESIAN_POINT('Ctrl Pts',(52.4513525211815,4.9242696204448,3.08960089643144));
#67277=CARTESIAN_POINT('Ctrl Pts',(52.5519224311394,2.85259453374416,5.06525117048629));
#67278=CARTESIAN_POINT('Ctrl Pts',(52.6524923410972,0.0891677282345522,
5.81258239599026));
#67279=CARTESIAN_POINT('Ctrl Pts',(52.753062251055,-2.6958821746702,5.15036739414614));
#67280=CARTESIAN_POINT('Ctrl Pts',(52.8536321610128,-4.82718297079972,3.23919273272347));
#67281=CARTESIAN_POINT('Ctrl Pts',(52.9542020709706,-5.78789605210394,0.542516622165996));
#67282=CARTESIAN_POINT('Ctrl Pts',(53.0547719809283,-5.34504932273691,-2.28571930256727));
#67283=CARTESIAN_POINT('Ctrl Pts',(53.1553418908863,-3.60603273460568,-4.55967026342535));
#67284=CARTESIAN_POINT('Ctrl Pts',(53.2559118008439,-0.99255631088897,-5.72790511170206));
#67285=CARTESIAN_POINT('Ctrl Pts',(53.3564817108019,1.86161416062682,-5.50712789877888));
#67286=CARTESIAN_POINT('Ctrl Pts',(53.4570516207595,4.26434480692677,-3.95087691570875));
#67287=CARTESIAN_POINT('Ctrl Pts',(53.5576215307175,5.63297549627246,-1.43654167257841));
#67288=CARTESIAN_POINT('Ctrl Pts',(53.6581914406752,5.63561450056838,1.42615367186469));
#67289=CARTESIAN_POINT('Ctrl Pts',(53.758761350633,4.2716217932542,3.94300801314016));
#67290=CARTESIAN_POINT('Ctrl Pts',(53.8593312605908,1.87176456925964,5.50368623779372));
#67291=CARTESIAN_POINT('Ctrl Pts',(53.9599011705486,-0.981994129710483,
5.72972541999358));
#67292=CARTESIAN_POINT('Ctrl Pts',(54.0604710805064,-3.59761974878958,4.56631086087063));
#67293=CARTESIAN_POINT('Ctrl Pts',(54.1610409904643,-5.34082635831325,2.29557035626498));
#67294=CARTESIAN_POINT('Ctrl Pts',(54.261610900422,-5.78888583753521,-0.531844976840823));
#67295=CARTESIAN_POINT('Ctrl Pts',(54.3621808103798,-4.83314809906796,-3.23028641703264));
#67296=CARTESIAN_POINT('Ctrl Pts',(54.4627507203376,-2.70537098973005,-5.14538998627536));
#67297=CARTESIAN_POINT('Ctrl Pts',(54.5633206302954,0.078446240209487,-5.81273346716538));
#67298=CARTESIAN_POINT('Ctrl Pts',(54.6638905402532,2.84325992667244,-5.0705086592284));
#67299=CARTESIAN_POINT('Ctrl Pts',(54.764460450211,4.91854716216131,-3.09866134240672));
#67300=CARTESIAN_POINT('Ctrl Pts',(54.8650303601689,5.8011660495001,-0.375447161461482));
#67301=CARTESIAN_POINT('Ctrl Pts',(54.9656002701266,5.27686000591952,2.43892212337069));
#67302=CARTESIAN_POINT('Ctrl Pts',(55.0661701800844,3.47320975124282,4.66163850225691));
#67303=CARTESIAN_POINT('Ctrl Pts',(55.1667400900422,0.826722671906332,5.75435770195244));
#67304=CARTESIAN_POINT('Ctrl Pts',(55.2337866966808,-1.07034715964058,5.55179856586871));
#67305=CARTESIAN_POINT('Ctrl Pts',(55.26731,-1.93782473268743,5.23040479991605));
#67306=CARTESIAN_POINT('Ctrl Pts',(18.5943714011907,-2.5844886242714,5.20662521554142));
#67307=CARTESIAN_POINT('Ctrl Pts',(18.62789470451,-3.44802228533999,4.77798039642798));
#67308=CARTESIAN_POINT('Ctrl Pts',(18.6949413111485,-4.95685577985632,3.48321239743886));
#67309=CARTESIAN_POINT('Ctrl Pts',(18.7955112211063,-6.01818731712236,0.694543040107923));
#67310=CARTESIAN_POINT('Ctrl Pts',(18.8960811310641,-5.62003321802158,-2.26178872417008));
#67311=CARTESIAN_POINT('Ctrl Pts',(18.9966510410219,-3.85906871975241,-4.67001313762182));
#67312=CARTESIAN_POINT('Ctrl Pts',(19.0972209509797,-1.1622613390067,-5.94557351228712));
#67313=CARTESIAN_POINT('Ctrl Pts',(19.1977908609375,1.81638213979233,-5.77943430746988));
#67314=CARTESIAN_POINT('Ctrl Pts',(19.2983607708953,4.35456027613521,-4.21173777105813));
#67315=CARTESIAN_POINT('Ctrl Pts',(19.3989306808532,5.83675834943404,-1.62272373465775));
#67316=CARTESIAN_POINT('Ctrl Pts',(19.4995005908109,5.90354905198227,1.35981232901817));
#67317=CARTESIAN_POINT('Ctrl Pts',(19.6000705007687,4.53873342263602,4.0125884728718));
#67318=CARTESIAN_POINT('Ctrl Pts',(19.7006404107265,2.0732792381507,5.69231873872973));
#67319=CARTESIAN_POINT('Ctrl Pts',(19.8012103206843,-0.894943577534932,
5.99166488739198));
#67320=CARTESIAN_POINT('Ctrl Pts',(19.9017802306421,-3.64614324352199,4.83803833909629));
#67321=CARTESIAN_POINT('Ctrl Pts',(20.0023501405999,-5.51315636405137,2.51119120843917));
#67322=CARTESIAN_POINT('Ctrl Pts',(20.1029200505578,-6.04323378541225,-0.424617398710297));
#67323=CARTESIAN_POINT('Ctrl Pts',(20.2034899605155,-5.1078322296771,-3.25745676963478));
#67324=CARTESIAN_POINT('Ctrl Pts',(20.3040598704734,-2.93378574822532,-5.30036561803028));
#67325=CARTESIAN_POINT('Ctrl Pts',(20.4046297804311,-0.0482987518864741,
-6.05794039741912));
#67326=CARTESIAN_POINT('Ctrl Pts',(20.505199690389,2.8489006520323,-5.3464698296177));
#67327=CARTESIAN_POINT('Ctrl Pts',(20.6057696003468,5.05524409931645,-3.33848493853243));
#67328=CARTESIAN_POINT('Ctrl Pts',(20.7063395103046,6.03569520469174,-0.520920319627098));
#67329=CARTESIAN_POINT('Ctrl Pts',(20.8069094202624,5.55249541838547,2.42296702627515));
#67330=CARTESIAN_POINT('Ctrl Pts',(20.9074793302202,3.72282027299234,4.77928695513278));
#67331=CARTESIAN_POINT('Ctrl Pts',(21.008049240178,0.9903644160455,5.97663391097251));
#67332=CARTESIAN_POINT('Ctrl Pts',(21.1086191501357,-1.98225395922582,5.72465228853798));
#67333=CARTESIAN_POINT('Ctrl Pts',(21.2091890600936,-4.47417745578252,4.08444741393546));
#67334=CARTESIAN_POINT('Ctrl Pts',(21.3097589700513,-5.88111677080375,1.45376755753582));
#67335=CARTESIAN_POINT('Ctrl Pts',(21.4103288800092,-5.86189033154339,-1.52944968015864));
#67336=CARTESIAN_POINT('Ctrl Pts',(21.510898789967,-4.42116053296483,-4.14177668698978));
#67337=CARTESIAN_POINT('Ctrl Pts',(21.6114686999248,-1.90830311100522,-5.74972641259574));
#67338=CARTESIAN_POINT('Ctrl Pts',(21.7120386098826,1.06731617265169,-5.96337243267167));
#67339=CARTESIAN_POINT('Ctrl Pts',(21.8126085198404,3.78411220321663,-4.73090577126927));
#67340=CARTESIAN_POINT('Ctrl Pts',(21.9131784297982,5.58326428197402,-2.35119853283214));
#67341=CARTESIAN_POINT('Ctrl Pts',(22.0137483397559,6.02847957858663,0.598672325837003));
#67342=CARTESIAN_POINT('Ctrl Pts',(22.1143182497138,5.01179376688014,3.4033656608453));
#67343=CARTESIAN_POINT('Ctrl Pts',(22.2148881596716,2.779752281001,5.38274575281322));
#67344=CARTESIAN_POINT('Ctrl Pts',(22.3154580696294,-0.126376740130381,
6.05681463334594));
#67345=CARTESIAN_POINT('Ctrl Pts',(22.4160279795872,-3.00185951056889,5.26211117917195));
#67346=CARTESIAN_POINT('Ctrl Pts',(22.516597889545,-5.14939393378118,3.19135029382499));
#67347=CARTESIAN_POINT('Ctrl Pts',(22.6171677995028,-6.04820476079752,0.34668970943132));
#67348=CARTESIAN_POINT('Ctrl Pts',(22.7177377094606,-5.48033113978855,-2.58204283105899));
#67349=CARTESIAN_POINT('Ctrl Pts',(22.8183076194184,-3.5834819350071,-4.88463220771401));
#67350=CARTESIAN_POINT('Ctrl Pts',(22.9188775293762,-0.817641445750429,
-6.00270247882989));
#67351=CARTESIAN_POINT('Ctrl Pts',(23.019447439334,2.14647639025152,-5.66512256612795));
#67352=CARTESIAN_POINT('Ctrl Pts',(23.1200173492918,4.59007554936591,-3.95375530783995));
#67353=CARTESIAN_POINT('Ctrl Pts',(23.2205872592496,5.92058533902773,-1.28360579090672));
#67354=CARTESIAN_POINT('Ctrl Pts',(23.3211571692074,5.81535828058497,1.69781702535671));
#67355=CARTESIAN_POINT('Ctrl Pts',(23.4217270791652,4.29991184512756,4.26752067450071));
#67356=CARTESIAN_POINT('Ctrl Pts',(23.522296989123,1.74174048871413,5.80235423368249));
#67357=CARTESIAN_POINT('Ctrl Pts',(23.6228668990808,-1.2388014368723,5.93012188602919));
#67358=CARTESIAN_POINT('Ctrl Pts',(23.7234368090386,-3.91893508041301,4.6198400858328));
#67359=CARTESIAN_POINT('Ctrl Pts',(23.8240067189964,-5.64873034048527,2.18925104171279));
#67360=CARTESIAN_POINT('Ctrl Pts',(23.9245766289542,-6.00871335557892,-0.772229495452498));
#67361=CARTESIAN_POINT('Ctrl Pts',(24.025146538912,-4.91158855441746,-3.54644504472784));
#67362=CARTESIAN_POINT('Ctrl Pts',(24.1257164488698,-2.62340775684606,-5.4606507235383));
#67363=CARTESIAN_POINT('Ctrl Pts',(24.2262863588276,0.300947163455891,-6.05065330257545));
#67364=CARTESIAN_POINT('Ctrl Pts',(24.3268562687854,3.15232265568373,-5.17337766431394));
#67365=CARTESIAN_POINT('Ctrl Pts',(24.4274261787433,5.23926261751802,-3.04156239584817));
#67366=CARTESIAN_POINT('Ctrl Pts',(24.527996088701,6.05568590471169,-0.172170864653346));
#67367=CARTESIAN_POINT('Ctrl Pts',(24.6285659986588,5.40361057292087,2.7389719530103));
#67368=CARTESIAN_POINT('Ctrl Pts',(24.7291359086166,3.44116432877971,4.98591642985454));
#67369=CARTESIAN_POINT('Ctrl Pts',(24.8297058185744,0.64423869716238,6.02378046447892));
#67370=CARTESIAN_POINT('Ctrl Pts',(24.9302757285322,-2.30891426393765,5.60088292191012));
#67371=CARTESIAN_POINT('Ctrl Pts',(25.03084563849,-4.70215750361244,3.81977609217878));
#67372=CARTESIAN_POINT('Ctrl Pts',(25.1314155484478,-5.95513159641322,1.11237684826688));
#67373=CARTESIAN_POINT('Ctrl Pts',(25.2319854584056,-5.76399140343187,-1.86477282378385));
#67374=CARTESIAN_POINT('Ctrl Pts',(25.3325553683634,-4.17508825692739,-4.3897166913169));
#67375=CARTESIAN_POINT('Ctrl Pts',(25.4331252783212,-1.57372980215375,-5.85015803999965));
#67376=CARTESIAN_POINT('Ctrl Pts',(25.533695188279,1.40925677493045,-5.89194109996629));
#67377=CARTESIAN_POINT('Ctrl Pts',(25.6342650982368,4.05049979722267,-4.50493351514298));
#67378=CARTESIAN_POINT('Ctrl Pts',(25.7348350081947,5.70950010547477,-2.02548343087346));
#67379=CARTESIAN_POINT('Ctrl Pts',(25.8354049181524,5.98395155305067,0.945144641788645));
#67380=CARTESIAN_POINT('Ctrl Pts',(25.9359748281102,4.80729990016889,3.68657595242462));
#67381=CARTESIAN_POINT('Ctrl Pts',(26.0365447380681,2.46488215975777,5.53401576810792));
#67382=CARTESIAN_POINT('Ctrl Pts',(26.1371146480258,-0.475267382553351,
6.03946152386455));
#67383=CARTESIAN_POINT('Ctrl Pts',(26.2376845579837,-3.30016499371908,5.08034305902568));
#67384=CARTESIAN_POINT('Ctrl Pts',(26.3382544679414,-5.32477543478461,2.8892457756781));
#67385=CARTESIAN_POINT('Ctrl Pts',(26.4388243778993,-6.05813241663425,-0.00249112112580119));
#67386=CARTESIAN_POINT('Ctrl Pts',(26.539394287857,-5.32239750246424,-2.89362392320112));
#67387=CARTESIAN_POINT('Ctrl Pts',(26.6399641978149,-3.29598577561902,-5.08305541481463));
#67388=CARTESIAN_POINT('Ctrl Pts',(26.7405341077727,-0.470300335465298,
-6.03985034397546));
#67389=CARTESIAN_POINT('Ctrl Pts',(26.8411040177305,2.46943253119076,-5.53198676399865));
#67390=CARTESIAN_POINT('Ctrl Pts',(26.9416739276883,4.81033013479139,-3.68262115584499));
#67391=CARTESIAN_POINT('Ctrl Pts',(27.0422438376461,5.98472682157525,-0.940223087504847));
#67392=CARTESIAN_POINT('Ctrl Pts',(27.1428137476039,5.70783240595158,2.03017827018424));
#67393=CARTESIAN_POINT('Ctrl Pts',(27.2433836575617,4.04679354535049,4.50826314498931));
#67394=CARTESIAN_POINT('Ctrl Pts',(27.3439535675195,1.40441073359784,5.89309808797669));
#67395=CARTESIAN_POINT('Ctrl Pts',(27.4445234774773,-1.57854047209525,5.84886181757755));
#67396=CARTESIAN_POINT('Ctrl Pts',(27.5450933874351,-4.17869697215815,4.38628159128385));
#67397=CARTESIAN_POINT('Ctrl Pts',(27.6456632973929,-5.7655230536149,1.8600318549408));
#67398=CARTESIAN_POINT('Ctrl Pts',(27.7462332073507,-5.95421475769761,-1.11727400505664));
#67399=CARTESIAN_POINT('Ctrl Pts',(27.8468031173085,-4.69901450859748,-3.82364188060932));
#67400=CARTESIAN_POINT('Ctrl Pts',(27.9473730272663,-2.30430728620892,-5.60277989161486));
#67401=CARTESIAN_POINT('Ctrl Pts',(28.0479429372241,0.649192469471501,-6.02324860193738));
#67402=CARTESIAN_POINT('Ctrl Pts',(28.1485128471819,3.44526361014859,-4.98308471127526));
#67403=CARTESIAN_POINT('Ctrl Pts',(28.2490827571396,5.40586129114638,-2.73452706771108));
#67404=CARTESIAN_POINT('Ctrl Pts',(28.3496526670975,6.05554226256158,0.177151035813719));
#67405=CARTESIAN_POINT('Ctrl Pts',(28.4502225770553,5.23675944809004,3.04587016565037));
#67406=CARTESIAN_POINT('Ctrl Pts',(28.5507924870131,3.14806697540939,5.17596840228919));
#67407=CARTESIAN_POINT('Ctrl Pts',(28.6513623969709,0.295970971138304,6.05089875699492));
#67408=CARTESIAN_POINT('Ctrl Pts',(28.7519323069287,-2.62789773885353,5.45849137191659));
#67409=CARTESIAN_POINT('Ctrl Pts',(28.8525022168865,-4.91450350934312,3.54240452797438));
#67410=CARTESIAN_POINT('Ctrl Pts',(28.9530721268443,-6.00934640936257,0.767287635401802));
#67411=CARTESIAN_POINT('Ctrl Pts',(29.0536420368021,-5.64692797812932,-2.19389584825251));
#67412=CARTESIAN_POINT('Ctrl Pts',(29.1542119467599,-3.91513437323725,-4.62306147727406));
#67413=CARTESIAN_POINT('Ctrl Pts',(29.2547818567177,-1.23392405309511,-5.93113867772054));
#67414=CARTESIAN_POINT('Ctrl Pts',(29.3553517666755,1.74651178772539,-5.80091985451407));
#67415=CARTESIAN_POINT('Ctrl Pts',(29.4559216766333,4.30342002346993,-4.2639829601861));
#67416=CARTESIAN_POINT('Ctrl Pts',(29.5564915865911,5.81675260803036,-1.69303386857182));
#67417=CARTESIAN_POINT('Ctrl Pts',(29.6570614965489,5.91952769237091,1.28847447875902));
#67418=CARTESIAN_POINT('Ctrl Pts',(29.7576314065067,4.58682240701069,3.95752887414659));
#67419=CARTESIAN_POINT('Ctrl Pts',(29.8582013164645,2.14181663641865,5.66688592430795));
#67420=CARTESIAN_POINT('Ctrl Pts',(29.9587712264223,-0.822577824767718,
6.00202801604255));
#67421=CARTESIAN_POINT('Ctrl Pts',(30.0593411363801,-3.5874978715465,4.88168348060468));
#67422=CARTESIAN_POINT('Ctrl Pts',(30.1599110463379,-5.4824527726963,2.57753490341331));
#67423=CARTESIAN_POINT('Ctrl Pts',(30.2604809562957,-6.04791759591984,-0.351663669039821));
#67424=CARTESIAN_POINT('Ctrl Pts',(30.3610508662535,-5.14676760835371,-3.19558410447297));
#67425=CARTESIAN_POINT('Ctrl Pts',(30.4616207762113,-2.99753090624697,-5.26457814542186));
#67426=CARTESIAN_POINT('Ctrl Pts',(30.5621906861691,-0.12139553973591,-6.0569165180058));
#67427=CARTESIAN_POINT('Ctrl Pts',(30.6627605961269,2.78417814066035,-5.38045784894078));
#67428=CARTESIAN_POINT('Ctrl Pts',(30.7633305060847,5.01459101864687,-3.39924278316002));
#67429=CARTESIAN_POINT('Ctrl Pts',(30.8639004160425,6.02896989131526,-0.593714268628649));
#67430=CARTESIAN_POINT('Ctrl Pts',(30.9644703260003,5.58132875524992,2.35578944495891));
#67431=CARTESIAN_POINT('Ctrl Pts',(31.0650402359581,3.78022020060429,4.73401624607505));
#67432=CARTESIAN_POINT('Ctrl Pts',(31.1656101459159,1.06241150143411,5.96424818269493));
#67433=CARTESIAN_POINT('Ctrl Pts',(31.2661800558737,-1.91303107227957,5.74815506920718));
#67434=CARTESIAN_POINT('Ctrl Pts',(31.3667499658316,-4.42456525775745,4.13813929961341));
#67435=CARTESIAN_POINT('Ctrl Pts',(31.4673198757893,-5.86314617702181,1.5246283120924));
#67436=CARTESIAN_POINT('Ctrl Pts',(31.5678897857471,-5.87991919552279,-1.45860372866722));
#67437=CARTESIAN_POINT('Ctrl Pts',(31.6684596957049,-4.47081687071256,-4.08812562083301));
#67438=CARTESIAN_POINT('Ctrl Pts',(31.7690296056627,-1.97754530336189,-5.72628056912257));
#67439=CARTESIAN_POINT('Ctrl Pts',(31.8695995156205,0.995279297726343,-5.97581740874642));
#67440=CARTESIAN_POINT('Ctrl Pts',(31.9701694255783,3.72674952588087,-4.77622367090424));
#67441=CARTESIAN_POINT('Ctrl Pts',(32.0707393355362,5.55448620210214,-2.41839980437813));
#67442=CARTESIAN_POINT('Ctrl Pts',(32.1713092454939,6.03526475577469,0.525883932881758));
#67443=CARTESIAN_POINT('Ctrl Pts',(32.2718791554517,5.05249680150087,3.34264126911381));
#67444=CARTESIAN_POINT('Ctrl Pts',(32.3724490654095,2.8445027221972,5.34881097502727));
#67445=CARTESIAN_POINT('Ctrl Pts',(32.4730189753674,-0.053280818609776,
6.05789862390643));
#67446=CARTESIAN_POINT('Ctrl Pts',(32.5735888853251,-2.93814380676952,5.29795107130118));
#67447=CARTESIAN_POINT('Ctrl Pts',(32.674158795283,-5.11050945102608,3.2532549445336));
#67448=CARTESIAN_POINT('Ctrl Pts',(32.7747287052407,-6.04358095268194,0.419647294211818));
#67449=CARTESIAN_POINT('Ctrl Pts',(32.8752986151986,-5.51108927580026,-2.51572446371195));
#67450=CARTESIAN_POINT('Ctrl Pts',(32.9758685251563,-3.64216319364069,-4.84103520479332));
#67451=CARTESIAN_POINT('Ctrl Pts',(33.0764384351142,-0.890015672301798,
-5.99239907601425));
#67452=CARTESIAN_POINT('Ctrl Pts',(33.1770083450719,2.07795988341927,-5.69061132973071));
#67453=CARTESIAN_POINT('Ctrl Pts',(33.2775782550298,4.54203195617863,-4.00885523462889));
#67454=CARTESIAN_POINT('Ctrl Pts',(33.3781481649875,5.90466518947603,-1.35495519606713));
#67455=CARTESIAN_POINT('Ctrl Pts',(33.4787180749454,5.83542219723063,1.62752031115663));
#67456=CARTESIAN_POINT('Ctrl Pts',(33.5792879849031,4.35109434545558,4.21532354394106));
#67457=CARTESIAN_POINT('Ctrl Pts',(33.679857894861,1.81162986045434,5.78091444599118));
#67458=CARTESIAN_POINT('Ctrl Pts',(33.7804278048188,-1.16715330620413,5.94463857126538));
#67459=CARTESIAN_POINT('Ctrl Pts',(33.8809977147765,-3.86290280082714,4.66679296032308));
#67460=CARTESIAN_POINT('Ctrl Pts',(33.9815676247344,-5.62190169154708,2.25725407381167));
#67461=CARTESIAN_POINT('Ctrl Pts',(34.0821375346921,-6.01759426156107,-0.699666982490047));
#67462=CARTESIAN_POINT('Ctrl Pts',(34.18270744465,-4.95402540326419,-3.48691939783132));
#67463=CARTESIAN_POINT('Ctrl Pts',(34.2832773546078,-2.6891096492429,-5.42859686083872));
#67464=CARTESIAN_POINT('Ctrl Pts',(34.3838472645656,0.227912879857088,-6.0538442581846));
#67465=CARTESIAN_POINT('Ctrl Pts',(34.4844171745234,3.08966673178568,-5.21103963424345));
#67466=CARTESIAN_POINT('Ctrl Pts',(34.5849870844812,5.20217906092996,-3.10456238481063));
#67467=CARTESIAN_POINT('Ctrl Pts',(34.685556994439,6.05316744598368,-0.24523142955757));
#67468=CARTESIAN_POINT('Ctrl Pts',(34.7861269043967,5.43626793612645,2.67356793626095));
#67469=CARTESIAN_POINT('Ctrl Pts',(34.8866968143546,3.50107813145393,4.94402937902015));
#67470=CARTESIAN_POINT('Ctrl Pts',(34.9872667243123,0.716879893732276,6.01556795332924));
#67471=CARTESIAN_POINT('Ctrl Pts',(35.0878366342702,-2.24116110110868,5.62833647732939));
#67472=CARTESIAN_POINT('Ctrl Pts',(35.188406544228,-4.65572245818653,3.87623825061062));
#67473=CARTESIAN_POINT('Ctrl Pts',(35.2889764541858,-5.94127512693356,1.18415558489583));
#67474=CARTESIAN_POINT('Ctrl Pts',(35.3895463641436,-5.78607369181921,-1.79508379080112));
#67475=CARTESIAN_POINT('Ctrl Pts',(35.4901162741014,-4.22775436725687,-4.33901689248841));
#67476=CARTESIAN_POINT('Ctrl Pts',(35.5906861840592,-1.64420824800695,-5.83074213289743));
#67477=CARTESIAN_POINT('Ctrl Pts',(35.691256094017,1.33805695600305,-5.90851742534887));
#67478=CARTESIAN_POINT('Ctrl Pts',(35.7918260039748,3.9958445000201,-4.55348232837445));
#67479=CARTESIAN_POINT('Ctrl Pts',(35.8923959139326,5.68464319251983,-2.09423168653741));
#67480=CARTESIAN_POINT('Ctrl Pts',(35.9929658238904,5.99492080433738,0.872868336510265));
#67481=CARTESIAN_POINT('Ctrl Pts',(36.0935357338482,4.85143528170287,3.62829853934429));
#67482=CARTESIAN_POINT('Ctrl Pts',(36.194105643806,2.53148087951004,5.50386946973076));
#67483=CARTESIAN_POINT('Ctrl Pts',(36.2946755537638,-0.402355456792645,
6.04475679159621));
#67484=CARTESIAN_POINT('Ctrl Pts',(36.3952454637216,-3.23862094118222,5.11979579499956));
#67485=CARTESIAN_POINT('Ctrl Pts',(36.4958153736794,-5.2895236352329,2.95328872538259));
#67486=CARTESIAN_POINT('Ctrl Pts',(36.5963852836372,-6.05772140111323,0.0706116821359479));
#67487=CARTESIAN_POINT('Ctrl Pts',(36.696955193595,-5.35692694188392,-2.82918863324405));
#67488=CARTESIAN_POINT('Ctrl Pts',(36.7975251035528,-3.35708231064414,-5.04291314050912));
#67489=CARTESIAN_POINT('Ctrl Pts',(36.8980950135106,-0.54314810894586,-6.03373555228499));
#67490=CARTESIAN_POINT('Ctrl Pts',(36.9986649234684,2.40249904161435,-5.56138228664435));
#67491=CARTESIAN_POINT('Ctrl Pts',(37.0992348334262,4.76554224272314,-3.74039860388978));
#67492=CARTESIAN_POINT('Ctrl Pts',(37.199804743384,5.97294555228697,-1.01237147953434));
#67493=CARTESIAN_POINT('Ctrl Pts',(37.3003746533419,5.73191470710404,1.96115485712974));
#67494=CARTESIAN_POINT('Ctrl Pts',(37.4009445632996,4.10089947964499,4.45910282915821));
#67495=CARTESIAN_POINT('Ctrl Pts',(37.5015144732574,1.47541965854388,5.87572220363945));
#67496=CARTESIAN_POINT('Ctrl Pts',(37.6020843832152,-1.50784815967059,5.86748400172828));
#67497=CARTESIAN_POINT('Ctrl Pts',(37.702654293173,-4.12546409716388,4.43638598029649));
#67498=CARTESIAN_POINT('Ctrl Pts',(37.8032242031308,-5.74265854241269,1.92946817761106));
#67499=CARTESIAN_POINT('Ctrl Pts',(37.9037941130886,-5.9672632345716,-1.04534399720345));
#67500=CARTESIAN_POINT('Ctrl Pts',(38.0043640230464,-4.74481172913825,-3.76666115255824));
#67501=CARTESIAN_POINT('Ctrl Pts',(38.1049339330042,-2.37174746385888,-5.57456622086761));
#67502=CARTESIAN_POINT('Ctrl Pts',(38.205503842962,0.576463519738073,-6.03064377936308));
#67503=CARTESIAN_POINT('Ctrl Pts',(38.3060737529198,3.38488259603486,-5.02429541271407));
#67504=CARTESIAN_POINT('Ctrl Pts',(38.4066436628776,5.37247055659719,-2.79955973353948));
#67505=CARTESIAN_POINT('Ctrl Pts',(38.5072135728355,6.0572390319614,0.104066771077096));
#67506=CARTESIAN_POINT('Ctrl Pts',(38.6077834827932,5.27313225632011,2.98245717329113));
#67507=CARTESIAN_POINT('Ctrl Pts',(38.708353392751,3.21029544778464,5.13760427836678));
#67508=CARTESIAN_POINT('Ctrl Pts',(38.8089233027089,0.368964756675754,6.04688676853557));
#67509=CARTESIAN_POINT('Ctrl Pts',(38.9094932126666,-2.56183957031156,5.48980442266801));
#67510=CARTESIAN_POINT('Ctrl Pts',(39.0100631226245,-4.87140000680326,3.60144923008454));
#67511=CARTESIAN_POINT('Ctrl Pts',(39.1106330325822,-5.99965013508599,0.839745699436374));
#67512=CARTESIAN_POINT('Ctrl Pts',(39.2112029425401,-5.6729902702813,-2.12559544044792));
#67513=CARTESIAN_POINT('Ctrl Pts',(39.3117728524979,-3.97063514840612,-4.57548151579714));
#67514=CARTESIAN_POINT('Ctrl Pts',(39.4123427624556,-1.30540442107904,-5.91581726227125));
#67515=CARTESIAN_POINT('Ctrl Pts',(39.5129126724135,1.67638575463012,-5.82157241514975));
#67516=CARTESIAN_POINT('Ctrl Pts',(39.6134825823712,4.25165382792243,-4.31560126873092));
#67517=CARTESIAN_POINT('Ctrl Pts',(39.7140524923291,5.79589950788908,-1.76310052963817));
#67518=CARTESIAN_POINT('Ctrl Pts',(39.8146224022869,5.93464454646915,1.21695057016433));
#67519=CARTESIAN_POINT('Ctrl Pts',(39.9151923122447,4.63424339124267,3.90189220428793));
#67520=CARTESIAN_POINT('Ctrl Pts',(40.0157622222025,2.21004220292946,5.64062833773242));
#67521=CARTESIAN_POINT('Ctrl Pts',(40.1163321321603,-0.750092317126442,
6.01151695489143));
#67522=CARTESIAN_POINT('Ctrl Pts',(40.2169020421181,-3.52833009598016,4.92461788537547));
#67523=CARTESIAN_POINT('Ctrl Pts',(40.3174719520759,-5.45095086384642,2.64350321790825));
#67524=CARTESIAN_POINT('Ctrl Pts',(40.4180418620337,-6.05172073956474,-0.278658704298321));
#67525=CARTESIAN_POINT('Ctrl Pts',(40.5186117719915,-5.1849535454334,-3.13324613058997));
#67526=CARTESIAN_POINT('Ctrl Pts',(40.6191816819493,-3.06083957989115,-5.22802406740167));
#67527=CARTESIAN_POINT('Ctrl Pts',(40.719751591907,-0.19447465108379,-6.05501066830152));
#67528=CARTESIAN_POINT('Ctrl Pts',(40.8203215018649,2.71905021320203,-5.41366239446507));
#67529=CARTESIAN_POINT('Ctrl Pts',(40.9208914118227,4.97320774142276,-3.4595056502067));
#67530=CARTESIAN_POINT('Ctrl Pts',(41.0214613217805,6.02136667342831,-0.666421763814872));
#67531=CARTESIAN_POINT('Ctrl Pts',(41.1220312317383,5.60934937049263,2.2882688266271));
#67532=CARTESIAN_POINT('Ctrl Pts',(41.2226011416961,3.83706967390126,4.68805619641941));
#67533=CARTESIAN_POINT('Ctrl Pts',(41.3231710516539,1.13430388444848,5.95099397419325));
#67534=CARTESIAN_POINT('Ctrl Pts',(41.4237409616117,-1.84352962054176,5.77082083601151));
#67535=CARTESIAN_POINT('Ctrl Pts',(41.5243108715695,-4.37430877951378,4.19122861278503));
#67536=CARTESIAN_POINT('Ctrl Pts',(41.6248807815273,-5.84432182498416,1.59526705888798));
#67537=CARTESIAN_POINT('Ctrl Pts',(41.7254506914851,-5.89709185885572,-1.38754538353777));
#67538=CARTESIAN_POINT('Ctrl Pts',(41.8260206014429,-4.51982219334054,-4.03387926489447));
#67539=CARTESIAN_POINT('Ctrl Pts',(41.9265905114008,-2.04649953673286,-5.70200089699322));
#67540=CARTESIAN_POINT('Ctrl Pts',(42.0271604213585,0.923097495847049,-5.98739222001702));
#67541=CARTESIAN_POINT('Ctrl Pts',(42.1277303313163,3.66884418031286,-4.8208460838056));
#67542=CARTESIAN_POINT('Ctrl Pts',(42.2283002412741,5.52489930929906,-2.48524892219391));
#67543=CARTESIAN_POINT('Ctrl Pts',(42.3288701512318,6.04117111177205,0.453018963676277));
#67544=CARTESIAN_POINT('Ctrl Pts',(42.4294400611898,5.09246412005362,3.28143014082667));
#67545=CARTESIAN_POINT('Ctrl Pts',(42.5300099711475,2.90883896296137,5.31409733357577));
#67546=CARTESIAN_POINT('Ctrl Pts',(42.6305798811053,0.01982286136298,6.05810049746014));
#67547=CARTESIAN_POINT('Ctrl Pts',(42.731149791063,-2.87400026705184,5.33301950569705));
#67548=CARTESIAN_POINT('Ctrl Pts',(42.831719701021,-5.07088080472847,3.31468587461856));
#67549=CARTESIAN_POINT('Ctrl Pts',(42.9322896109787,-6.03807711241803,0.492543772321716));
#67550=CARTESIAN_POINT('Ctrl Pts',(43.0328595209366,-5.54104491809615,-2.44903977076732));
#67551=CARTESIAN_POINT('Ctrl Pts',(43.1334294308942,-3.70031410102634,-4.79673327764896));
#67552=CARTESIAN_POINT('Ctrl Pts',(43.2339993408522,-0.962260299794141,
-5.98122309386629));
#67553=CARTESIAN_POINT('Ctrl Pts',(43.3345692508099,2.00914079579688,-5.71527145862941));
#67554=CARTESIAN_POINT('Ctrl Pts',(43.4351391607677,4.49332697793318,-4.06337141454449));
#67555=CARTESIAN_POINT('Ctrl Pts',(43.5357090707255,5.8878852359054,-1.42610730029916));
#67556=CARTESIAN_POINT('Ctrl Pts',(43.6362789806834,5.85463639263101,1.55698660663465));
#67557=CARTESIAN_POINT('Ctrl Pts',(43.7368488906411,4.40164326398255,4.16251260175827));
#67558=CARTESIAN_POINT('Ctrl Pts',(43.8374188005989,1.88125543287904,5.75863287416575));
#67559=CARTESIAN_POINT('Ctrl Pts',(43.9379887105567,-1.095335221259,5.95828963178433));
#67560=CARTESIAN_POINT('Ctrl Pts',(44.0385586205146,-3.80630802713771,4.71306628276184));
#67561=CARTESIAN_POINT('Ctrl Pts',(44.1391285304723,-5.59425441301462,2.32492841731219));
#67562=CARTESIAN_POINT('Ctrl Pts',(44.2396984404302,-6.02559891943012,-0.627002587970594));
#67563=CARTESIAN_POINT('Ctrl Pts',(44.3402683503879,-4.99574087489218,-3.42688600541233));
#67564=CARTESIAN_POINT('Ctrl Pts',(44.4408382603457,-2.7544199686699,-5.39575251650331));
#67565=CARTESIAN_POINT('Ctrl Pts',(44.5414081703035,0.154845408871141,-6.05615368716076));
#67566=CARTESIAN_POINT('Ctrl Pts',(44.6419780802614,3.02656090805623,-5.2479428019925));
#67567=CARTESIAN_POINT('Ctrl Pts',(44.7425479902191,5.16433799238815,-3.16711030492081));
#67568=CARTESIAN_POINT('Ctrl Pts',(44.843117900177,6.04976755917625,-0.318256285245154));
#67569=CARTESIAN_POINT('Ctrl Pts',(44.9436878101347,5.46813370067749,2.60777460963838));
#67570=CARTESIAN_POINT('Ctrl Pts',(45.0442577200926,3.56048212689068,4.90142240653173));
#67571=CARTESIAN_POINT('Ctrl Pts',(45.1448276300503,0.789416702298039,6.00647948912606));
#67572=CARTESIAN_POINT('Ctrl Pts',(45.2453975400082,-2.17308159304928,5.65497046615715));
#67573=CARTESIAN_POINT('Ctrl Pts',(45.3459674499659,-4.60860947273312,3.93213597310593));
#67574=CARTESIAN_POINT('Ctrl Pts',(45.4465373599238,-5.92655352250245,1.25576189147193));
#67575=CARTESIAN_POINT('Ctrl Pts',(45.5471072698815,-5.80731344481216,-1.72513336784826));
#67576=CARTESIAN_POINT('Ctrl Pts',(45.6476771798394,-4.2798048558568,-4.28768527050947));
#67577=CARTESIAN_POINT('Ctrl Pts',(45.7482470897971,-1.71444727353495,-5.81047718603454));
#67578=CARTESIAN_POINT('Ctrl Pts',(45.848816999755,1.26666229677368,-5.92423338577162));
#67579=CARTESIAN_POINT('Ctrl Pts',(45.9493869097128,3.94060735049394,-4.60136808920917));
#67580=CARTESIAN_POINT('Ctrl Pts',(46.0499568196705,5.6589585139073,-2.16267499200307));
#67581=CARTESIAN_POINT('Ctrl Pts',(46.1505267296284,6.00501710909191,0.800464929071172));
#67582=CARTESIAN_POINT('Ctrl Pts',(46.2510966395861,4.89486422461261,3.56949279390883));
#67583=CARTESIAN_POINT('Ctrl Pts',(46.351666549544,2.59771097930425,5.47292172894527));
#67584=CARTESIAN_POINT('Ctrl Pts',(46.4522364595017,-0.329384942301194,
6.04917185596049));
#67585=CARTESIAN_POINT('Ctrl Pts',(46.5528063694596,-3.17660529894262,5.15850301520595));
#67586=CARTESIAN_POINT('Ctrl Pts',(46.6533762794173,-5.25350160510346,3.01690163385131));
#67587=CARTESIAN_POINT('Ctrl Pts',(46.7539461893752,-6.05642829439157,0.143704203323096));
#67588=CARTESIAN_POINT('Ctrl Pts',(46.8545160993329,-5.39067633583681,-2.76434137280626));
#67589=CARTESIAN_POINT('Ctrl Pts',(46.9550860092908,-3.41769000629041,-5.00203654565438));
#67590=CARTESIAN_POINT('Ctrl Pts',(47.0556559192486,-0.615916792264225,
-6.02674216207779));
#67591=CARTESIAN_POINT('Ctrl Pts',(47.1562258292064,2.33521571368719,-5.58996799218991));
#67592=CARTESIAN_POINT('Ctrl Pts',(47.2567957391642,4.72006041929019,-3.79763139620073));
#67593=CARTESIAN_POINT('Ctrl Pts',(47.3573656491219,5.96029453637867,-1.08437245574289));
#67594=CARTESIAN_POINT('Ctrl Pts',(47.4579355590799,5.7551623591878,1.8918458717737));
#67595=CARTESIAN_POINT('Ctrl Pts',(47.5585054690375,4.1544082641027,4.40929320394034));
#67596=CARTESIAN_POINT('Ctrl Pts',(47.6590753789954,1.54621374120647,5.85749072979751));
#67597=CARTESIAN_POINT('Ctrl Pts',(47.7596452889532,-1.4369362829072,5.88525179597474));
#67598=CARTESIAN_POINT('Ctrl Pts',(47.860215198911,-4.07163049537184,4.48584436782168));
#67599=CARTESIAN_POINT('Ctrl Pts',(47.9607851088687,-5.7189578176851,1.9986235420153));
#67600=CARTESIAN_POINT('Ctrl Pts',(48.0613550188267,-5.97944279225262,-0.973261772257315));
#67601=CARTESIAN_POINT('Ctrl Pts',(48.1619249287844,-4.78991803697473,-3.70913194456918));
#67602=CARTESIAN_POINT('Ctrl Pts',(48.2624948387422,-2.43884228102927,-5.54554081325017));
#67603=CARTESIAN_POINT('Ctrl Pts',(48.3630647487,0.503650628640414,-6.03716080847854));
#67604=CARTESIAN_POINT('Ctrl Pts',(48.4636346586578,3.3240086944217,-5.06477450461206));
#67605=CARTESIAN_POINT('Ctrl Pts',(48.5642045686156,5.33829751320773,-2.86418474328027));
#67606=CARTESIAN_POINT('Ctrl Pts',(48.6647744785734,6.05805378040047,0.0309673527246042));
#67607=CARTESIAN_POINT('Ctrl Pts',(48.7653443885312,5.30873722079254,2.91860989235135));
#67608=CARTESIAN_POINT('Ctrl Pts',(48.865914298489,3.27205645505567,5.098492045506));
#67609=CARTESIAN_POINT('Ctrl Pts',(48.9664842084468,0.44190481564781,6.04199426655359));
#67610=CARTESIAN_POINT('Ctrl Pts',(49.0670541184046,-2.49540836115029,5.5203180790839));
#67611=CARTESIAN_POINT('Ctrl Pts',(49.1676240283624,-4.82758715848853,3.65996950948447));
#67612=CARTESIAN_POINT('Ctrl Pts',(49.2681939383203,-5.98908022561877,0.912081484441761));
#67613=CARTESIAN_POINT('Ctrl Pts',(49.3687638482779,-5.69822649360848,-2.05698551543216));
#67614=CARTESIAN_POINT('Ctrl Pts',(49.4693337582359,-4.02555774209492,-4.52723529852593));
#67615=CARTESIAN_POINT('Ctrl Pts',(49.5699036681935,-1.37669470343887,-5.8996344189011));
#67616=CARTESIAN_POINT('Ctrl Pts',(49.6704735781515,1.6060156157028,-5.84137727126729));
#67617=CARTESIAN_POINT('Ctrl Pts',(49.7710434881091,4.19926853054085,-4.36659116377622));
#67618=CARTESIAN_POINT('Ctrl Pts',(49.8716133980671,5.77420244157352,-1.83291045795632));
#67619=CARTESIAN_POINT('Ctrl Pts',(49.9721833080248,5.94889723112367,1.1452494560961));
#67620=CARTESIAN_POINT('Ctrl Pts',(50.0727532179827,4.68098956310768,3.84568736290879));
#67621=CARTESIAN_POINT('Ctrl Pts',(50.1733231279404,2.27794595556811,5.61354939469407));
#67622=CARTESIAN_POINT('Ctrl Pts',(50.2738930378982,-0.677497585275496,
6.02013053057035));
#67623=CARTESIAN_POINT('Ctrl Pts',(50.374462947856,-3.46864854489916,4.96683519508433));
#67624=CARTESIAN_POINT('Ctrl Pts',(50.4750328578139,-5.4186552182969,2.70908660038451));
#67625=CARTESIAN_POINT('Ctrl Pts',(50.5756027677716,-6.05464266579148,-0.205613162849079));
#67626=CARTESIAN_POINT('Ctrl Pts',(50.6761726777295,-5.22238447884166,-3.0704519110895));
#67627=CARTESIAN_POINT('Ctrl Pts',(50.7767425876872,-3.12370255135105,-5.19070871402375));
#67628=CARTESIAN_POINT('Ctrl Pts',(50.877312497645,-0.26752544413057,-6.0522231221182));
#67629=CARTESIAN_POINT('Ctrl Pts',(50.9778824076028,2.65352635299801,-5.44607863302619));
#67630=CARTESIAN_POINT('Ctrl Pts',(51.0784523175607,4.93110029375614,-3.519264763566));
#67631=CARTESIAN_POINT('Ctrl Pts',(51.1790222275184,6.01288665811098,-0.739032218425107));
#67632=CARTESIAN_POINT('Ctrl Pts',(51.2795921374763,5.63655318393917,2.22041500350376));
#67633=CARTESIAN_POINT('Ctrl Pts',(51.380162047434,3.89336041476873,4.64141349847986));
#67634=CARTESIAN_POINT('Ctrl Pts',(51.4807319573918,1.20603109653318,5.93687321553647));
#67635=CARTESIAN_POINT('Ctrl Pts',(51.5813018673497,-1.7737597244255,5.79264628845618));
#67636=CARTESIAN_POINT('Ctrl Pts',(51.6818717773074,-4.32341533911426,4.24370762290134));
#67637=CARTESIAN_POINT('Ctrl Pts',(51.7824416872653,-5.82464645578769,1.66567351189812));
#67638=CARTESIAN_POINT('Ctrl Pts',(51.8830115972231,-5.91340582095539,-1.31628499188082));
#67639=CARTESIAN_POINT('Ctrl Pts',(51.9835815071809,-4.56816936497055,-3.97904551822462));
#67640=CARTESIAN_POINT('Ctrl Pts',(52.0841514171387,-2.11515577039187,-5.67689093167526));
#67641=CARTESIAN_POINT('Ctrl Pts',(52.1847213270964,0.850781277720655,-5.99809518102555));
#67642=CARTESIAN_POINT('Ctrl Pts',(52.2852912370543,3.61040459836179,-4.86476651230871));
#67643=CARTESIAN_POINT('Ctrl Pts',(52.385861147012,5.49450791184205,-2.55173615208908));
#67644=CARTESIAN_POINT('Ctrl Pts',(52.4864310569699,6.04619778652662,0.380088028407498));
#67645=CARTESIAN_POINT('Ctrl Pts',(52.5870009669276,5.13168990272672,3.21974118920008));
#67646=CARTESIAN_POINT('Ctrl Pts',(52.6875708768855,2.97275163500614,5.27860988326863));
#67647=CARTESIAN_POINT('Ctrl Pts',(52.7881407868432,0.0929236548564317,
6.05742022460096));
#67648=CARTESIAN_POINT('Ctrl Pts',(52.8887106968011,-2.80943823166339,5.3673113759123));
#67649=CARTESIAN_POINT('Ctrl Pts',(52.9892806067589,-5.03051376533478,3.37563413881495));
#67650=CARTESIAN_POINT('Ctrl Pts',(53.0898505167167,-6.03169404154821,0.56536852906504));
#67651=CARTESIAN_POINT('Ctrl Pts',(53.1904204266745,-5.57019370450064,-2.38199846262534));
#67652=CARTESIAN_POINT('Ctrl Pts',(53.2909903366322,-3.75792618995677,-4.7517328769804));
#67653=CARTESIAN_POINT('Ctrl Pts',(53.3915602465901,-1.03436480759078,-5.96917616035072));
#67654=CARTESIAN_POINT('Ctrl Pts',(53.4921301565479,1.94002914690096,-5.7390993608176));
#67655=CARTESIAN_POINT('Ctrl Pts',(53.5927000665057,4.44396770976864,-4.11729591147515));
#67656=CARTESIAN_POINT('Ctrl Pts',(53.6932699764635,5.87024791585588,-1.49705173847708));
#67657=CARTESIAN_POINT('Ctrl Pts',(53.7938398864213,5.87299808039652,1.48622617398105));
#67658=CARTESIAN_POINT('Ctrl Pts',(53.894409796379,4.45155121760574,4.10909555467727));
#67659=CARTESIAN_POINT('Ctrl Pts',(53.9949797063369,1.95060711145293,5.73551273005053));
#67660=CARTESIAN_POINT('Ctrl Pts',(54.0955496162947,-1.02335772579348,5.97107314374103));
#67661=CARTESIAN_POINT('Ctrl Pts',(54.1961195262525,-3.74915883201502,4.75865318993734));
#67662=CARTESIAN_POINT('Ctrl Pts',(54.2966894362103,-5.56579286020032,2.39226446280162));
#67663=CARTESIAN_POINT('Ctrl Pts',(54.3972593461681,-6.03272551876107,-0.554247372267884));
#67664=CARTESIAN_POINT('Ctrl Pts',(54.4978292561259,-5.03673015697496,-3.36635267093772));
#67665=CARTESIAN_POINT('Ctrl Pts',(54.5983991660837,-2.81932673497138,-5.36212430946776));
#67666=CARTESIAN_POINT('Ctrl Pts',(54.6989690760415,0.0817505558831741,
-6.05757765920217));
#67667=CARTESIAN_POINT('Ctrl Pts',(54.7995389859993,2.96302383524132,-5.28408882816219));
#67668=CARTESIAN_POINT('Ctrl Pts',(54.9001088959571,5.12572640282613,-3.22918327964378));
#67669=CARTESIAN_POINT('Ctrl Pts',(55.000678805915,6.04552299830646,-0.391261761841782));
#67670=CARTESIAN_POINT('Ctrl Pts',(55.1012487158727,5.49913211454772,2.54165449878592));
#67671=CARTESIAN_POINT('Ctrl Pts',(55.2018186258305,3.6195084315661,4.85799622605417));
#67672=CARTESIAN_POINT('Ctrl Pts',(55.3023885357883,0.861545917421489,5.99674298766766));
#67673=CARTESIAN_POINT('Ctrl Pts',(55.3694351424269,-1.11543236559086,5.78565164753667));
#67674=CARTESIAN_POINT('Ctrl Pts',(55.4029584457461,-2.01944986373189,5.45072012049539));
#67675=CARTESIAN_POINT('Ctrl Pts',(18.7300198469368,-2.68895233313972,5.4170743448565));
#67676=CARTESIAN_POINT('Ctrl Pts',(18.7635431502561,-3.58738958330546,4.97110392129998));
#67677=CARTESIAN_POINT('Ctrl Pts',(18.8305897568946,-5.15720935627613,3.62400206174433));
#67678=CARTESIAN_POINT('Ctrl Pts',(18.9311596668524,-6.26143937167068,0.722616114702605));
#67679=CARTESIAN_POINT('Ctrl Pts',(19.0317295768102,-5.84719208744128,-2.35320906805725));
#67680=CARTESIAN_POINT('Ctrl Pts',(19.1322994867681,-4.01505030444853,-4.85877268109136));
#67681=CARTESIAN_POINT('Ctrl Pts',(19.2328693967258,-1.209239348121,-6.18589055396794));
#67682=CARTESIAN_POINT('Ctrl Pts',(19.3334393066836,1.88979937725391,-6.01303608743097));
#67683=CARTESIAN_POINT('Ctrl Pts',(19.4340092166414,4.53056937621935,-4.3819740585053));
#67684=CARTESIAN_POINT('Ctrl Pts',(19.5345791265992,6.0726771378643,-1.68831339839199));
#67685=CARTESIAN_POINT('Ctrl Pts',(19.635149036557,6.14216748646266,1.41477524815045));
#67686=CARTESIAN_POINT('Ctrl Pts',(19.7357189465149,4.72218670714282,4.17477524750178));
#67687=CARTESIAN_POINT('Ctrl Pts',(19.8362888564726,2.15708012498876,5.92239935194035));
#67688=CARTESIAN_POINT('Ctrl Pts',(19.9368587664304,-0.9311167393973,6.23384491889024));
#67689=CARTESIAN_POINT('Ctrl Pts',(20.0374286763883,-3.79351848932746,5.0335893753062));
#67690=CARTESIAN_POINT('Ctrl Pts',(20.137998586346,-5.7359953256746,2.61269227323296));
#67691=CARTESIAN_POINT('Ctrl Pts',(20.2385684963038,-6.28749820540378,-0.44178021687973));
#67692=CARTESIAN_POINT('Ctrl Pts',(20.3391384062616,-5.31428819701165,-3.38912150688244));
#67693=CARTESIAN_POINT('Ctrl Pts',(20.4397083162195,-3.052367868265,-5.51460368648902));
#67694=CARTESIAN_POINT('Ctrl Pts',(20.5402782261772,-0.0502509627448719,
-6.3027992511492));
#67695=CARTESIAN_POINT('Ctrl Pts',(20.6408481361351,2.96405175988155,-5.56257140673792));
#67696=CARTESIAN_POINT('Ctrl Pts',(20.7414180460928,5.25957448130762,-3.47342479294108));
#67697=CARTESIAN_POINT('Ctrl Pts',(20.8419879560507,6.27965491910467,-0.541975652624894));
#67698=CARTESIAN_POINT('Ctrl Pts',(20.9425578660084,5.7769244444727,2.52090211473068));
#67699=CARTESIAN_POINT('Ctrl Pts',(21.0431277759663,3.87329476512769,4.97246329043967));
#67700=CARTESIAN_POINT('Ctrl Pts',(21.1436976859241,1.03039443941634,6.21820639808852));
#67701=CARTESIAN_POINT('Ctrl Pts',(21.2442675958818,-2.06237565082662,5.95603980730125));
#67702=CARTESIAN_POINT('Ctrl Pts',(21.3448375058397,-4.65502142111349,4.24953869022517));
#67703=CARTESIAN_POINT('Ctrl Pts',(21.4454074157974,-6.11882850394745,1.51252809896995));
#67704=CARTESIAN_POINT('Ctrl Pts',(21.5459773257553,-6.09882494184173,-1.5912692542966));
#67705=CARTESIAN_POINT('Ctrl Pts',(21.6465472357131,-4.59986158138049,-4.30918518318667));
#67706=CARTESIAN_POINT('Ctrl Pts',(21.7471171456709,-1.98543574712842,-5.98212741463425));
#67707=CARTESIAN_POINT('Ctrl Pts',(21.8476870556287,1.11045654668285,-6.2044088976147));
#67708=CARTESIAN_POINT('Ctrl Pts',(21.9482569655865,3.93706408383606,-4.92212656385934));
#67709=CARTESIAN_POINT('Ctrl Pts',(22.0488268755443,5.80893696979688,-2.44623277547445));
#67710=CARTESIAN_POINT('Ctrl Pts',(22.1493967855021,6.27214764108139,0.622870355174984));
#67711=CARTESIAN_POINT('Ctrl Pts',(22.2499666954599,5.21436790864827,3.54092796087949));
#67712=CARTESIAN_POINT('Ctrl Pts',(22.3505366054177,2.89210844704538,5.60031358420288));
#67713=CARTESIAN_POINT('Ctrl Pts',(22.4511065153755,-0.131484823356128,
6.30162798426772));
#67714=CARTESIAN_POINT('Ctrl Pts',(22.5516764253333,-3.12319313727969,5.47480302276966));
#67715=CARTESIAN_POINT('Ctrl Pts',(22.6522463352911,-5.35752980394714,3.32034304111744));
#67716=CARTESIAN_POINT('Ctrl Pts',(22.7528162452489,-6.2926701050727,0.360702730240734));
#67717=CARTESIAN_POINT('Ctrl Pts',(22.8533861552067,-5.70184332262903,-2.68640768221608));
#67718=CARTESIAN_POINT('Ctrl Pts',(22.9539560651645,-3.72832444275807,-5.08206654427227));
#67719=CARTESIAN_POINT('Ctrl Pts',(23.0545259751223,-0.850690094966891,
-6.24532864413108));
#67720=CARTESIAN_POINT('Ctrl Pts',(23.1550958850801,2.23323586855536,-5.89410392394609));
#67721=CARTESIAN_POINT('Ctrl Pts',(23.2556657950379,4.77560405638639,-4.11356407601786));
#67722=CARTESIAN_POINT('Ctrl Pts',(23.3562357049957,6.15989237152066,-1.33548848072923));
#67723=CARTESIAN_POINT('Ctrl Pts',(23.4568056149535,6.05041208917317,1.76644192150945));
#67724=CARTESIAN_POINT('Ctrl Pts',(23.5573755249113,4.47371208356945,4.44001167838594));
#67725=CARTESIAN_POINT('Ctrl Pts',(23.6579454348691,1.81214074879979,6.03688242534326));
#67726=CARTESIAN_POINT('Ctrl Pts',(23.7585153448269,-1.2888731576111,6.16981438087633));
#67727=CARTESIAN_POINT('Ctrl Pts',(23.8590852547847,-4.07733643280026,4.80657166020007));
#67728=CARTESIAN_POINT('Ctrl Pts',(23.9596551647425,-5.87704913292351,2.27773944956002));
#67729=CARTESIAN_POINT('Ctrl Pts',(24.0602250747003,-6.25158247744522,-0.803442616854901));
#67730=CARTESIAN_POINT('Ctrl Pts',(24.1607949846581,-5.11011245272797,-3.68979054030895));
#67731=CARTESIAN_POINT('Ctrl Pts',(24.2613648946159,-2.72944455715552,-5.6813674340156));
#67732=CARTESIAN_POINT('Ctrl Pts',(24.3619348045737,0.313111293942983,-6.29521761565747));
#67733=CARTESIAN_POINT('Ctrl Pts',(24.4625047145315,3.2797379257955,-5.38248294460629));
#67734=CARTESIAN_POINT('Ctrl Pts',(24.5630746244893,5.45103093393507,-3.16450079288374));
#67735=CARTESIAN_POINT('Ctrl Pts',(24.6636445344471,6.30045363299915,-0.179129922979928));
#67736=CARTESIAN_POINT('Ctrl Pts',(24.7642144444049,5.62202174967209,2.84967979904634));
#67737=CARTESIAN_POINT('Ctrl Pts',(24.8647843543627,3.58025443164712,5.18744462288997));
#67738=CARTESIAN_POINT('Ctrl Pts',(24.9653542643205,0.670278495933398,6.26725859118388));
#67739=CARTESIAN_POINT('Ctrl Pts',(25.0659241742783,-2.4022393980492,5.82726774615162));
#67740=CARTESIAN_POINT('Ctrl Pts',(25.1664940842361,-4.89221630592146,3.9741694889568));
#67741=CARTESIAN_POINT('Ctrl Pts',(25.2670639941939,-6.19583497096784,1.15733855176901));
#67742=CARTESIAN_POINT('Ctrl Pts',(25.3676339041517,-5.99696898910696,-1.94014598795254));
#67743=CARTESIAN_POINT('Ctrl Pts',(25.4682038141095,-4.34384318975053,-4.5671467957289));
#67744=CARTESIAN_POINT('Ctrl Pts',(25.5687737240674,-1.63733915618441,-6.08661843707195));
#67745=CARTESIAN_POINT('Ctrl Pts',(25.6693436340251,1.46621821328794,-6.13009034696077));
#67746=CARTESIAN_POINT('Ctrl Pts',(25.769913543983,4.21421892820066,-4.68702062466917));
#67747=CARTESIAN_POINT('Ctrl Pts',(25.8704834539407,5.94027518074521,-2.10735243561707));
#67748=CARTESIAN_POINT('Ctrl Pts',(25.9710533638985,6.22581981551831,0.983346905002763));
#67749=CARTESIAN_POINT('Ctrl Pts',(26.0716232738563,5.00160850439243,3.83558546765264));
#67750=CARTESIAN_POINT('Ctrl Pts',(26.1721931838142,2.56451143647945,5.75769785617871));
#67751=CARTESIAN_POINT('Ctrl Pts',(26.2727630937719,-0.494477447174819,
6.2835734709729));
#67752=CARTESIAN_POINT('Ctrl Pts',(26.3733330037298,-3.43355597554957,5.28568792813638));
#67753=CARTESIAN_POINT('Ctrl Pts',(26.4739029136875,-5.54000013555698,3.00602761279857));
#67754=CARTESIAN_POINT('Ctrl Pts',(26.5744728236454,-6.30299903168285,-0.0025918109681364));
#67755=CARTESIAN_POINT('Ctrl Pts',(26.6750427336031,-5.53752608842792,-3.01058272280617));
#67756=CARTESIAN_POINT('Ctrl Pts',(26.775612643561,-3.42920783559051,-5.28850991595965));
#67757=CARTESIAN_POINT('Ctrl Pts',(26.8761825535188,-0.489309634582833,
-6.28397800699392));
#67758=CARTESIAN_POINT('Ctrl Pts',(26.9767524634765,2.5692457315994,-5.75558684076064));
#67759=CARTESIAN_POINT('Ctrl Pts',(27.0773223734344,5.0047612195492,-3.83147082021713));
#67760=CARTESIAN_POINT('Ctrl Pts',(27.1778922833922,6.22662642000029,-0.978226424010917));
#67761=CARTESIAN_POINT('Ctrl Pts',(27.27846219335,5.93854007365992,2.11223703793258));
#67762=CARTESIAN_POINT('Ctrl Pts',(27.3790321033077,4.2103628715226,4.69048483645164));
#67763=CARTESIAN_POINT('Ctrl Pts',(27.4796020132656,1.46117629744218,6.13129409983505));
#67764=CARTESIAN_POINT('Ctrl Pts',(27.5801719232234,-1.64234427094553,6.08526982200225));
#67765=CARTESIAN_POINT('Ctrl Pts',(27.6807418331812,-4.34759776740598,4.56357285070868));
#67766=CARTESIAN_POINT('Ctrl Pts',(27.781311743139,-5.99856254780733,1.93521339157265));
#67767=CARTESIAN_POINT('Ctrl Pts',(27.8818816530967,-6.19488107410007,-1.16243364913257));
#67768=CARTESIAN_POINT('Ctrl Pts',(27.9824515630546,-4.88894627265482,-3.97819153057936));
#67769=CARTESIAN_POINT('Ctrl Pts',(28.0830214730123,-2.39744620863596,-5.829241390402));
#67770=CARTESIAN_POINT('Ctrl Pts',(28.1835913829702,0.675432497186664,-6.26670523103035));
#67771=CARTESIAN_POINT('Ctrl Pts',(28.284161292928,3.58451940387321,-5.1844984476934));
#67772=CARTESIAN_POINT('Ctrl Pts',(28.3847312028858,5.6243634407776,-2.84505525375576));
#67773=CARTESIAN_POINT('Ctrl Pts',(28.4853011128436,6.30030418490677,0.18431139011253));
#67774=CARTESIAN_POINT('Ctrl Pts',(28.5858710228014,5.44842658767854,3.16898268053903));
#67775=CARTESIAN_POINT('Ctrl Pts',(28.6864409327592,3.27531023310016,5.38517839888599));
#67776=CARTESIAN_POINT('Ctrl Pts',(28.787010842717,0.307933966475966,6.2954729912191));
#67777=CARTESIAN_POINT('Ctrl Pts',(28.8875807526748,-2.73411602194027,5.6791208025053));
#67778=CARTESIAN_POINT('Ctrl Pts',(28.9881506626326,-5.11314522864148,3.685586707934));
#67779=CARTESIAN_POINT('Ctrl Pts',(29.0887205725904,-6.25224111893916,0.798301009347454));
#67780=CARTESIAN_POINT('Ctrl Pts',(29.1892904825482,-5.87517392000258,-2.28257199680546));
#67781=CARTESIAN_POINT('Ctrl Pts',(29.289860392506,-4.07338210298355,-4.80992325863648));
#67782=CARTESIAN_POINT('Ctrl Pts',(29.3904303024638,-1.28379863247516,-6.17087227076803));
#67783=CARTESIAN_POINT('Ctrl Pts',(29.4910002124216,1.81710490127779,-6.03539006930216));
#67784=CARTESIAN_POINT('Ctrl Pts',(29.5915701223794,4.47736206068688,-4.43633097146737));
#67785=CARTESIAN_POINT('Ctrl Pts',(29.6921400323372,6.05186277462106,-1.76146543197267));
#67786=CARTESIAN_POINT('Ctrl Pts',(29.792709942295,6.15879197532669,1.34055395845544));
#67787=CARTESIAN_POINT('Ctrl Pts',(29.8932798522528,4.77221942368032,4.11749016794541));
#67788=CARTESIAN_POINT('Ctrl Pts',(29.9938497622106,2.22838776985482,5.89593855616223));
#67789=CARTESIAN_POINT('Ctrl Pts',(30.0944196721684,-0.855825999900363,
6.24462691990268));
#67790=CARTESIAN_POINT('Ctrl Pts',(30.1949895821262,-3.73250270139929,5.07899863112071));
#67791=CARTESIAN_POINT('Ctrl Pts',(30.295559492084,-5.70405071085424,2.6817175464396));
#67792=CARTESIAN_POINT('Ctrl Pts',(30.3961294020418,-6.29237133313748,-0.365877734753705));
#67793=CARTESIAN_POINT('Ctrl Pts',(30.4966993119996,-5.35479732378858,-3.32474798022731));
#67794=CARTESIAN_POINT('Ctrl Pts',(30.5972692219574,-3.11868957298405,-5.47736970253418));
#67795=CARTESIAN_POINT('Ctrl Pts',(30.6978391319152,-0.12630228538831,-6.30173398705345));
#67796=CARTESIAN_POINT('Ctrl Pts',(30.798409041873,2.89671319768946,-5.59793320442559));
#67797=CARTESIAN_POINT('Ctrl Pts',(30.8989789518308,5.21727822390134,-3.53663843858597));
#67798=CARTESIAN_POINT('Ctrl Pts',(30.9995488617886,6.27265777199985,-0.61771189582904));
#67799=CARTESIAN_POINT('Ctrl Pts',(31.1001187717464,5.80692321007211,2.45100924992232));
#67800=CARTESIAN_POINT('Ctrl Pts',(31.2006886817042,3.9330147684679,4.92536276246656));
#67801=CARTESIAN_POINT('Ctrl Pts',(31.301258591662,1.10535363116214,6.20532004500618));
#67802=CARTESIAN_POINT('Ctrl Pts',(31.4018285016199,-1.99035481018033,5.98049255834927));
#67803=CARTESIAN_POINT('Ctrl Pts',(31.5023984115776,-4.60340392340859,4.30540077447214));
#67804=CARTESIAN_POINT('Ctrl Pts',(31.6029683215354,-6.10013154795234,1.58625300899802));
#67805=CARTESIAN_POINT('Ctrl Pts',(31.7035382314932,-6.11758252328589,-1.51755974566603));
#67806=CARTESIAN_POINT('Ctrl Pts',(31.804108141451,-4.65152500291308,-4.25336556836506));
#67807=CARTESIAN_POINT('Ctrl Pts',(31.9046780514089,-2.05747667349994,-5.95773390215462));
#67808=CARTESIAN_POINT('Ctrl Pts',(32.0052479613666,1.03550797810202,-6.21735689325986));
#67809=CARTESIAN_POINT('Ctrl Pts',(32.1058178713245,3.87738283640918,-4.9692761898287));
#67810=CARTESIAN_POINT('Ctrl Pts',(32.2063877812822,5.77899569464942,-2.51615028805955));
#67811=CARTESIAN_POINT('Ctrl Pts',(32.30695769124,6.27920707166246,0.547139892589688));
#67812=CARTESIAN_POINT('Ctrl Pts',(32.4075276011978,5.25671613911887,3.47774912027968));
#67813=CARTESIAN_POINT('Ctrl Pts',(32.5080975111557,2.95947606797094,5.56500718004803));
#67814=CARTESIAN_POINT('Ctrl Pts',(32.6086674211134,-0.0554344020580869,
6.3027557891725));
#67815=CARTESIAN_POINT('Ctrl Pts',(32.7092373310713,-3.05690207730752,5.51209154501553));
#67816=CARTESIAN_POINT('Ctrl Pts',(32.809807241029,-5.31707363027884,3.38474984615883));
#67817=CARTESIAN_POINT('Ctrl Pts',(32.9103771509868,-6.28785940499703,0.436609223298352));
#67818=CARTESIAN_POINT('Ctrl Pts',(33.0109470609447,-5.73384468677316,-2.61740876036626));
#67819=CARTESIAN_POINT('Ctrl Pts',(33.1115169709025,-3.78937756786474,-5.03670737278258));
#67820=CARTESIAN_POINT('Ctrl Pts',(33.2120868808602,-0.925989650754001,
-6.23460878304126));
#67821=CARTESIAN_POINT('Ctrl Pts',(33.3126567908181,2.16194995954613,-5.92062293034251));
#67822=CARTESIAN_POINT('Ctrl Pts',(33.4132267007759,4.72561856572486,-4.17089111367767));
#67823=CARTESIAN_POINT('Ctrl Pts',(33.5137966107337,6.14332873766329,-1.40972179236871));
#67824=CARTESIAN_POINT('Ctrl Pts',(33.6143665206914,6.07128697907194,1.69330385006073));
#67825=CARTESIAN_POINT('Ctrl Pts',(33.7149364306493,4.52696335439357,4.38570476649495));
#67826=CARTESIAN_POINT('Ctrl Pts',(33.8155063406071,1.88485501321466,6.01457605239459));
#67827=CARTESIAN_POINT('Ctrl Pts',(33.9160762505649,-1.21432904613156,6.18491782310809));
#67828=CARTESIAN_POINT('Ctrl Pts',(34.0166461605227,-4.01903935712015,4.8554223458725));
#67829=CARTESIAN_POINT('Ctrl Pts',(34.1172160704805,-5.84913608371143,2.34849112944965));
#67830=CARTESIAN_POINT('Ctrl Pts',(34.2177859804383,-6.2608223451068,-0.727947164216232));
#67831=CARTESIAN_POINT('Ctrl Pts',(34.3183558903961,-5.15426457730915,-3.62785889719748));
#67832=CARTESIAN_POINT('Ctrl Pts',(34.4189258003539,-2.79780208645283,-5.6480179705733));
#67833=CARTESIAN_POINT('Ctrl Pts',(34.5194957103117,0.237125001940042,-6.29853754806097));
#67834=CARTESIAN_POINT('Ctrl Pts',(34.6200656202695,3.21454948148645,-5.42166719210558));
#67835=CARTESIAN_POINT('Ctrl Pts',(34.7206355302273,5.41244847894878,-3.2300472091912));
#67836=CARTESIAN_POINT('Ctrl Pts',(34.8212054401851,6.29783337945691,-0.255143558565227));
#67837=CARTESIAN_POINT('Ctrl Pts',(34.9217753501429,5.6559991068023,2.78163218537792));
#67838=CARTESIAN_POINT('Ctrl Pts',(35.0223452601007,3.64258991959439,5.14386451887569));
#67839=CARTESIAN_POINT('Ctrl Pts',(35.1229151700585,0.745855812530698,6.2587141345322));
#67840=CARTESIAN_POINT('Ctrl Pts',(35.2234850800163,-2.33174768701761,5.85583096024525));
#67841=CARTESIAN_POINT('Ctrl Pts',(35.3240549899741,-4.84390437969943,4.03291381896607));
#67842=CARTESIAN_POINT('Ctrl Pts',(35.4246248999319,-6.18141843007595,1.23201854823549));
#67843=CARTESIAN_POINT('Ctrl Pts',(35.5251948098897,-6.01994383230129,-1.86764015988531));
#67844=CARTESIAN_POINT('Ctrl Pts',(35.6257647198475,-4.39863803733388,-4.51439773695212));
#67845=CARTESIAN_POINT('Ctrl Pts',(35.7263346298053,-1.71066630478676,-6.06641774893109));
#67846=CARTESIAN_POINT('Ctrl Pts',(35.8269045397631,1.39214053408053,-6.14733667894063));
#67847=CARTESIAN_POINT('Ctrl Pts',(35.9274744497209,4.15735449182779,-4.73753175611078));
#67848=CARTESIAN_POINT('Ctrl Pts',(36.0280443596787,5.91441356407679,-2.17887946062728));
#67849=CARTESIAN_POINT('Ctrl Pts',(36.1286142696366,6.23723243833396,0.908149228416427));
#67850=CARTESIAN_POINT('Ctrl Pts',(36.2291841795942,5.04752781548373,3.77495251133004));
#67851=CARTESIAN_POINT('Ctrl Pts',(36.3297540895522,2.63380204243537,5.72633305983351));
#67852=CARTESIAN_POINT('Ctrl Pts',(36.4303239995099,-0.418618458651225,
6.28908277071906));
#67853=CARTESIAN_POINT('Ctrl Pts',(36.5308939094677,-3.36952434387368,5.32673532352805));
#67854=CARTESIAN_POINT('Ctrl Pts',(36.6314638194255,-5.50332347628994,3.07265914578803));
#67855=CARTESIAN_POINT('Ctrl Pts',(36.7320337293833,-6.30257140312459,0.0734657702275063));
#67856=CARTESIAN_POINT('Ctrl Pts',(36.8326036393411,-5.57345119013571,-2.9435429913717));
#67857=CARTESIAN_POINT('Ctrl Pts',(36.9331735492989,-3.49277386132561,-5.24674511144952));
#67858=CARTESIAN_POINT('Ctrl Pts',(37.0337434592567,-0.565101877823921,
-6.27761605854952));
#67859=CARTESIAN_POINT('Ctrl Pts',(37.1343133692145,2.49960682459419,-5.78617051540318));
#67860=CARTESIAN_POINT('Ctrl Pts',(37.2348832791723,4.95816302378145,-3.89158360317305));
#67861=CARTESIAN_POINT('Ctrl Pts',(37.3354531891301,6.21436895783059,-1.05329101716025));
#67862=CARTESIAN_POINT('Ctrl Pts',(37.4360230990879,5.96359576911283,2.04042373381078));
#67863=CARTESIAN_POINT('Ctrl Pts',(37.5365930090457,4.26665574001952,4.63933748578796));
#67864=CARTESIAN_POINT('Ctrl Pts',(37.6371629190035,1.53505536683108,6.11321589113635));
#67865=CARTESIAN_POINT('Ctrl Pts',(37.7377328289614,-1.56879461139425,6.10464470531572));
#67866=CARTESIAN_POINT('Ctrl Pts',(37.8383027389191,-4.29221324681985,4.61570243350924));
#67867=CARTESIAN_POINT('Ctrl Pts',(37.938872648877,-5.97477386475187,2.00745629490579));
#67868=CARTESIAN_POINT('Ctrl Pts',(38.0394425588347,-6.20845696373824,-1.08759626713632));
#67869=CARTESIAN_POINT('Ctrl Pts',(38.1400124687925,-4.93659459343594,-3.91890767063194));
#67870=CARTESIAN_POINT('Ctrl Pts',(38.2405823787503,-2.46761228378761,-5.79988733750746));
#67871=CARTESIAN_POINT('Ctrl Pts',(38.3411522887081,0.599763880487827,-6.27439931774677));
#67872=CARTESIAN_POINT('Ctrl Pts',(38.4417221986659,3.52169782003892,-5.22737486461532));
#67873=CARTESIAN_POINT('Ctrl Pts',(38.5422921086238,5.58962306980901,-2.91271650668886));
#67874=CARTESIAN_POINT('Ctrl Pts',(38.6428620185815,6.30206953685826,0.108273096759718));
#67875=CARTESIAN_POINT('Ctrl Pts',(38.7434319285394,5.4862695662216,3.10300656744865));
#67876=CARTESIAN_POINT('Ctrl Pts',(38.8440018384971,3.34005394851439,5.34526361668836));
#67877=CARTESIAN_POINT('Ctrl Pts',(38.944571748455,0.38387812350663,6.29129884023737));
#67878=CARTESIAN_POINT('Ctrl Pts',(39.0451416584127,-2.6653878159982,5.71169951075923));
#67879=CARTESIAN_POINT('Ctrl Pts',(39.1457115683706,-5.06829950456569,3.74701796671673));
#67880=CARTESIAN_POINT('Ctrl Pts',(39.2462814783283,-6.24215292621357,0.873687791285975));
#67881=CARTESIAN_POINT('Ctrl Pts',(39.3468513882862,-5.90228963667894,-2.21151092143611));
#67882=CARTESIAN_POINT('Ctrl Pts',(39.447421298244,-4.13112619110987,-4.76042013944201));
#67883=CARTESIAN_POINT('Ctrl Pts',(39.5479912082017,-1.35816820038853,-6.15493157153938));
#67884=CARTESIAN_POINT('Ctrl Pts',(39.6485611181596,1.74414440977687,-6.05687739588006));
#67885=CARTESIAN_POINT('Ctrl Pts',(39.7491310281174,4.42350350198092,-4.49003566565361));
#67886=CARTESIAN_POINT('Ctrl Pts',(39.8497009380751,6.03016680283326,-1.8343641516576));
#67887=CARTESIAN_POINT('Ctrl Pts',(39.950270848033,6.17451984493906,1.26613909004208));
#67888=CARTESIAN_POINT('Ctrl Pts',(40.0508407579908,4.82155713985089,4.05960469233543));
#67889=CARTESIAN_POINT('Ctrl Pts',(40.1514106679486,2.29937097888354,5.86861965136154));
#67890=CARTESIAN_POINT('Ctrl Pts',(40.2519805779064,-0.780410665098583,
6.25449939680861));
#67891=CARTESIAN_POINT('Ctrl Pts',(40.3525504878642,-3.67094339459419,5.12366842258203));
#67892=CARTESIAN_POINT('Ctrl Pts',(40.453120397822,-5.67127551095404,2.75035226648001));
#67893=CARTESIAN_POINT('Ctrl Pts',(40.5536903077798,-6.29632819790416,-0.289921946661285));
#67894=CARTESIAN_POINT('Ctrl Pts',(40.6542602177376,-5.39452671692239,-3.25989033731036));
#67895=CARTESIAN_POINT('Ctrl Pts',(40.7548301276954,-3.18455715085024,-5.43933812736875));
#67896=CARTESIAN_POINT('Ctrl Pts',(40.8554000376532,-0.202335217055038,
-6.29975110387848));
#67897=CARTESIAN_POINT('Ctrl Pts',(40.955969947611,2.82895283270006,-5.63247986070409));
#67898=CARTESIAN_POINT('Ctrl Pts',(41.0565398575688,5.17422225576911,-3.59933709990915));
#67899=CARTESIAN_POINT('Ctrl Pts',(41.1571097675266,6.26474723593307,-0.693358190798846));
#67900=CARTESIAN_POINT('Ctrl Pts',(41.2576796774844,5.83607640425734,2.38075948271757));
#67901=CARTESIAN_POINT('Ctrl Pts',(41.3582495874421,3.99216206841114,4.87754503110101));
#67902=CARTESIAN_POINT('Ctrl Pts',(41.4588194974001,1.18015186754284,6.1915301081731));
#67903=CARTESIAN_POINT('Ctrl Pts',(41.5593894073578,-1.91804414529604,6.0040744638599));
#67904=CARTESIAN_POINT('Ctrl Pts',(41.6599593173156,-4.55111610400801,4.36063593054014));
#67905=CARTESIAN_POINT('Ctrl Pts',(41.7605292272734,-6.08054632522933,1.65974693782488));
#67906=CARTESIAN_POINT('Ctrl Pts',(41.8610991372312,-6.13544929689117,-1.44362925855516));
#67907=CARTESIAN_POINT('Ctrl Pts',(41.961669047189,-4.70251109562762,-4.19692660245303));
#67908=CARTESIAN_POINT('Ctrl Pts',(42.0622389571469,-2.12921800173078,-5.93247285809084));
#67909=CARTESIAN_POINT('Ctrl Pts',(42.1628088671045,0.96040862469385,-6.22939955248438));
#67910=CARTESIAN_POINT('Ctrl Pts',(42.2633787770625,3.81713698637752,-5.01570221784623));
#67911=CARTESIAN_POINT('Ctrl Pts',(42.3639486870201,5.74821291476561,-2.5857014130407));
#67912=CARTESIAN_POINT('Ctrl Pts',(42.4645185969781,6.28535215954959,0.471329758581282));
#67913=CARTESIAN_POINT('Ctrl Pts',(42.5650885069357,5.29829891625416,3.41406386948147));
#67914=CARTESIAN_POINT('Ctrl Pts',(42.6656584168937,3.02641274669477,5.52889043095649));
#67915=CARTESIAN_POINT('Ctrl Pts',(42.7662283268514,0.0206240912847744,
6.30296582235201));
#67916=CARTESIAN_POINT('Ctrl Pts',(42.8667982368092,-2.99016588850797,5.5485774276009));
#67917=CARTESIAN_POINT('Ctrl Pts',(42.967368146767,-5.2758432143581,3.44866378303112));
#67918=CARTESIAN_POINT('Ctrl Pts',(43.0679380567248,-6.2821331023235,0.512452139784996));
#67919=CARTESIAN_POINT('Ctrl Pts',(43.1685079666826,-5.76501112081578,-2.54802870622549));
#67920=CARTESIAN_POINT('Ctrl Pts',(43.2690778766404,-3.84987890519716,-4.99061478439249));
#67921=CARTESIAN_POINT('Ctrl Pts',(43.3696477865983,-1.00115436915438,-6.22298107340863));
#67922=CARTESIAN_POINT('Ctrl Pts',(43.470217696556,2.09034923958594,-5.94627980904374));
#67923=CARTESIAN_POINT('Ctrl Pts',(43.5707876065138,4.67494495715925,-4.22761080971396));
#67924=CARTESIAN_POINT('Ctrl Pts',(43.6713575164716,6.12587054694812,-1.48374982827714));
#67925=CARTESIAN_POINT('Ctrl Pts',(43.7719274264294,6.09127780242711,1.61991920926246));
#67926=CARTESIAN_POINT('Ctrl Pts',(43.8724973363872,4.57955543436417,4.33075923302884));
#67927=CARTESIAN_POINT('Ctrl Pts',(43.973067246345,1.95729481568055,5.99139387082747));
#67928=CARTESIAN_POINT('Ctrl Pts',(44.0736371563028,-1.13960811091008,6.19912065251409));
#67929=CARTESIAN_POINT('Ctrl Pts',(44.1742070662607,-3.96015705161237,4.9035660123469));
#67930=CARTESIAN_POINT('Ctrl Pts',(44.2747769762184,-5.82037131631542,2.41890083531584));
#67931=CARTESIAN_POINT('Ctrl Pts',(44.3753468861763,-6.26915054715452,-0.652345712020124));
#67932=CARTESIAN_POINT('Ctrl Pts',(44.475916796134,-5.19766616697324,-3.56539898574908));
#67933=CARTESIAN_POINT('Ctrl Pts',(44.5764867060918,-2.86575221560104,-5.61384607463161));
#67934=CARTESIAN_POINT('Ctrl Pts',(44.6770566160497,0.161104181132725,-6.30094032297563));
#67935=CARTESIAN_POINT('Ctrl Pts',(44.7776265260074,3.14889295262483,-5.46006196702825));
#67936=CARTESIAN_POINT('Ctrl Pts',(44.8781964359653,5.37307789376282,-3.29512328425448));
#67937=CARTESIAN_POINT('Ctrl Pts',(44.978766345923,6.29429607096292,-0.331120041585609));
#67938=CARTESIAN_POINT('Ctrl Pts',(45.0793362558809,5.68915286926505,2.71317952613023));
#67939=CARTESIAN_POINT('Ctrl Pts',(45.1799061658387,3.7043949941563,5.09953539434219));
#67940=CARTESIAN_POINT('Ctrl Pts',(45.2804760757965,0.821324521814106,6.24925831925242));
#67941=CARTESIAN_POINT('Ctrl Pts',(45.3810459857542,-2.26091644004823,5.88354148128475));
#67942=CARTESIAN_POINT('Ctrl Pts',(45.4816158957121,-4.79488711146061,4.09107089882682));
#67943=CARTESIAN_POINT('Ctrl Pts',(45.5821858056699,-6.16610178592019,1.30651914511453));
#67944=CARTESIAN_POINT('Ctrl Pts',(45.6827557156277,-6.04204208525136,-1.79486237659897));
#67945=CARTESIAN_POINT('Ctrl Pts',(45.7833256255854,-4.4527923800721,-4.46099131705619));
#67946=CARTESIAN_POINT('Ctrl Pts',(45.8838955355434,-1.78374435581676,-6.04533370327649));
#67947=CARTESIAN_POINT('Ctrl Pts',(45.984465445501,1.31786013922577,-6.16368787044887));
#67948=CARTESIAN_POINT('Ctrl Pts',(46.085035355459,4.09988468495787,-4.78735303491675));
#67949=CARTESIAN_POINT('Ctrl Pts',(46.1856052654166,5.88769072388608,-2.25008920950809));
#67950=CARTESIAN_POINT('Ctrl Pts',(46.2861751753745,6.24773683056493,0.832819312265029));
#67951=CARTESIAN_POINT('Ctrl Pts',(46.3867450853323,5.09271213406274,3.71376986772862));
#67952=CARTESIAN_POINT('Ctrl Pts',(46.4873149952901,2.70270912900301,5.69413442718755));
#67953=CARTESIAN_POINT('Ctrl Pts',(46.5878849052478,-0.342698513270351,
6.29367628972773));
#67954=CARTESIAN_POINT('Ctrl Pts',(46.6884548152057,-3.30500206108037,5.36700706978603));
#67955=CARTESIAN_POINT('Ctrl Pts',(46.7890247251635,-5.46584545411902,3.13884325549484));
#67956=CARTESIAN_POINT('Ctrl Pts',(46.8895946351213,-6.30122602969034,0.149512653752343));
#67957=CARTESIAN_POINT('Ctrl Pts',(46.990164545079,-5.60856471733773,-2.87607463782029));
#67958=CARTESIAN_POINT('Ctrl Pts',(47.0907344550369,-3.5558312890441,-5.20421630552899));
#67959=CARTESIAN_POINT('Ctrl Pts',(47.1913043649946,-0.640811834118883,
-6.27033999908552));
#67960=CARTESIAN_POINT('Ctrl Pts',(47.2918742749525,2.42960393895095,-5.8159116405524));
#67961=CARTESIAN_POINT('Ctrl Pts',(47.3924441849103,4.910842848298,-3.95112971568884));
#67962=CARTESIAN_POINT('Ctrl Pts',(47.4930140948681,6.20120659432713,-1.1282022360165));
#67963=CARTESIAN_POINT('Ctrl Pts',(47.5935840048259,5.9877830794084,1.96831331470099));
#67964=CARTESIAN_POINT('Ctrl Pts',(47.6941539147837,4.32232732218855,4.58751458098405));
#67965=CARTESIAN_POINT('Ctrl Pts',(47.7947238247415,1.60871091012128,6.09424751044258));
#67966=CARTESIAN_POINT('Ctrl Pts',(47.8952937346993,-1.49501651282591,6.12313066472181));
#67967=CARTESIAN_POINT('Ctrl Pts',(47.9958636446571,-4.23620371836591,4.6671599037725));
#67968=CARTESIAN_POINT('Ctrl Pts',(48.0964335546149,-5.95011516884782,2.07940688378343));
#67969=CARTESIAN_POINT('Ctrl Pts',(48.1970034645728,-6.22112881291391,-1.01260051551003));
#67970=CARTESIAN_POINT('Ctrl Pts',(48.2975733745305,-4.98352407517448,-3.85905316146789));
#67971=CARTESIAN_POINT('Ctrl Pts',(48.3981432844883,-2.53741903916567,-5.7696887377534));
#67972=CARTESIAN_POINT('Ctrl Pts',(48.4987131944461,0.524007929557735,-6.28117976184725));
#67973=CARTESIAN_POINT('Ctrl Pts',(48.5992831044039,3.45836342644444,-5.26949010071282));
#67974=CARTESIAN_POINT('Ctrl Pts',(48.6998530143616,5.55406876947679,-2.97995362628372));
#67975=CARTESIAN_POINT('Ctrl Pts',(48.8004229243196,6.30291721701269,0.0322190372896381));
#67976=CARTESIAN_POINT('Ctrl Pts',(48.9009928342773,5.52331366515492,3.03657861205532));
#67977=CARTESIAN_POINT('Ctrl Pts',(49.0015627442351,3.40431130412388,5.30457048737156));
#67978=CARTESIAN_POINT('Ctrl Pts',(49.1021326541929,0.459766382371591,6.28620858582657));
#67979=CARTESIAN_POINT('Ctrl Pts',(49.2027025641507,-2.59627149132571,5.74344651356729));
#67980=CARTESIAN_POINT('Ctrl Pts',(49.3032724741086,-5.02271576332149,3.80790360589141));
#67981=CARTESIAN_POINT('Ctrl Pts',(49.4038423840663,-6.23115578640957,0.948947351739475));
#67982=CARTESIAN_POINT('Ctrl Pts',(49.5044122940242,-5.92854589525094,-2.14012781832817));
#67983=CARTESIAN_POINT('Ctrl Pts',(49.6049822039819,-4.18826872795629,-4.71022383473465));
#67984=CARTESIAN_POINT('Ctrl Pts',(49.7055521139398,-1.43233999951405,-6.13809462591371));
#67985=CARTESIAN_POINT('Ctrl Pts',(49.8061220238974,1.67092994581097,-6.07748275415662));
#67986=CARTESIAN_POINT('Ctrl Pts',(49.9066919338554,4.36900081766127,-4.54308654618796));
#67987=CARTESIAN_POINT('Ctrl Pts',(50.0072618438131,6.00759275218989,-1.90699576158792));
#67988=CARTESIAN_POINT('Ctrl Pts',(50.107831753771,6.18934861582061,1.19153985360055));
#67989=CARTESIAN_POINT('Ctrl Pts',(50.2084016637287,4.87019276808361,4.00112808000257));
#67990=CARTESIAN_POINT('Ctrl Pts',(50.3089715736866,2.37001936648793,5.84044619128974));
#67991=CARTESIAN_POINT('Ctrl Pts',(50.4095414836443,-0.704881691300416,
6.26346112881276));
#67992=CARTESIAN_POINT('Ctrl Pts',(50.5101113936022,-3.6088495457308,5.16759213436563));
#67993=CARTESIAN_POINT('Ctrl Pts',(50.6106813035599,-5.63767449192264,2.81858649574634));
#67994=CARTESIAN_POINT('Ctrl Pts',(50.7112512135177,-6.29936822689513,-0.213923941771339));
#67995=CARTESIAN_POINT('Ctrl Pts',(50.8118211234756,-5.43347058952238,-3.19455800756135));
#67996=CARTESIAN_POINT('Ctrl Pts',(50.9123910334333,-3.24996101147774,-5.40051450648485));
#67997=CARTESIAN_POINT('Ctrl Pts',(51.0129609433911,-0.278338685809411,
-6.29685088650358));
#67998=CARTESIAN_POINT('Ctrl Pts',(51.113530853349,2.76078053156579,-5.66620634705498));
#67999=CARTESIAN_POINT('Ctrl Pts',(51.2141007633068,5.13041284659533,-3.66151164607849));
#68000=CARTESIAN_POINT('Ctrl Pts',(51.3146706732645,6.25592446273203,-0.768903522862193));
#68001=CARTESIAN_POINT('Ctrl Pts',(51.4152405832224,5.86437978193538,2.31016304275399));
#68002=CARTESIAN_POINT('Ctrl Pts',(51.5158104931801,4.05072805224571,4.8290170591569));
#68003=CARTESIAN_POINT('Ctrl Pts',(51.616380403138,1.25477825686932,6.17683859567069));
#68004=CARTESIAN_POINT('Ctrl Pts',(51.7169503130957,-1.84545418564875,6.02678208993408));
#68005=CARTESIAN_POINT('Ctrl Pts',(51.8175202230536,-4.49816557676692,4.41523611541536));
#68006=CARTESIAN_POINT('Ctrl Pts',(51.9180901330113,-6.06007568766899,1.73299918367025));
#68007=CARTESIAN_POINT('Ctrl Pts',(52.0186600429692,-6.15242266099837,-1.36948855829945));
#68008=CARTESIAN_POINT('Ctrl Pts',(52.1192299529269,-4.75281243521733,-4.13987650377665));
#68009=CARTESIAN_POINT('Ctrl Pts',(52.2197998628848,-2.20064928525366,-5.90634796081224));
#68010=CARTESIAN_POINT('Ctrl Pts',(52.3203697728425,0.885169422002587,-6.24053512170498));
#68011=CARTESIAN_POINT('Ctrl Pts',(52.4209396828005,3.75633530640134,-5.06139788761504));
#68012=CARTESIAN_POINT('Ctrl Pts',(52.5215095927581,5.71659311256105,-2.65487602277651));
#68013=CARTESIAN_POINT('Ctrl Pts',(52.6220795027161,6.29058200992785,0.395450992195018));
#68014=CARTESIAN_POINT('Ctrl Pts',(52.7226494126737,5.33911018500865,3.34988148196873));
#68015=CARTESIAN_POINT('Ctrl Pts',(52.8232193226317,3.09290873626811,5.49196859605096));
#68016=CARTESIAN_POINT('Ctrl Pts',(52.9237892325893,0.0966795814783073,
6.30225805321166));
#68017=CARTESIAN_POINT('Ctrl Pts',(53.0243591425472,-2.92299428865657,5.58425535767847));
#68018=CARTESIAN_POINT('Ctrl Pts',(53.1249290525049,-5.23384455986985,3.51207554490642));
#68019=CARTESIAN_POINT('Ctrl Pts',(53.2254989624628,-6.27549203099247,0.588220435964089));
#68020=CARTESIAN_POINT('Ctrl Pts',(53.3260688724206,-5.79533808626437,-2.47827762268341));
#68021=CARTESIAN_POINT('Ctrl Pts',(53.4266387823784,-3.90981964530785,-4.94379549053544));
#68022=CARTESIAN_POINT('Ctrl Pts',(53.5272086923362,-1.0761733042926,-6.21044720899938));
#68023=CARTESIAN_POINT('Ctrl Pts',(53.627778602294,2.01844413317511,-5.97107082285632));
#68024=CARTESIAN_POINT('Ctrl Pts',(53.7283485122517,4.62359061261052,-4.28371490724156));
#68025=CARTESIAN_POINT('Ctrl Pts',(53.8289184222097,6.10752033543931,-1.55756180437573));
#68026=CARTESIAN_POINT('Ctrl Pts',(53.9294883321674,6.11038166022464,1.54629867609741));
#68027=CARTESIAN_POINT('Ctrl Pts',(54.0300582421252,4.63148064195728,4.27518309621438));
#68028=CARTESIAN_POINT('Ctrl Pts',(54.130628152083,2.02944965364622,5.96733922230733));
#68029=CARTESIAN_POINT('Ctrl Pts',(54.2311980620408,-1.06472132187648,6.21242086748847));
#68030=CARTESIAN_POINT('Ctrl Pts',(54.3317679719986,-3.90069791524047,4.95099551900406));
#68031=CARTESIAN_POINT('Ctrl Pts',(54.4323378819564,-5.79075936208739,2.48895856933826));
#68032=CARTESIAN_POINT('Ctrl Pts',(54.5329077919142,-6.27656519998693,-0.576649767694941));
#68033=CARTESIAN_POINT('Ctrl Pts',(54.633477701872,-5.24031221488195,-3.50241892484281));
#68034=CARTESIAN_POINT('Ctrl Pts',(54.7340476118299,-2.93328248021272,-5.57885863266014));
#68035=CARTESIAN_POINT('Ctrl Pts',(54.8346175217876,0.085054871556865,-6.30242185123897));
#68036=CARTESIAN_POINT('Ctrl Pts',(54.9351874317455,3.0827877438102,-5.49766899709598));
#68037=CARTESIAN_POINT('Ctrl Pts',(55.0357573417032,5.33290564349095,-3.35970521688084));
#68038=CARTESIAN_POINT('Ctrl Pts',(55.1363272516611,6.28987994711282,-0.407076362222084));
#68039=CARTESIAN_POINT('Ctrl Pts',(55.2368971616187,5.72140422317592,2.64438687420114));
#68040=CARTESIAN_POINT('Ctrl Pts',(55.3374670715767,3.76580711188938,5.05435394985144));
#68041=CARTESIAN_POINT('Ctrl Pts',(55.4380369815344,0.896369162936647,6.23912827338287));
#68042=CARTESIAN_POINT('Ctrl Pts',(55.505083588173,-1.16051757154113,6.01950472920463));
#68043=CARTESIAN_POINT('Ctrl Pts',(55.5386068914922,-2.10107499477635,5.67103544107472));
#68044=CARTESIAN_POINT('Ctrl Pts',(18.8656682926829,-2.79341604200804,5.62752347417158));
#68045=CARTESIAN_POINT('Ctrl Pts',(18.8991915960022,-3.72675688127093,5.16422744617198));
#68046=CARTESIAN_POINT('Ctrl Pts',(18.9662382026407,-5.35756293269594,3.76479172604979));
#68047=CARTESIAN_POINT('Ctrl Pts',(19.0668081125985,-6.50469142621899,0.75068918929729));
#68048=CARTESIAN_POINT('Ctrl Pts',(19.1673780225563,-6.07435095686098,-2.44462941194441));
#68049=CARTESIAN_POINT('Ctrl Pts',(19.2679479325142,-4.17103188914465,-5.04753222456091));
#68050=CARTESIAN_POINT('Ctrl Pts',(19.3685178424719,-1.2562173572353,-6.42620759564877));
#68051=CARTESIAN_POINT('Ctrl Pts',(19.4690877524297,1.9632166147155,-6.24663786739205));
#68052=CARTESIAN_POINT('Ctrl Pts',(19.5696576623875,4.70657847630348,-4.55221034595246));
#68053=CARTESIAN_POINT('Ctrl Pts',(19.6702275723453,6.30859592629457,-1.75390306212622));
#68054=CARTESIAN_POINT('Ctrl Pts',(19.7707974823031,6.38078592094303,1.46973816728273));
#68055=CARTESIAN_POINT('Ctrl Pts',(19.8713673922609,4.90563999164961,4.33696202213174));
#68056=CARTESIAN_POINT('Ctrl Pts',(19.9719373022188,2.24088101182681,6.15247996515098));
#68057=CARTESIAN_POINT('Ctrl Pts',(20.0725072121765,-0.967289901259671,
6.47602495038849));
#68058=CARTESIAN_POINT('Ctrl Pts',(20.1730771221343,-3.94089373513293,5.22914041151611));
#68059=CARTESIAN_POINT('Ctrl Pts',(20.2736470320921,-5.95883428729783,2.71419333802675));
#68060=CARTESIAN_POINT('Ctrl Pts',(20.3742169420499,-6.53176262539532,-0.458943035049169));
#68061=CARTESIAN_POINT('Ctrl Pts',(20.4747868520077,-5.52074416434619,-3.52078624413008));
#68062=CARTESIAN_POINT('Ctrl Pts',(20.5753567619656,-3.17094998830467,-5.72884175494776));
#68063=CARTESIAN_POINT('Ctrl Pts',(20.6759266719233,-0.0522031736032762,
-6.54765810487926));
#68064=CARTESIAN_POINT('Ctrl Pts',(20.7764965818812,3.07920286773082,-5.77867298385814));
#68065=CARTESIAN_POINT('Ctrl Pts',(20.8770664918389,5.46390486329879,-3.60836464734974));
#68066=CARTESIAN_POINT('Ctrl Pts',(20.9776364017968,6.52361463351761,-0.563030985622693));
#68067=CARTESIAN_POINT('Ctrl Pts',(21.0782063117546,6.00135347055993,2.61883720318622));
#68068=CARTESIAN_POINT('Ctrl Pts',(21.1787762217123,4.02376925726304,5.16563962574656));
#68069=CARTESIAN_POINT('Ctrl Pts',(21.2793461316702,1.07042446278717,6.45977888520451));
#68070=CARTESIAN_POINT('Ctrl Pts',(21.3799160416279,-2.14249734242742,6.18742732606452));
#68071=CARTESIAN_POINT('Ctrl Pts',(21.4804859515858,-4.83586538644446,4.41462996651488));
#68072=CARTESIAN_POINT('Ctrl Pts',(21.5810558615435,-6.35654023709114,1.57128864040408));
#68073=CARTESIAN_POINT('Ctrl Pts',(21.6816257715014,-6.33575955214008,-1.65308882843456));
#68074=CARTESIAN_POINT('Ctrl Pts',(21.7821956814592,-4.77856262979613,-4.47659367938356));
#68075=CARTESIAN_POINT('Ctrl Pts',(21.882765591417,-2.06256838325162,-6.21452841667276));
#68076=CARTESIAN_POINT('Ctrl Pts',(21.9833355013748,1.15359692071403,-6.44544536255773));
#68077=CARTESIAN_POINT('Ctrl Pts',(22.0839054113326,4.0900159644555,-5.11334735644941));
#68078=CARTESIAN_POINT('Ctrl Pts',(22.1844753212904,6.03460965761974,-2.54126701811676));
#68079=CARTESIAN_POINT('Ctrl Pts',(22.2850452312482,6.51581570357615,0.647068384512964));
#68080=CARTESIAN_POINT('Ctrl Pts',(22.385615141206,5.41694205041641,3.67849026091368));
#68081=CARTESIAN_POINT('Ctrl Pts',(22.4861850511638,3.00446461308975,5.81788141559254));
#68082=CARTESIAN_POINT('Ctrl Pts',(22.5867549611216,-0.136592906581867,
6.5464413351895));
#68083=CARTESIAN_POINT('Ctrl Pts',(22.6873248710794,-3.24452676399049,5.68749486636738));
#68084=CARTESIAN_POINT('Ctrl Pts',(22.7878947810372,-5.5656656741131,3.44933578840989));
#68085=CARTESIAN_POINT('Ctrl Pts',(22.888464690995,-6.53713544934789,0.374715751050151));
#68086=CARTESIAN_POINT('Ctrl Pts',(22.9890346009528,-5.9233555054695,-2.79077253337317));
#68087=CARTESIAN_POINT('Ctrl Pts',(23.0896045109106,-3.87316695050906,-5.27950088083053));
#68088=CARTESIAN_POINT('Ctrl Pts',(23.1901744208684,-0.883738744183345,
-6.48795480943227));
#68089=CARTESIAN_POINT('Ctrl Pts',(23.2907443308262,2.31999534685918,-6.12308528176423));
#68090=CARTESIAN_POINT('Ctrl Pts',(23.391314240784,4.96113256340688,-4.27337284419578));
#68091=CARTESIAN_POINT('Ctrl Pts',(23.4918841507418,6.39919940401359,-1.38737117055174));
#68092=CARTESIAN_POINT('Ctrl Pts',(23.5924540606996,6.28546589776137,1.83506681766218));
#68093=CARTESIAN_POINT('Ctrl Pts',(23.6930239706574,4.64751232201134,4.61250268227118));
#68094=CARTESIAN_POINT('Ctrl Pts',(23.7935938806152,1.88254100888544,6.27141061700401));
#68095=CARTESIAN_POINT('Ctrl Pts',(23.894163790573,-1.33894487834989,6.40950687572348));
#68096=CARTESIAN_POINT('Ctrl Pts',(23.9947337005308,-4.23573778518752,4.99330323456734));
#68097=CARTESIAN_POINT('Ctrl Pts',(24.0953036104886,-6.10536792536175,2.36622785740725));
#68098=CARTESIAN_POINT('Ctrl Pts',(24.1958735204464,-6.49445159931153,-0.834655738257308));
#68099=CARTESIAN_POINT('Ctrl Pts',(24.2964434304042,-5.30863635103847,-3.83313603589005));
#68100=CARTESIAN_POINT('Ctrl Pts',(24.397013340362,-2.83548135746499,-5.90208414449291));
#68101=CARTESIAN_POINT('Ctrl Pts',(24.4975832503198,0.325275424430082,-6.53978192873951));
#68102=CARTESIAN_POINT('Ctrl Pts',(24.5981531602776,3.40715319590727,-5.59158822489862));
#68103=CARTESIAN_POINT('Ctrl Pts',(24.6987230702354,5.66279925035214,-3.28743918991932));
#68104=CARTESIAN_POINT('Ctrl Pts',(24.7992929801932,6.54522136128659,-0.186088981306509));
#68105=CARTESIAN_POINT('Ctrl Pts',(24.899862890151,5.84043292642331,2.96038764508239));
#68106=CARTESIAN_POINT('Ctrl Pts',(25.0004328001088,3.71934453451454,5.3889728159254));
#68107=CARTESIAN_POINT('Ctrl Pts',(25.1010027100666,0.696318294704414,6.51073671788884));
#68108=CARTESIAN_POINT('Ctrl Pts',(25.2015726200244,-2.49556453216075,6.05365257039312));
#68109=CARTESIAN_POINT('Ctrl Pts',(25.3021425299822,-5.08227510823047,4.12856288573482));
#68110=CARTESIAN_POINT('Ctrl Pts',(25.40271243994,-6.43653834552245,1.20230025527115));
#68111=CARTESIAN_POINT('Ctrl Pts',(25.5032823498979,-6.22994657478204,-2.01551915212123));
#68112=CARTESIAN_POINT('Ctrl Pts',(25.6038522598556,-4.51259812257367,-4.7445769001409));
#68113=CARTESIAN_POINT('Ctrl Pts',(25.7044221698134,-1.70094851021507,-6.32307883414425));
#68114=CARTESIAN_POINT('Ctrl Pts',(25.8049920797713,1.52317965164543,-6.36823959395525));
#68115=CARTESIAN_POINT('Ctrl Pts',(25.905561989729,4.37793805917866,-4.86910773419536));
#68116=CARTESIAN_POINT('Ctrl Pts',(26.0061318996868,6.17105025601567,-2.18922144036068));
#68117=CARTESIAN_POINT('Ctrl Pts',(26.1067018096447,6.46768807798595,1.02154916821688));
#68118=CARTESIAN_POINT('Ctrl Pts',(26.2072717196024,5.19591710861598,3.98459498288065));
#68119=CARTESIAN_POINT('Ctrl Pts',(26.3078416295603,2.66414071320113,5.98137994424951));
#68120=CARTESIAN_POINT('Ctrl Pts',(26.408411539518,-0.513687511796294,6.52768541808125));
#68121=CARTESIAN_POINT('Ctrl Pts',(26.5089814494759,-3.56694695738004,5.49103279724709));
#68122=CARTESIAN_POINT('Ctrl Pts',(26.6095513594336,-5.75522483632937,3.12280944991903));
#68123=CARTESIAN_POINT('Ctrl Pts',(26.7101212693915,-6.54786564673141,-0.00269250081047194));
#68124=CARTESIAN_POINT('Ctrl Pts',(26.8106911793493,-5.75265467439162,-3.12754152241121));
#68125=CARTESIAN_POINT('Ctrl Pts',(26.911261089307,-3.56242989556197,-5.49396441710467));
#68126=CARTESIAN_POINT('Ctrl Pts',(27.0118309992649,-0.508318933700379,
-6.52810567001237));
#68127=CARTESIAN_POINT('Ctrl Pts',(27.1124009092226,2.66905893200806,-5.97918691752266));
#68128=CARTESIAN_POINT('Ctrl Pts',(27.2129708191805,5.199192304307,-3.98032048458925));
#68129=CARTESIAN_POINT('Ctrl Pts',(27.3135407291383,6.46852601842535,-1.01622976051699));
#68130=CARTESIAN_POINT('Ctrl Pts',(27.414110639096,6.16924774136823,2.19429580568093));
#68131=CARTESIAN_POINT('Ctrl Pts',(27.5146805490539,4.37393219769472,4.87270652791397));
#68132=CARTESIAN_POINT('Ctrl Pts',(27.6152504590117,1.5179418612865,6.36949011169342));
#68133=CARTESIAN_POINT('Ctrl Pts',(27.7158203689695,-1.70614806979581,6.32167782642693));
#68134=CARTESIAN_POINT('Ctrl Pts',(27.8163902789273,-4.51649856265382,4.74086411013352));
#68135=CARTESIAN_POINT('Ctrl Pts',(27.9169601888851,-6.23160204199977,2.01039492820449));
#68136=CARTESIAN_POINT('Ctrl Pts',(28.0175300988428,-6.43554739050252,-1.20759329320851));
#68137=CARTESIAN_POINT('Ctrl Pts',(28.1181000088007,-5.07887803671217,-4.13274118054939));
#68138=CARTESIAN_POINT('Ctrl Pts',(28.2186699187585,-2.490585131063,-6.05570288918915));
#68139=CARTESIAN_POINT('Ctrl Pts',(28.3192398287163,0.701672524901834,-6.51016186012329));
#68140=CARTESIAN_POINT('Ctrl Pts',(28.4198097386741,3.72377519759783,-5.38591218411155));
#68141=CARTESIAN_POINT('Ctrl Pts',(28.5203796486319,5.84286559040883,-2.95558343980043));
#68142=CARTESIAN_POINT('Ctrl Pts',(28.6209495585897,6.54506610725194,0.191471744411332));
#68143=CARTESIAN_POINT('Ctrl Pts',(28.7215194685475,5.66009372726706,3.29209519542769));
#68144=CARTESIAN_POINT('Ctrl Pts',(28.8220893785053,3.40255349079092,5.59438839548278));
#68145=CARTESIAN_POINT('Ctrl Pts',(28.9226592884631,0.319896961813634,6.54004722544329));
#68146=CARTESIAN_POINT('Ctrl Pts',(29.0232291984209,-2.84033430502701,5.899750233094));
#68147=CARTESIAN_POINT('Ctrl Pts',(29.1237991083787,-5.31178694793982,3.82876888789362));
#68148=CARTESIAN_POINT('Ctrl Pts',(29.2243690183365,-6.49513582851576,0.829314383293102));
#68149=CARTESIAN_POINT('Ctrl Pts',(29.3249389282943,-6.10341986187583,-2.3712481453584));
#68150=CARTESIAN_POINT('Ctrl Pts',(29.4255088382521,-4.23162983272986,-4.99678503999889));
#68151=CARTESIAN_POINT('Ctrl Pts',(29.5260787482099,-1.33367321185521,-6.41060586381551));
#68152=CARTESIAN_POINT('Ctrl Pts',(29.6266486581677,1.88769801483017,-6.26986028409025));
#68153=CARTESIAN_POINT('Ctrl Pts',(29.7272185681255,4.65130409790384,-4.60867898274863));
#68154=CARTESIAN_POINT('Ctrl Pts',(29.8277884780834,6.28697294121176,-1.82989699537353));
#68155=CARTESIAN_POINT('Ctrl Pts',(29.9283583880411,6.39805625828247,1.39263343815186));
#68156=CARTESIAN_POINT('Ctrl Pts',(30.028928297999,4.95761644034995,4.27745146174423));
#68157=CARTESIAN_POINT('Ctrl Pts',(30.1294982079567,2.314958903291,6.1249911880165));
#68158=CARTESIAN_POINT('Ctrl Pts',(30.2300681179145,-0.88907417503301,6.48722582376283));
#68159=CARTESIAN_POINT('Ctrl Pts',(30.3306380278723,-3.87750753125207,5.27631378163672));
#68160=CARTESIAN_POINT('Ctrl Pts',(30.4312079378301,-5.92564864901217,2.78590018946591));
#68161=CARTESIAN_POINT('Ctrl Pts',(30.5317778477879,-6.53682507035513,-0.380091800467598));
#68162=CARTESIAN_POINT('Ctrl Pts',(30.6323477577457,-5.56282703922345,-3.45391185598164));
#68163=CARTESIAN_POINT('Ctrl Pts',(30.7329176677035,-3.23984823972113,-5.69016125964651));
#68164=CARTESIAN_POINT('Ctrl Pts',(30.8334875776613,-0.131209031040714,
-6.54655145610109));
#68165=CARTESIAN_POINT('Ctrl Pts',(30.9340574876191,3.00924825471858,-5.81540855991041));
#68166=CARTESIAN_POINT('Ctrl Pts',(31.034627397577,5.41996542915581,-3.67403409401191));
#68167=CARTESIAN_POINT('Ctrl Pts',(31.1351973075347,6.51634565268443,-0.641709523029432));
#68168=CARTESIAN_POINT('Ctrl Pts',(31.2357672174926,6.03251766489431,2.54622905488571));
#68169=CARTESIAN_POINT('Ctrl Pts',(31.3363371274503,4.0858093363315,5.11670927885807));
#68170=CARTESIAN_POINT('Ctrl Pts',(31.4369070374082,1.14829576089017,6.44639190731743));
#68171=CARTESIAN_POINT('Ctrl Pts',(31.5374769473659,-2.0676785480811,6.21283004749135));
#68172=CARTESIAN_POINT('Ctrl Pts',(31.6380468573237,-4.78224258905971,4.47266224933087));
#68173=CARTESIAN_POINT('Ctrl Pts',(31.7386167672815,-6.33711691888288,1.64787770590364));
#68174=CARTESIAN_POINT('Ctrl Pts',(31.8391866772393,-6.35524585104898,-1.57651576266484));
#68175=CARTESIAN_POINT('Ctrl Pts',(31.9397565871971,-4.83223313511359,-4.4186055158971));
#68176=CARTESIAN_POINT('Ctrl Pts',(32.040326497155,-2.13740804363799,-6.18918723518668));
#68177=CARTESIAN_POINT('Ctrl Pts',(32.1408964071127,1.07573665847769,-6.45889637777332));
#68178=CARTESIAN_POINT('Ctrl Pts',(32.2414663170705,4.02801614693748,-5.16232870875315));
#68179=CARTESIAN_POINT('Ctrl Pts',(32.3420362270284,6.0035051871967,-2.61390077174097));
#68180=CARTESIAN_POINT('Ctrl Pts',(32.4426061369861,6.52314938755023,0.568395852297626));
#68181=CARTESIAN_POINT('Ctrl Pts',(32.543176046944,5.46093547673687,3.61285697144554));
#68182=CARTESIAN_POINT('Ctrl Pts',(32.6437459569018,3.07444941374469,5.78120338506881));
#68183=CARTESIAN_POINT('Ctrl Pts',(32.7443158668595,-0.0575879855063994,
6.54761295443854));
#68184=CARTESIAN_POINT('Ctrl Pts',(32.8448857768174,-3.17566034784553,5.72623201872991));
#68185=CARTESIAN_POINT('Ctrl Pts',(32.9454556867752,-5.5236378095316,3.51624474778404));
#68186=CARTESIAN_POINT('Ctrl Pts',(33.0460255967329,-6.53213785731212,0.453571152384891));
#68187=CARTESIAN_POINT('Ctrl Pts',(33.1465955066908,-5.95660009774608,-2.71909305702058));
#68188=CARTESIAN_POINT('Ctrl Pts',(33.2471654166485,-3.93659194208878,-5.23237954077183));
#68189=CARTESIAN_POINT('Ctrl Pts',(33.3477353266064,-0.961963629206205,
-6.47681849006828));
#68190=CARTESIAN_POINT('Ctrl Pts',(33.4483052365642,2.245940035673,-6.15063453095429));
#68191=CARTESIAN_POINT('Ctrl Pts',(33.548875146522,4.90920517527109,-4.33292699272645));
#68192=CARTESIAN_POINT('Ctrl Pts',(33.6494450564797,6.38199228585055,-1.46448838867028));
#68193=CARTESIAN_POINT('Ctrl Pts',(33.7500149664376,6.30715176091324,1.75908738896483));
#68194=CARTESIAN_POINT('Ctrl Pts',(33.8505848763953,4.70283236333157,4.55608598904884));
#68195=CARTESIAN_POINT('Ctrl Pts',(33.9511547863532,1.95808016597497,6.24823765879799));
#68196=CARTESIAN_POINT('Ctrl Pts',(34.051724696311,-1.261504786059,6.42519707495081));
#68197=CARTESIAN_POINT('Ctrl Pts',(34.1522946062687,-4.17517591341315,5.04405173142193));
#68198=CARTESIAN_POINT('Ctrl Pts',(34.2528645162266,-6.07637047587579,2.43972818508764));
#68199=CARTESIAN_POINT('Ctrl Pts',(34.3534344261843,-6.50405042865251,-0.756227345942419));
#68200=CARTESIAN_POINT('Ctrl Pts',(34.4540043361422,-5.35450375135413,-3.76879839656363));
#68201=CARTESIAN_POINT('Ctrl Pts',(34.5545742461,-2.90649452366275,-5.8674390803079));
#68202=CARTESIAN_POINT('Ctrl Pts',(34.6551441560578,0.246337124022986,-6.54323083793734));
#68203=CARTESIAN_POINT('Ctrl Pts',(34.7557140660156,3.33943223118723,-5.63229474996771));
#68204=CARTESIAN_POINT('Ctrl Pts',(34.8562839759734,5.62271789696759,-3.35553203357178));
#68205=CARTESIAN_POINT('Ctrl Pts',(34.9568538859312,6.54249931293014,-0.265055687572883));
#68206=CARTESIAN_POINT('Ctrl Pts',(35.057423795889,5.87573027747814,2.88969643449489));
#68207=CARTESIAN_POINT('Ctrl Pts',(35.1579937058468,3.78410170773486,5.34369965873123));
#68208=CARTESIAN_POINT('Ctrl Pts',(35.2585636158046,0.774831731329118,6.50186031573515));
#68209=CARTESIAN_POINT('Ctrl Pts',(35.3591335257624,-2.42233427292655,6.08332544316112));
#68210=CARTESIAN_POINT('Ctrl Pts',(35.4597034357202,-5.03208630121234,4.18958938732152));
#68211=CARTESIAN_POINT('Ctrl Pts',(35.560273345678,-6.42156173321834,1.27988151157515));
#68212=CARTESIAN_POINT('Ctrl Pts',(35.6608432556358,-6.25381397278339,-1.94019652896949));
#68213=CARTESIAN_POINT('Ctrl Pts',(35.7614131655936,-4.56952170741089,-4.68977858141583));
#68214=CARTESIAN_POINT('Ctrl Pts',(35.8619830755514,-1.77712436156657,-6.30209336496475));
#68215=CARTESIAN_POINT('Ctrl Pts',(35.9625529855092,1.44622411215802,-6.38615593253239));
#68216=CARTESIAN_POINT('Ctrl Pts',(36.063122895467,4.31886448363548,-4.92158118384713));
#68217=CARTESIAN_POINT('Ctrl Pts',(36.1636928054248,6.14418393563375,-2.26352723471714));
#68218=CARTESIAN_POINT('Ctrl Pts',(36.2642627153826,6.47954407233056,0.943430120322585));
#68219=CARTESIAN_POINT('Ctrl Pts',(36.3648326253404,5.24362034926458,3.92160648331579));
#68220=CARTESIAN_POINT('Ctrl Pts',(36.4654025352982,2.73612320536071,5.94879664993625));
#68221=CARTESIAN_POINT('Ctrl Pts',(36.565972445256,-0.434881460509812,6.5334087498419));
#68222=CARTESIAN_POINT('Ctrl Pts',(36.6665423552139,-3.50042774656513,5.53367485205654));
#68223=CARTESIAN_POINT('Ctrl Pts',(36.7671122651716,-5.717123317347,3.19202956619347));
#68224=CARTESIAN_POINT('Ctrl Pts',(36.8676821751294,-6.54742140513593,0.0763198583190625));
#68225=CARTESIAN_POINT('Ctrl Pts',(36.9682520850872,-5.78997543838753,-3.05789734949935));
#68226=CARTESIAN_POINT('Ctrl Pts',(37.068821995045,-3.62846541200707,-5.45057708238993));
#68227=CARTESIAN_POINT('Ctrl Pts',(37.1693919050029,-0.587055646701985,
-6.52149656481404));
#68228=CARTESIAN_POINT('Ctrl Pts',(37.2699618149606,2.59671460757404,-6.010958744162));
#68229=CARTESIAN_POINT('Ctrl Pts',(37.3705317249185,5.15078380483974,-4.04276860245633));
#68230=CARTESIAN_POINT('Ctrl Pts',(37.4711016348762,6.45579236337419,-1.09421055478614));
#68231=CARTESIAN_POINT('Ctrl Pts',(37.5716715448341,6.19527683112161,2.1196926104918));
#68232=CARTESIAN_POINT('Ctrl Pts',(37.6722414547918,4.43241200039406,4.81957214241771));
#68233=CARTESIAN_POINT('Ctrl Pts',(37.7728113647496,1.59469107511828,6.35070957863325));
#68234=CARTESIAN_POINT('Ctrl Pts',(37.8733812747074,-1.6297410631179,6.34180540890317));
#68235=CARTESIAN_POINT('Ctrl Pts',(37.9739511846652,-4.45896239647582,4.79501888672199));
#68236=CARTESIAN_POINT('Ctrl Pts',(38.0745210946231,-6.20688918709104,2.08544441220052));
#68237=CARTESIAN_POINT('Ctrl Pts',(38.1750910045808,-6.44965069290488,-1.12984853706919));
#68238=CARTESIAN_POINT('Ctrl Pts',(38.2756609145387,-5.12837745773363,-4.07115418870565));
#68239=CARTESIAN_POINT('Ctrl Pts',(38.3762308244964,-2.56347710371634,-6.0252084541473));
#68240=CARTESIAN_POINT('Ctrl Pts',(38.4768007344543,0.623064241237588,-6.51815485613047));
#68241=CARTESIAN_POINT('Ctrl Pts',(38.577370644412,3.65851304404296,-5.43045431651657));
#68242=CARTESIAN_POINT('Ctrl Pts',(38.6779405543699,5.80677558302084,-3.02587327983824));
#68243=CARTESIAN_POINT('Ctrl Pts',(38.7785104643276,6.54690004175509,0.112479422442342));
#68244=CARTESIAN_POINT('Ctrl Pts',(38.8790803742854,5.69940687612311,3.22355596160616));
#68245=CARTESIAN_POINT('Ctrl Pts',(38.9796502842433,3.46981244924414,5.55292295500994));
#68246=CARTESIAN_POINT('Ctrl Pts',(39.080220194201,0.398791490337503,6.53571091193916));
#68247=CARTESIAN_POINT('Ctrl Pts',(39.1807901041589,-2.76893606168483,5.93359459885046));
#68248=CARTESIAN_POINT('Ctrl Pts',(39.2813600141166,-5.26519900232813,3.89258670334893));
#68249=CARTESIAN_POINT('Ctrl Pts',(39.3819299240745,-6.48465571734115,0.907629883135581));
#68250=CARTESIAN_POINT('Ctrl Pts',(39.4824998340322,-6.13158900307658,-2.29742640242431));
#68251=CARTESIAN_POINT('Ctrl Pts',(39.5830697439901,-4.29161723381362,-4.94535876308686));
#68252=CARTESIAN_POINT('Ctrl Pts',(39.6836396539478,-1.41093197969802,-6.39404588080751));
#68253=CARTESIAN_POINT('Ctrl Pts',(39.7842095639057,1.81190306492362,-6.29218237661038));
#68254=CARTESIAN_POINT('Ctrl Pts',(39.8847794738634,4.59535317603941,-4.66447006257631));
#68255=CARTESIAN_POINT('Ctrl Pts',(39.9853493838213,6.26443409777744,-1.90562777367704));
#68256=CARTESIAN_POINT('Ctrl Pts',(40.0859192937791,6.41439514340897,1.31532760991984));
#68257=CARTESIAN_POINT('Ctrl Pts',(40.1864892037369,5.00887088845912,4.21731718038291));
#68258=CARTESIAN_POINT('Ctrl Pts',(40.2870591136947,2.38869975483763,6.09661096499068));
#68259=CARTESIAN_POINT('Ctrl Pts',(40.3876290236525,-0.810729013070725,
6.49748183872578));
#68260=CARTESIAN_POINT('Ctrl Pts',(40.4881989336103,-3.81355669320821,5.32271895978858));
#68261=CARTESIAN_POINT('Ctrl Pts',(40.588768843568,-5.89160015806168,2.85720131505177));
#68262=CARTESIAN_POINT('Ctrl Pts',(40.6893387535259,-6.54093565624356,-0.301185189024252));
#68263=CARTESIAN_POINT('Ctrl Pts',(40.7899086634837,-5.60409988841139,-3.38653454403075));
#68264=CARTESIAN_POINT('Ctrl Pts',(40.8904785734415,-3.30827472180933,-5.65065218733584));
#68265=CARTESIAN_POINT('Ctrl Pts',(40.9910484833993,-0.210195783026292,
-6.54449153945545));
#68266=CARTESIAN_POINT('Ctrl Pts',(41.0916183933571,2.93885545219809,-5.85129732694312));
#68267=CARTESIAN_POINT('Ctrl Pts',(41.1921883033149,5.37523677011546,-3.73916854961161));
#68268=CARTESIAN_POINT('Ctrl Pts',(41.2927582132727,6.50812779843782,-0.720294617782823));
#68269=CARTESIAN_POINT('Ctrl Pts',(41.3933281232305,6.06280343802205,2.47325013880805));
#68270=CARTESIAN_POINT('Ctrl Pts',(41.4938980331883,4.147254462921,5.0670338657826));
#68271=CARTESIAN_POINT('Ctrl Pts',(41.5944679431461,1.22599985063719,6.43206624215296));
#68272=CARTESIAN_POINT('Ctrl Pts',(41.6950378531039,-1.99255867005031,6.23732809170829));
#68273=CARTESIAN_POINT('Ctrl Pts',(41.7956077630617,-4.72792342850226,4.53004324829526));
#68274=CARTESIAN_POINT('Ctrl Pts',(41.8961776730195,-6.31677082547448,1.72422681676178));
#68275=CARTESIAN_POINT('Ctrl Pts',(41.9967475829772,-6.37380673492663,-1.49971313357255));
#68276=CARTESIAN_POINT('Ctrl Pts',(42.0973174929351,-4.88519999791469,-4.3599739400116));
#68277=CARTESIAN_POINT('Ctrl Pts',(42.1978874028929,-2.2119364667287,-6.16294481918845));
#68278=CARTESIAN_POINT('Ctrl Pts',(42.2984573128507,0.99771975354065,-6.47140688495174));
#68279=CARTESIAN_POINT('Ctrl Pts',(42.3990272228085,3.96542979244218,-5.21055835188687));
#68280=CARTESIAN_POINT('Ctrl Pts',(42.4995971327663,5.97152652023215,-2.68615390388749));
#68281=CARTESIAN_POINT('Ctrl Pts',(42.6001670427241,6.52953320732713,0.489640553486283));
#68282=CARTESIAN_POINT('Ctrl Pts',(42.7007369526819,5.5041337124547,3.54669759813628));
#68283=CARTESIAN_POINT('Ctrl Pts',(42.8013068626397,3.14398653042817,5.74368352833721));
#68284=CARTESIAN_POINT('Ctrl Pts',(42.9018767725975,0.0214253212065685,
6.5478311472439));
#68285=CARTESIAN_POINT('Ctrl Pts',(43.0024466825553,-3.10633150996409,5.76413534950475));
#68286=CARTESIAN_POINT('Ctrl Pts',(43.1030165925131,-5.48080562398773,3.5826416914437));
#68287=CARTESIAN_POINT('Ctrl Pts',(43.2035865024709,-6.52618909222896,0.532360507248275));
#68288=CARTESIAN_POINT('Ctrl Pts',(43.3041564124287,-5.98897732353542,-2.64701764168366));
#68289=CARTESIAN_POINT('Ctrl Pts',(43.4047263223865,-3.99944370936796,-5.18449629113601));
#68290=CARTESIAN_POINT('Ctrl Pts',(43.5052962323443,-1.04004843851462,-6.46473905295097));
#68291=CARTESIAN_POINT('Ctrl Pts',(43.6058661423021,2.171557683375,-6.17728815945807));
#68292=CARTESIAN_POINT('Ctrl Pts',(43.7064360522599,4.85656293638531,-4.39185020488342));
#68293=CARTESIAN_POINT('Ctrl Pts',(43.8070059622177,6.36385585799084,-1.54139235625514));
#68294=CARTESIAN_POINT('Ctrl Pts',(43.9075758721756,6.3279192122232,1.68285181189028));
#68295=CARTESIAN_POINT('Ctrl Pts',(44.0081457821333,4.7574676047458,4.4990058642994));
#68296=CARTESIAN_POINT('Ctrl Pts',(44.1087156920912,2.03333419848207,6.22415486748919));
#68297=CARTESIAN_POINT('Ctrl Pts',(44.2092856020489,-1.18388100056117,6.43995167324384));
#68298=CARTESIAN_POINT('Ctrl Pts',(44.3098555120068,-4.11400607608704,5.09406574193198));
#68299=CARTESIAN_POINT('Ctrl Pts',(44.4104254219644,-6.04648821961621,2.51287325331947));
#68300=CARTESIAN_POINT('Ctrl Pts',(44.5109953319224,-6.51270217487891,-0.677688836069641));
#68301=CARTESIAN_POINT('Ctrl Pts',(44.6115652418801,-5.39959145905429,-3.70391196608585));
#68302=CARTESIAN_POINT('Ctrl Pts',(44.712135151838,-2.97708446253219,-5.83193963275989));
#68303=CARTESIAN_POINT('Ctrl Pts',(44.8127050617957,0.167362953394307,-6.54572695879052));
#68304=CARTESIAN_POINT('Ctrl Pts',(44.9132749717535,3.27122499719343,-5.67218113206398));
#68305=CARTESIAN_POINT('Ctrl Pts',(45.0138448817114,5.58181779513749,-3.42313626358817));
#68306=CARTESIAN_POINT('Ctrl Pts',(45.1144147916691,6.5388245827496,-0.343983797926061));
#68307=CARTESIAN_POINT('Ctrl Pts',(45.214984701627,5.91017203785263,2.81858444262207));
#68308=CARTESIAN_POINT('Ctrl Pts',(45.3155546115847,3.8483078614219,5.29764838215264));
#68309=CARTESIAN_POINT('Ctrl Pts',(45.4161245215426,0.853232341330176,6.49203714937878));
#68310=CARTESIAN_POINT('Ctrl Pts',(45.5166944315003,-2.34875128704718,6.11211249641235));
#68311=CARTESIAN_POINT('Ctrl Pts',(45.6172643414582,-4.98116475018809,4.25000582454772));
#68312=CARTESIAN_POINT('Ctrl Pts',(45.7178342514159,-6.40565004933793,1.35727639875713));
#68313=CARTESIAN_POINT('Ctrl Pts',(45.8184041613738,-6.27677072569056,-1.86459138534968));
#68314=CARTESIAN_POINT('Ctrl Pts',(45.9189740713315,-4.62577990428741,-4.63429736360291));
#68315=CARTESIAN_POINT('Ctrl Pts',(46.0195439812894,-1.85304143809858,-6.28019022051844));
#68316=CARTESIAN_POINT('Ctrl Pts',(46.1201138912471,1.36905798167786,-6.4031423551261));
#68317=CARTESIAN_POINT('Ctrl Pts',(46.220683801205,4.25916201942181,-4.97333798062435));
#68318=CARTESIAN_POINT('Ctrl Pts',(46.3212537111627,6.11642293386486,-2.33750342701311));
#68319=CARTESIAN_POINT('Ctrl Pts',(46.4218236211206,6.49045655203795,0.86517369545888));
#68320=CARTESIAN_POINT('Ctrl Pts',(46.5223935310784,5.29056004351288,3.85804694154842));
#68321=CARTESIAN_POINT('Ctrl Pts',(46.6229634410362,2.80770727870176,5.91534712542984));
#68322=CARTESIAN_POINT('Ctrl Pts',(46.723533350994,-0.356012084239504,6.53818072349498));
#68323=CARTESIAN_POINT('Ctrl Pts',(46.8241032609518,-3.43339882321811,5.57551112436612));
#68324=CARTESIAN_POINT('Ctrl Pts',(46.9246731709096,-5.67818930313457,3.26078487713835));
#68325=CARTESIAN_POINT('Ctrl Pts',(47.0252430808674,-6.5460237649891,0.155321104181599));
#68326=CARTESIAN_POINT('Ctrl Pts',(47.1258129908252,-5.82645309883866,-2.98780790283434));
#68327=CARTESIAN_POINT('Ctrl Pts',(47.226382900783,-3.69397257179779,-5.4063960654036));
#68328=CARTESIAN_POINT('Ctrl Pts',(47.3269528107408,-0.665706875973545,
-6.51393783609326));
#68329=CARTESIAN_POINT('Ctrl Pts',(47.4275227206986,2.5239921642147,-6.04185528891488));
#68330=CARTESIAN_POINT('Ctrl Pts',(47.5280926306564,5.1016252773058,-4.10462803517695));
#68331=CARTESIAN_POINT('Ctrl Pts',(47.6286625406142,6.44211865227558,-1.17203201629012));
#68332=CARTESIAN_POINT('Ctrl Pts',(47.729232450572,6.22040379962901,2.04478075762829));
#68333=CARTESIAN_POINT('Ctrl Pts',(47.8298023605298,4.4902463802744,4.76573595802775));
#68334=CARTESIAN_POINT('Ctrl Pts',(47.9303722704876,1.6712080790361,6.33100429108768));
#68335=CARTESIAN_POINT('Ctrl Pts',(48.0309421804453,-1.55309674274462,6.36100953346888));
#68336=CARTESIAN_POINT('Ctrl Pts',(48.1315120904032,-4.40077694135999,4.84847543972333));
#68337=CARTESIAN_POINT('Ctrl Pts',(48.232082000361,-6.18127252001054,2.16019022555157));
#68338=CARTESIAN_POINT('Ctrl Pts',(48.3326519103188,-6.4628148335752,-1.05193925876276));
#68339=CARTESIAN_POINT('Ctrl Pts',(48.4332218202766,-5.17713011337423,-4.00897437836659));
#68340=CARTESIAN_POINT('Ctrl Pts',(48.5337917302344,-2.63599579730208,-5.99383666225665));
#68341=CARTESIAN_POINT('Ctrl Pts',(48.6343616401922,0.544365230475053,-6.52519871521594));
#68342=CARTESIAN_POINT('Ctrl Pts',(48.7349315501501,3.59271815846718,-5.47420569681358));
#68343=CARTESIAN_POINT('Ctrl Pts',(48.8355014601077,5.76984002574585,-3.09572250928716));
#68344=CARTESIAN_POINT('Ctrl Pts',(48.9360713700657,6.5477806536249,0.0334707218546678));
#68345=CARTESIAN_POINT('Ctrl Pts',(49.0366412800234,5.73789010951729,3.1545473317593));
#68346=CARTESIAN_POINT('Ctrl Pts',(49.1372111899813,3.53656615319209,5.51064892923712));
#68347=CARTESIAN_POINT('Ctrl Pts',(49.237781099939,0.47762794909537,6.53042290509955));
#68348=CARTESIAN_POINT('Ctrl Pts',(49.3383510098969,-2.69713462150112,5.96657494805069));
#68349=CARTESIAN_POINT('Ctrl Pts',(49.4389209198545,-5.21784436815445,3.95583770229834));
#68350=CARTESIAN_POINT('Ctrl Pts',(49.5394908298125,-6.47323134720036,0.985813219037189));
#68351=CARTESIAN_POINT('Ctrl Pts',(49.6400607397701,-6.1588652968934,-2.22327012122418));
#68352=CARTESIAN_POINT('Ctrl Pts',(49.7406306497281,-4.35097971381765,-4.89321237094338));
#68353=CARTESIAN_POINT('Ctrl Pts',(49.8412005596858,-1.48798529558923,-6.37655483292632));
#68354=CARTESIAN_POINT('Ctrl Pts',(49.9417704696437,1.73584427591915,-6.31358823704594));
#68355=CARTESIAN_POINT('Ctrl Pts',(50.0423403796014,4.53873310478168,-4.7195819285997));
#68356=CARTESIAN_POINT('Ctrl Pts',(50.1429102895593,6.24098306280626,-1.98108106521952));
#68357=CARTESIAN_POINT('Ctrl Pts',(50.243480199517,6.42980000051754,1.237830251105));
#68358=CARTESIAN_POINT('Ctrl Pts',(50.3440501094749,5.05939597305955,4.15656879709634));
#68359=CARTESIAN_POINT('Ctrl Pts',(50.4446200194327,2.46209277740775,6.06734298788543));
#68360=CARTESIAN_POINT('Ctrl Pts',(50.5451899293904,-0.732265797325339,
6.50679172705517));
#68361=CARTESIAN_POINT('Ctrl Pts',(50.6457598393482,-3.74905054656244,5.36834907364693));
#68362=CARTESIAN_POINT('Ctrl Pts',(50.7463297493061,-5.85669376554837,2.92808639110816));
#68363=CARTESIAN_POINT('Ctrl Pts',(50.8468996592638,-6.54409378799878,-0.222234720693599));
#68364=CARTESIAN_POINT('Ctrl Pts',(50.9474695692217,-5.6445567002031,-3.31866410403319));
#68365=CARTESIAN_POINT('Ctrl Pts',(51.0480394791794,-3.37621947160443,-5.61032029894595));
#68366=CARTESIAN_POINT('Ctrl Pts',(51.1486093891373,-0.289151927488252,
-6.54147865088895));
#68367=CARTESIAN_POINT('Ctrl Pts',(51.249179299095,2.86803471013357,-5.88633406108379));
#68368=CARTESIAN_POINT('Ctrl Pts',(51.3497492090529,5.32972539943451,-3.80375852859097));
#68369=CARTESIAN_POINT('Ctrl Pts',(51.4503191190106,6.49896226735308,-0.798774827299281));
#68370=CARTESIAN_POINT('Ctrl Pts',(51.5508890289685,6.09220637993161,2.39991108200422));
#68371=CARTESIAN_POINT('Ctrl Pts',(51.6514589389262,4.20809568972269,5.01662061983395));
#68372=CARTESIAN_POINT('Ctrl Pts',(51.7520288488841,1.30352541720547,6.41680397580489));
#68373=CARTESIAN_POINT('Ctrl Pts',(51.8525987588419,-1.91714864687201,6.26091789141199));
#68374=CARTESIAN_POINT('Ctrl Pts',(51.9531686687997,-4.67291581441957,4.58676460792938));
#68375=CARTESIAN_POINT('Ctrl Pts',(52.0537385787574,-6.2955049195503,1.80032485544239));
#68376=CARTESIAN_POINT('Ctrl Pts',(52.1543084887153,-6.39143950104136,-1.42269212471807));
#68377=CARTESIAN_POINT('Ctrl Pts',(52.254878398673,-4.9374555054641,-4.30070748932868));
#68378=CARTESIAN_POINT('Ctrl Pts',(52.3554483086309,-2.28614280011545,-6.13580498994922));
#68379=CARTESIAN_POINT('Ctrl Pts',(52.4560182185886,0.919557566284525,-6.4829750623844));
#68380=CARTESIAN_POINT('Ctrl Pts',(52.5565881285465,3.90226601444088,-5.25802926292137));
#68381=CARTESIAN_POINT('Ctrl Pts',(52.6571580385042,5.93867831328004,-2.75801589346395));
#68382=CARTESIAN_POINT('Ctrl Pts',(52.7577279484621,6.53496623332907,0.410813955982539));
#68383=CARTESIAN_POINT('Ctrl Pts',(52.8582978584198,5.54653046729059,3.48002177473738));
#68384=CARTESIAN_POINT('Ctrl Pts',(52.9588677683777,3.21306583753008,5.70532730883329));
#68385=CARTESIAN_POINT('Ctrl Pts',(53.0594376783355,0.100435508100187,6.54709588182237));
#68386=CARTESIAN_POINT('Ctrl Pts',(53.1600075882933,-3.03655034564976,5.80119933944462));
#68387=CARTESIAN_POINT('Ctrl Pts',(53.260577498251,-5.43717535440492,3.6485169509979));
#68388=CARTESIAN_POINT('Ctrl Pts',(53.3611474082089,-6.51929002043674,0.611072342863134));
#68389=CARTESIAN_POINT('Ctrl Pts',(53.4617173181666,-6.02048246802809,-2.57455678274148));
#68390=CARTESIAN_POINT('Ctrl Pts',(53.5622872281245,-4.06171310065894,-5.13585810409048));
#68391=CARTESIAN_POINT('Ctrl Pts',(53.6628571380823,-1.11798180099441,-6.45171825764804));
#68392=CARTESIAN_POINT('Ctrl Pts',(53.7634270480401,2.09685911944926,-6.20304228489504));
#68393=CARTESIAN_POINT('Ctrl Pts',(53.8639969579979,4.80321351545239,-4.45013390300796));
#68394=CARTESIAN_POINT('Ctrl Pts',(53.9645668679557,6.34479275502275,-1.61807187027439));
#68395=CARTESIAN_POINT('Ctrl Pts',(54.0651367779135,6.34776524005276,1.60637117821377));
#68396=CARTESIAN_POINT('Ctrl Pts',(54.1657066878713,4.81141006630882,4.4412706377515));
#68397=CARTESIAN_POINT('Ctrl Pts',(54.266276597829,2.10829219583951,6.19916571456412));
#68398=CARTESIAN_POINT('Ctrl Pts',(54.3668465077869,-1.10608491795948,6.45376859123593));
#68399=CARTESIAN_POINT('Ctrl Pts',(54.4674164177447,-4.05223699846591,5.14333784807076));
#68400=CARTESIAN_POINT('Ctrl Pts',(54.5679863277025,-6.01572586397445,2.58565267587491));
#68401=CARTESIAN_POINT('Ctrl Pts',(54.6685562376603,-6.5204048812128,-0.599052163122007));
#68402=CARTESIAN_POINT('Ctrl Pts',(54.7691261476181,-5.44389427278895,-3.63848517874789));
#68403=CARTESIAN_POINT('Ctrl Pts',(54.8696960575759,-3.04723822545406,-5.79559295585254));
#68404=CARTESIAN_POINT('Ctrl Pts',(54.9702659675337,0.0883591872305582,
-6.54726604327576));
#68405=CARTESIAN_POINT('Ctrl Pts',(55.0708358774915,3.20255165237907,-5.71124916602977));
#68406=CARTESIAN_POINT('Ctrl Pts',(55.1714057874493,5.54008488415577,-3.4902271541179));
#68407=CARTESIAN_POINT('Ctrl Pts',(55.2719756974071,6.53423689591918,-0.422890962602382));
#68408=CARTESIAN_POINT('Ctrl Pts',(55.3725456073649,5.94367633180412,2.74711924961637));
#68409=CARTESIAN_POINT('Ctrl Pts',(55.4731155173227,3.91210579221266,5.2507116736487));
#68410=CARTESIAN_POINT('Ctrl Pts',(55.5736854272806,0.931192408451803,6.48151355909809));
#68411=CARTESIAN_POINT('Ctrl Pts',(55.6407320339191,-1.20560277749141,6.25335781087259));
#68412=CARTESIAN_POINT('Ctrl Pts',(55.6742553372383,-2.18270012582081,5.89135076165406));
#68413=CARTESIAN_POINT('Ctrl Pts',(54.6500381542954,-6.28284206479216,-0.000151303447314885));
#68414=CARTESIAN_POINT('Ctrl Pts',(54.6562108487504,-6.28303579177905,-0.191999457349239));
#68415=CARTESIAN_POINT('Ctrl Pts',(54.6623835432053,-6.2744219736263,-0.383830271012445));
#68416=CARTESIAN_POINT('Ctrl Pts',(54.6685562376603,-6.25687327693577,-0.574840192560178));
#68417=CARTESIAN_POINT('Ctrl Pts',(54.7020795409796,-6.16156801173819,-1.61219650166392));
#68418=CARTESIAN_POINT('Ctrl Pts',(54.7356028442988,-5.80273114226353,-2.62534084020598));
#68419=CARTESIAN_POINT('Ctrl Pts',(54.7691261476181,-5.22387003297044,-3.49143097232768));
#68420=CARTESIAN_POINT('Ctrl Pts',(54.8026494509374,-4.64500892367729,-4.35752110444949));
#68421=CARTESIAN_POINT('Ctrl Pts',(54.8361727542566,-3.84612357456576,-5.07655703015095));
#68422=CARTESIAN_POINT('Ctrl Pts',(54.8696960575759,-2.92408133122912,-5.56135384090563));
#68423=CARTESIAN_POINT('Ctrl Pts',(54.9032193608952,-2.00203908789258,-6.04615065166025));
#68424=CARTESIAN_POINT('Ctrl Pts',(54.9367426642144,-0.956839950330982,
-6.29670834746801));
#68425=CARTESIAN_POINT('Ctrl Pts',(54.9702659675337,0.0847916959744696,
-6.28265104916422));
#68426=CARTESIAN_POINT('Ctrl Pts',(55.003789270853,1.1264233422801,-6.26859375086043));
#68427=CARTESIAN_POINT('Ctrl Pts',(55.0373125741723,2.16448749732965,-5.98992145844508));
#68428=CARTESIAN_POINT('Ctrl Pts',(55.0708358774915,3.07310844681725,-5.48041497691869));
#68429=CARTESIAN_POINT('Ctrl Pts',(55.1043591808108,3.98172939630475,-4.97090849539237));
#68430=CARTESIAN_POINT('Ctrl Pts',(55.1378824841301,4.76090714023026,-4.23056782475512));
#68431=CARTESIAN_POINT('Ctrl Pts',(55.1714057874493,5.31618801415359,-3.34917479085056));
#68432=CARTESIAN_POINT('Ctrl Pts',(55.2033738582996,5.84570797673908,-2.50867185215095));
#68433=CARTESIAN_POINT('Ctrl Pts',(55.2353419291498,6.17162348859082,-1.53990053280162));
#68434=CARTESIAN_POINT('Ctrl Pts',(55.26731,6.25905495981401,-0.550339049542188));
#68435=CARTESIAN_POINT('',(18.8656682926829,-3.45323752142241,-4.38092825610446));
#68436=CARTESIAN_POINT('Ctrl Pts',(18.8656682926829,-3.45323752142232,-4.38092825610453));
#68437=CARTESIAN_POINT('Ctrl Pts',(18.8656682926829,-3.48865003681434,-4.35647151778965));
#68438=CARTESIAN_POINT('Ctrl Pts',(18.8656682926829,-3.5237620968794,-4.33160624123511));
#68439=CARTESIAN_POINT('Ctrl Pts',(18.8656682926829,-3.5585659267768,-4.30633657109999));
#68440=CARTESIAN_POINT('Ctrl Pts',(18.8656682926829,-3.68740336288153,-4.21279285705991));
#68441=CARTESIAN_POINT('Ctrl Pts',(18.8656682926829,-3.81201866337803,-4.11371135394565));
#68442=CARTESIAN_POINT('Ctrl Pts',(18.8656682926829,-3.93218904012421,-4.00949381605839));
#68443=CARTESIAN_POINT('Ctrl Pts',(18.8656682926829,-4.05370504575145,-3.90410928400258));
#68444=CARTESIAN_POINT('Ctrl Pts',(18.8656682926829,-4.17067657834504,-3.79347260745858));
#68445=CARTESIAN_POINT('Ctrl Pts',(18.8656682926829,-4.28284675048816,-3.67795294690854));
#68446=CARTESIAN_POINT('Ctrl Pts',(18.8656682926829,-4.3285937966682,-3.63083985842061));
#68447=CARTESIAN_POINT('Ctrl Pts',(18.8656682926829,-4.37354187975475,-3.58291408948346));
#68448=CARTESIAN_POINT('Ctrl Pts',(18.8656682926829,-4.41767199555344,-3.53419877631017));
#68449=CARTESIAN_POINT('Ctrl Pts',(18.8656682926829,-4.43553589143567,-3.51447878993244));
#68450=CARTESIAN_POINT('Ctrl Pts',(18.8656682926829,-4.45326188525846,-3.49463361845393));
#68451=CARTESIAN_POINT('Ctrl Pts',(18.8656682926829,-4.47084393932776,-3.47467064156079));
#68452=CARTESIAN_POINT('Ctrl Pts',(18.8656682926829,-4.57861483771785,-3.35230564678634));
#68453=CARTESIAN_POINT('Ctrl Pts',(18.8656682926829,-4.68103827851746,-3.22545389454906));
#68454=CARTESIAN_POINT('Ctrl Pts',(18.8656682926829,-4.77786631372815,-3.09451187441685));
#68455=CARTESIAN_POINT('Ctrl Pts',(18.8656682926829,-4.87490927228197,-2.96327921018901));
#68456=CARTESIAN_POINT('Ctrl Pts',(18.8656682926829,-4.96633249885538,-2.8279375517774));
#68457=CARTESIAN_POINT('Ctrl Pts',(18.8656682926829,-5.05185193133021,-2.68884672257815));
#68458=CARTESIAN_POINT('Ctrl Pts',(18.8656682926829,-5.08003907019056,-2.64300249275363));
#68459=CARTESIAN_POINT('Ctrl Pts',(18.8656682926829,-5.10758453375029,-2.59675068825047));
#68460=CARTESIAN_POINT('Ctrl Pts',(18.8656682926829,-5.1344771770417,-2.55010341702788));
#68461=CARTESIAN_POINT('Ctrl Pts',(18.8656682926829,-5.15017525977826,-2.52287393589613));
#68462=CARTESIAN_POINT('Ctrl Pts',(18.8656682926829,-5.16565088937481,-2.49550969580718));
#68463=CARTESIAN_POINT('Ctrl Pts',(18.8656682926829,-5.18090176556707,-2.46801305218364));
#68464=CARTESIAN_POINT('Ctrl Pts',(18.8656682926829,-5.19227387157726,-2.44750965668889));
#68465=CARTESIAN_POINT('Ctrl Pts',(18.8656682926829,-5.20351883698298,-2.42693647585482));
#68466=CARTESIAN_POINT('Ctrl Pts',(18.8656682926829,-5.21463146845408,-2.40630289334088));
#68467=CARTESIAN_POINT('Ctrl Pts',(18.8656682926829,-5.25995705387755,-2.32214378041977));
#68468=CARTESIAN_POINT('Ctrl Pts',(18.8656682926829,-5.30310402907468,-2.23693950757812));
#68469=CARTESIAN_POINT('Ctrl Pts',(18.8656682926829,-5.34402670803788,-2.15076859179026));
#68470=CARTESIAN_POINT('Ctrl Pts',(18.8656682926829,-5.41360113147134,-2.00426567618043));
#68471=CARTESIAN_POINT('Ctrl Pts',(18.8656682926829,-5.4767487513006,-1.85497050694108));
#68472=CARTESIAN_POINT('Ctrl Pts',(18.8656682926829,-5.53348127395234,-1.70334548898074));
#68473=CARTESIAN_POINT('Ctrl Pts',(18.8656682926829,-5.59097936210052,-1.54967439803224));
#68474=CARTESIAN_POINT('Ctrl Pts',(18.8656682926829,-5.64188832664486,-1.39360953369602));
#68475=CARTESIAN_POINT('Ctrl Pts',(18.8656682926829,-5.6861761332453,-1.23560191172807));
#68476=CARTESIAN_POINT('Ctrl Pts',(18.8656682926829,-5.72963766859383,-1.08054221528722));
#68477=CARTESIAN_POINT('Ctrl Pts',(18.8656682926829,-5.76672284284825,-0.923610856409404));
#68478=CARTESIAN_POINT('Ctrl Pts',(18.8656682926829,-5.79735709018424,-0.765215240674514));
#68479=CARTESIAN_POINT('Ctrl Pts',(18.8656682926829,-5.82033277568623,-0.646418528873346));
#68480=CARTESIAN_POINT('Ctrl Pts',(18.8656682926829,-5.83967893411615,-0.526797729632665));
#68481=CARTESIAN_POINT('Ctrl Pts',(18.8656682926829,-5.85534696996504,-0.406521158123589));
#68482=CARTESIAN_POINT('Ctrl Pts',(18.8656682926829,-5.8588777922724,-0.379416599145501));
#68483=CARTESIAN_POINT('Ctrl Pts',(18.8656682926829,-5.86222176578814,-0.352278731796697));
#68484=CARTESIAN_POINT('Ctrl Pts',(18.8656682926829,-5.86537822718048,-0.325109475094044));
#68485=CARTESIAN_POINT('Ctrl Pts',(18.8656682926829,-5.86791752154436,-0.303252486574072));
#68486=CARTESIAN_POINT('Ctrl Pts',(18.8656682926829,-5.87033448129072,-0.281383433945046));
#68487=CARTESIAN_POINT('Ctrl Pts',(18.8656682926829,-5.87262849180244,-0.259508980115285));
#68488=CARTESIAN_POINT('Ctrl Pts',(18.8656682926829,-5.89018289996684,-0.0921195593006232));
#68489=CARTESIAN_POINT('Ctrl Pts',(18.8656682926829,-5.9005537142749,0.0756879104303696));
#68490=CARTESIAN_POINT('Ctrl Pts',(18.8656682926829,-5.90373035404805,0.243439431795315));
#68491=CARTESIAN_POINT('Ctrl Pts',(18.8656682926829,-5.90649206425808,0.389279414414141));
#68492=CARTESIAN_POINT('Ctrl Pts',(18.8656682926829,-5.90381560822746,0.535077850343277));
#68493=CARTESIAN_POINT('Ctrl Pts',(18.8656682926829,-5.89566406821674,0.680534476662218));
#68494=CARTESIAN_POINT('Ctrl Pts',(18.8656682926829,-5.88633282846231,0.847041744278821));
#68495=CARTESIAN_POINT('Ctrl Pts',(18.8656682926829,-5.86982839107916,1.01310157460892));
#68496=CARTESIAN_POINT('Ctrl Pts',(18.8656682926829,-5.84633900059541,1.1783009017161));
#68497=CARTESIAN_POINT('Ctrl Pts',(18.8656682926829,-5.82271391797959,1.34445454259855));
#68498=CARTESIAN_POINT('Ctrl Pts',(18.8656682926829,-5.79202283543017,1.50973842898197));
#68499=CARTESIAN_POINT('Ctrl Pts',(18.8656682926829,-5.75440471333326,1.67372929806714));
#68500=CARTESIAN_POINT('Ctrl Pts',(18.8656682926829,-5.73578643671118,1.75489303495586));
#68501=CARTESIAN_POINT('Ctrl Pts',(18.8656682926829,-5.71547055624302,1.83573992830929));
#68502=CARTESIAN_POINT('Ctrl Pts',(18.8656682926829,-5.69346932747585,1.91621755238797));
#68503=CARTESIAN_POINT('Ctrl Pts',(18.8656682926829,-5.68781994444017,1.93688225839293));
#68504=CARTESIAN_POINT('Ctrl Pts',(18.8656682926829,-5.68205868413308,1.95752520127841));
#68505=CARTESIAN_POINT('Ctrl Pts',(18.8656682926829,-5.67618817005215,1.97813692025152));
#68506=CARTESIAN_POINT('Ctrl Pts',(18.8656682926829,-5.62959721149286,2.14172050616481));
#68507=CARTESIAN_POINT('Ctrl Pts',(18.8656682926829,-5.57621803009231,2.3030318060249));
#68508=CARTESIAN_POINT('Ctrl Pts',(18.8656682926829,-5.51628649487988,2.46165162563508));
#68509=CARTESIAN_POINT('Ctrl Pts',(18.8656682926829,-5.45587730439769,2.62153564767983));
#68510=CARTESIAN_POINT('Ctrl Pts',(18.8656682926829,-5.38881077087805,2.77868584241825));
#68511=CARTESIAN_POINT('Ctrl Pts',(18.8656682926829,-5.31527537851503,2.93267169117675));
#68512=CARTESIAN_POINT('Ctrl Pts',(18.8656682926829,-5.24179519018865,3.08654194062772));
#68513=CARTESIAN_POINT('Ctrl Pts',(18.8656682926829,-5.16185565593192,3.23725332913277));
#68514=CARTESIAN_POINT('Ctrl Pts',(18.8656682926829,-5.07559460954087,3.38436410593989));
#68515=CARTESIAN_POINT('Ctrl Pts',(18.8656682926829,-5.05043690689858,3.4272683985868));
#68516=CARTESIAN_POINT('Ctrl Pts',(18.8656682926829,-5.02474119684349,3.46986631351909));
#68517=CARTESIAN_POINT('Ctrl Pts',(18.8656682926829,-4.99851012946874,3.51214655673337));
#68518=CARTESIAN_POINT('Ctrl Pts',(18.8656682926829,-4.93079775741929,3.62128796215033));
#68519=CARTESIAN_POINT('Ctrl Pts',(18.8656682926829,-4.85951900835881,3.72831322166999));
#68520=CARTESIAN_POINT('Ctrl Pts',(18.8656682926829,-4.78481237253093,3.83309766072526));
#68521=CARTESIAN_POINT('Ctrl Pts',(18.8656682926829,-4.75212821935624,3.87894085281194));
#68522=CARTESIAN_POINT('Ctrl Pts',(18.8656682926829,-4.7187877661218,3.92435501713608));
#68523=CARTESIAN_POINT('Ctrl Pts',(18.8656682926829,-4.6848018029294,3.96932910582263));
#68524=CARTESIAN_POINT('Ctrl Pts',(18.8656682926829,-4.66369258750289,3.99726321854209));
#68525=CARTESIAN_POINT('Ctrl Pts',(18.8656682926829,-4.64233433481401,4.02502754913883));
#68526=CARTESIAN_POINT('Ctrl Pts',(18.8656682926829,-4.62072954176209,4.05261937053978));
#68527=CARTESIAN_POINT('Ctrl Pts',(18.8656682926829,-4.60757582916439,4.06941818401988));
#68528=CARTESIAN_POINT('Ctrl Pts',(18.8656682926829,-4.59433336696083,4.0861496280533));
#68529=CARTESIAN_POINT('Ctrl Pts',(18.8656682926829,-4.58100877205513,4.10280586710038));
#68530=CARTESIAN_POINT('Ctrl Pts',(18.8656682926829,-4.47422348374094,4.23629144782243));
#68531=CARTESIAN_POINT('Ctrl Pts',(18.8656682926829,-4.36205657963184,4.36508990258962));
#68532=CARTESIAN_POINT('Ctrl Pts',(18.8656682926829,-4.24491373451659,4.48896255029951));
#68533=CARTESIAN_POINT('Ctrl Pts',(18.8656682926829,-4.12562038138394,4.6151092517237));
#68534=CARTESIAN_POINT('Ctrl Pts',(18.8656682926829,-4.0011663610317,4.73614821512326));
#68535=CARTESIAN_POINT('Ctrl Pts',(18.8656682926829,-3.87193135828886,4.85180438829313));
#68536=CARTESIAN_POINT('Ctrl Pts',(18.8656682926829,-3.74243680935971,4.96769283691494));
#68537=CARTESIAN_POINT('Ctrl Pts',(18.8656682926829,-3.60814155977152,5.078177406693));
#68538=CARTESIAN_POINT('Ctrl Pts',(18.8656682926829,-3.46938570366927,5.18294999428408));
#68539=CARTESIAN_POINT('Ctrl Pts',(18.8656682926829,-3.33204959495397,5.28665055067132));
#68540=CARTESIAN_POINT('Ctrl Pts',(18.8656682926829,-3.19034314609964,5.3847558922719));
#68541=CARTESIAN_POINT('Ctrl Pts',(18.8656682926829,-3.04456302413475,5.4769289961042));
#68542=CARTESIAN_POINT('Ctrl Pts',(18.8656682926829,-2.96213372136761,5.52904697062894));
#68543=CARTESIAN_POINT('Ctrl Pts',(18.8656682926829,-2.87840143703307,5.57926756973073));
#68544=CARTESIAN_POINT('Ctrl Pts',(18.8656682926829,-2.79341604200811,5.62752347417154));
#68545=CARTESIAN_POINT('Ctrl Pts',(18.8656682926829,-3.45323752142241,-4.38092825610446));
#68546=CARTESIAN_POINT('Ctrl Pts',(18.8976363635332,-2.76035226152897,-4.92661473406192));
#68547=CARTESIAN_POINT('Ctrl Pts',(18.9631277377027,-1.07108282839872,-5.70279110802667));
#68548=CARTESIAN_POINT('Ctrl Pts',(19.0621424151914,1.74296490233074,-5.54583252750879));
#68549=CARTESIAN_POINT('Ctrl Pts',(19.1627123251492,4.17855117605108,-4.04150148361096));
#68550=CARTESIAN_POINT('Ctrl Pts',(19.263282235107,5.60083956100377,-1.55713407092352));
#68551=CARTESIAN_POINT('Ctrl Pts',(19.3638521450648,5.66493061750189,1.30484940988588));
#68552=CARTESIAN_POINT('Ctrl Pts',(19.4644220550226,4.35528013812923,3.85040169824184));
#68553=CARTESIAN_POINT('Ctrl Pts',(19.5649919649805,1.98947835131264,5.4622381255191));
#68554=CARTESIAN_POINT('Ctrl Pts',(19.6655618749382,-0.858770415672562,
5.74948485589373));
#68555=CARTESIAN_POINT('Ctrl Pts',(19.766131784896,-3.49876799771652,4.64248730288639));
#68556=CARTESIAN_POINT('Ctrl Pts',(19.861975432269,-5.20612390037616,2.51461999470827));
#68557=CARTESIAN_POINT('Ctrl Pts',(19.9242957763227,-5.57736077906089,0.794440147261595));
#68558=CARTESIAN_POINT('Ctrl Pts',(19.9530928170571,-5.57809442763664,-0.000115493386879852));
#68559=CARTESIAN_POINT('Origin',(18.8656682926829,-1.21203632162606E-15,
2.67744564496562E-16));
#68560=CARTESIAN_POINT('',(18.8656682926829,-6.28269,-7.69407619853508E-16));
#68561=CARTESIAN_POINT('Origin',(18.8656682926829,0.,0.));
#68562=CARTESIAN_POINT('Origin',(18.8656682926829,0.,0.));
#68563=CARTESIAN_POINT('',(18.8656682926829,3.45292578700092,-4.38059386100379));
#68564=CARTESIAN_POINT('Ctrl Pts',(18.8656682926829,2.79368235183429,5.62796419942309));
#68565=CARTESIAN_POINT('Ctrl Pts',(18.8656682926829,2.83576950574192,5.60408862809779));
#68566=CARTESIAN_POINT('Ctrl Pts',(18.8656682926829,2.87756131190663,5.57972664274282));
#68567=CARTESIAN_POINT('Ctrl Pts',(18.8656682926829,2.91904845943543,5.55488054600549));
#68568=CARTESIAN_POINT('Ctrl Pts',(18.8656682926829,3.06884955249153,5.46516667867235));
#68569=CARTESIAN_POINT('Ctrl Pts',(18.8656682926829,3.21468106272101,5.36914430082019));
#68570=CARTESIAN_POINT('Ctrl Pts',(18.8656682926829,3.35622549203696,5.26716183191894));
#68571=CARTESIAN_POINT('Ctrl Pts',(18.8656682926829,3.49796073607223,5.16504188140662));
#68572=CARTESIAN_POINT('Ctrl Pts',(18.8656682926829,3.6353978454227,5.05694519678979));
#68573=CARTESIAN_POINT('Ctrl Pts',(18.8656682926829,3.76818146341041,4.94318453571594));
#68574=CARTESIAN_POINT('Ctrl Pts',(18.8656682926829,3.80445178328906,4.91211040451447));
#68575=CARTESIAN_POINT('Ctrl Pts',(18.8656682926829,3.84037465782938,4.8806134817403));
#68576=CARTESIAN_POINT('Ctrl Pts',(18.8656682926829,3.87594229270048,4.84869974661354));
#68577=CARTESIAN_POINT('Ctrl Pts',(18.8656682926829,3.90190760479151,4.82540187776282));
#68578=CARTESIAN_POINT('Ctrl Pts',(18.8656682926829,3.92768359091741,4.80188187019607));
#68579=CARTESIAN_POINT('Ctrl Pts',(18.8656682926829,3.9532671322017,4.77814200052023));
#68580=CARTESIAN_POINT('Ctrl Pts',(18.8656682926829,3.97302840818941,4.7598048160248));
#68581=CARTESIAN_POINT('Ctrl Pts',(18.8656682926829,3.99266782739885,4.74134297711141));
#68582=CARTESIAN_POINT('Ctrl Pts',(18.8656682926829,4.01218355661887,4.72275839410534));
#68583=CARTESIAN_POINT('Ctrl Pts',(18.8656682926829,4.13756687421348,4.60335744079516));
#68584=CARTESIAN_POINT('Ctrl Pts',(18.8656682926829,4.25785698662503,4.47888420345246));
#68585=CARTESIAN_POINT('Ctrl Pts',(18.8656682926829,4.37272354223849,4.34965993119528));
#68586=CARTESIAN_POINT('Ctrl Pts',(18.8656682926829,4.48679275701944,4.2213326631903));
#68587=CARTESIAN_POINT('Ctrl Pts',(18.8656682926829,4.59551387493921,4.08831950882343));
#68588=CARTESIAN_POINT('Ctrl Pts',(18.8656682926829,4.69852069627652,3.95090699223527));
#68589=CARTESIAN_POINT('Ctrl Pts',(18.8656682926829,4.73486744777379,3.90241992576527));
#68590=CARTESIAN_POINT('Ctrl Pts',(18.8656682926829,4.77050230029976,3.85338488547739));
#68591=CARTESIAN_POINT('Ctrl Pts',(18.8656682926829,4.80540773103432,3.80381382155591));
#68592=CARTESIAN_POINT('Ctrl Pts',(18.8656682926829,4.82578390156854,3.7748765349856));
#68593=CARTESIAN_POINT('Ctrl Pts',(18.8656682926829,4.84591149370507,3.74575658302111));
#68594=CARTESIAN_POINT('Ctrl Pts',(18.8656682926829,4.86578689507932,3.71645630022115));
#68595=CARTESIAN_POINT('Ctrl Pts',(18.8656682926829,4.87882532276676,3.69723507236691));
#68596=CARTESIAN_POINT('Ctrl Pts',(18.8656682926829,4.8917549419235,3.67793655455239));
#68597=CARTESIAN_POINT('Ctrl Pts',(18.8656682926829,4.90456734688091,3.65857283768931));
#68598=CARTESIAN_POINT('Ctrl Pts',(18.8656682926829,4.96261329803569,3.57084650005438));
#68599=CARTESIAN_POINT('Ctrl Pts',(18.8656682926829,5.01829450643616,3.48172290231582));
#68600=CARTESIAN_POINT('Ctrl Pts',(18.8656682926829,5.07154077855382,3.3912753413832));
#68601=CARTESIAN_POINT('Ctrl Pts',(18.8656682926829,5.15772293769219,3.24488075299308));
#68602=CARTESIAN_POINT('Ctrl Pts',(18.8656682926829,5.23752878987822,3.09501884953656));
#68603=CARTESIAN_POINT('Ctrl Pts',(18.8656682926829,5.31086851293914,2.94214018851873));
#68604=CARTESIAN_POINT('Ctrl Pts',(18.8656682926829,5.38457302915425,2.78850110618168));
#68605=CARTESIAN_POINT('Ctrl Pts',(18.8656682926829,5.45174713407391,2.63181444742355));
#68606=CARTESIAN_POINT('Ctrl Pts',(18.8656682926829,5.51225047381773,2.47251913208819));
#68607=CARTESIAN_POINT('Ctrl Pts',(18.8656682926829,5.57066005449078,2.31873633908343));
#68608=CARTESIAN_POINT('Ctrl Pts',(18.8656682926829,5.62285245369036,2.1625216197253));
#68609=CARTESIAN_POINT('Ctrl Pts',(18.8656682926829,5.66865558800209,2.00426337214573));
#68610=CARTESIAN_POINT('Ctrl Pts',(18.8656682926829,5.70300793873588,1.88556968646105));
#68611=CARTESIAN_POINT('Ctrl Pts',(18.8656682926829,5.73376542007911,1.76572633040402));
#68612=CARTESIAN_POINT('Ctrl Pts',(18.8656682926829,5.76083805161128,1.6448980065652));
#68613=CARTESIAN_POINT('Ctrl Pts',(18.8656682926829,5.76715184157729,1.61671882281072));
#68614=CARTESIAN_POINT('Ctrl Pts',(18.8656682926829,5.77326514699577,1.58848607606894));
#68615=CARTESIAN_POINT('Ctrl Pts',(18.8656682926829,5.77917670617993,1.5602018761831));
#68616=CARTESIAN_POINT('Ctrl Pts',(18.8656682926829,5.78340953605446,1.53994965464149));
#68617=CARTESIAN_POINT('Ctrl Pts',(18.8656682926829,5.78753871869447,1.51967184833655));
#68618=CARTESIAN_POINT('Ctrl Pts',(18.8656682926829,5.79156137635828,1.49938216970943));
#68619=CARTESIAN_POINT('Ctrl Pts',(18.8656682926829,5.82418927474855,1.3348119706163));
#68620=CARTESIAN_POINT('Ctrl Pts',(18.8656682926829,5.84986051383317,1.16923824915711));
#68621=CARTESIAN_POINT('Ctrl Pts',(18.8656682926829,5.86846654733547,1.00308241347301));
#68622=CARTESIAN_POINT('Ctrl Pts',(18.8656682926829,5.88557367486975,0.850312126820536));
#68623=CARTESIAN_POINT('Ctrl Pts',(18.8656682926829,5.89670763199262,0.697049144108283));
#68624=CARTESIAN_POINT('Ctrl Pts',(18.8656682926829,5.90174533861939,0.543617239147347));
#68625=CARTESIAN_POINT('Ctrl Pts',(18.8656682926829,5.90723869521276,0.376307741156566));
#68626=CARTESIAN_POINT('Ctrl Pts',(18.8656682926829,5.90548366105168,0.208796643477492));
#68627=CARTESIAN_POINT('Ctrl Pts',(18.8656682926829,5.89656614992036,0.041539681498394));
#68628=CARTESIAN_POINT('Ctrl Pts',(18.8656682926829,5.88769080065284,-0.124926491980615));
#68629=CARTESIAN_POINT('Ctrl Pts',(18.8656682926829,5.87172030576114,-0.291141651826502));
#68630=CARTESIAN_POINT('Ctrl Pts',(18.8656682926829,5.84869066007965,-0.4566401983567));
#68631=CARTESIAN_POINT('Ctrl Pts',(18.8656682926829,5.83770118329379,-0.535614163494544));
#68632=CARTESIAN_POINT('Ctrl Pts',(18.8656682926829,5.82510358325441,-0.614424642607473));
#68633=CARTESIAN_POINT('Ctrl Pts',(18.8656682926829,5.81089806702808,-0.693018993923835));
#68634=CARTESIAN_POINT('Ctrl Pts',(18.8656682926829,5.80729284562518,-0.712965473375758));
#68635=CARTESIAN_POINT('Ctrl Pts',(18.8656682926829,5.80358357016803,-0.732900503194119));
#68636=CARTESIAN_POINT('Ctrl Pts',(18.8656682926829,5.79977180301852,-0.75281498132816));
#68637=CARTESIAN_POINT('Ctrl Pts',(18.8656682926829,5.7687219432075,-0.915034164719276));
#68638=CARTESIAN_POINT('Ctrl Pts',(18.8656682926829,5.73093354192466,-1.07559795340867));
#68639=CARTESIAN_POINT('Ctrl Pts',(18.8656682926829,5.68653260689291,-1.23408041710266));
#68640=CARTESIAN_POINT('Ctrl Pts',(18.8656682926829,5.64217918661081,-1.39239328403969));
#68641=CARTESIAN_POINT('Ctrl Pts',(18.8656682926829,5.59122714042856,-1.54862999865536));
#68642=CARTESIAN_POINT('Ctrl Pts',(18.8656682926829,5.53375236356643,-1.70235124610643));
#68643=CARTESIAN_POINT('Ctrl Pts',(18.8656682926829,5.4770089713036,-1.85411634237068));
#68644=CARTESIAN_POINT('Ctrl Pts',(18.8656682926829,5.41390750143894,-2.00343021336511));
#68645=CARTESIAN_POINT('Ctrl Pts',(18.8656682926829,5.34447662605786,-2.14984576322425));
#68646=CARTESIAN_POINT('Ctrl Pts',(18.8656682926829,5.32531108420779,-2.19026198054724));
#68647=CARTESIAN_POINT('Ctrl Pts',(18.8656682926829,5.30566301286859,-2.2304571801222));
#68648=CARTESIAN_POINT('Ctrl Pts',(18.8656682926829,5.28553245444563,-2.27042152789026));
#68649=CARTESIAN_POINT('Ctrl Pts',(18.8656682926829,5.232647265755,-2.37541226029837));
#68650=CARTESIAN_POINT('Ctrl Pts',(18.8656682926829,5.17643271285519,-2.4788104498093));
#68651=CARTESIAN_POINT('Ctrl Pts',(18.8656682926829,5.11698334956708,-2.58047663726544));
#68652=CARTESIAN_POINT('Ctrl Pts',(18.8656682926829,5.09097425312854,-2.6249555942775));
#68653=CARTESIAN_POINT('Ctrl Pts',(18.8656682926829,5.06434587802933,-2.66910290268612));
#68654=CARTESIAN_POINT('Ctrl Pts',(18.8656682926829,5.03710563512655,-2.71290623030739));
#68655=CARTESIAN_POINT('Ctrl Pts',(18.8656682926829,5.01908597407371,-2.74188251805709));
#68656=CARTESIAN_POINT('Ctrl Pts',(18.8656682926829,5.00079855728729,-2.7707082734982));
#68657=CARTESIAN_POINT('Ctrl Pts',(18.8656682926829,4.98224546314655,-2.79937982321383));
#68658=CARTESIAN_POINT('Ctrl Pts',(18.8656682926829,4.97113612836914,-2.81654794848511));
#68659=CARTESIAN_POINT('Ctrl Pts',(18.8656682926829,4.9599316556517,-2.8336605039157));
#68660=CARTESIAN_POINT('Ctrl Pts',(18.8656682926829,4.94864037660227,-2.8507050608972));
#68661=CARTESIAN_POINT('Ctrl Pts',(18.8656682926829,4.85950934438235,-2.98525128465474));
#68662=CARTESIAN_POINT('Ctrl Pts',(18.8656682926829,4.76485187654229,-3.11575104860376));
#68663=CARTESIAN_POINT('Ctrl Pts',(18.8656682926829,4.66498905339689,-3.24190539502472));
#68664=CARTESIAN_POINT('Ctrl Pts',(18.8656682926829,4.56466269505643,-3.36864531451214));
#68665=CARTESIAN_POINT('Ctrl Pts',(18.8656682926829,4.45908202239174,-3.49099993670225));
#68666=CARTESIAN_POINT('Ctrl Pts',(18.8656682926829,4.34853253898482,-3.60863276114994));
#68667=CARTESIAN_POINT('Ctrl Pts',(18.8656682926829,4.23874440681553,-3.72545545158598));
#68668=CARTESIAN_POINT('Ctrl Pts',(18.8656682926829,4.12405510639962,-3.83762162938683));
#68669=CARTESIAN_POINT('Ctrl Pts',(18.8656682926829,4.00471307570633,-3.94476131146243));
#68670=CARTESIAN_POINT('Ctrl Pts',(18.8656682926829,3.88777618067956,-4.04974177545567));
#68671=CARTESIAN_POINT('Ctrl Pts',(18.8656682926829,3.76637165277503,-4.14989663134919));
#68672=CARTESIAN_POINT('Ctrl Pts',(18.8656682926829,3.64071140247854,-4.24483318001998));
#68673=CARTESIAN_POINT('Ctrl Pts',(18.8656682926829,3.57913066675992,-4.29135753835876));
#68674=CARTESIAN_POINT('Ctrl Pts',(18.8656682926829,3.51652760821553,-4.33662797130161));
#68675=CARTESIAN_POINT('Ctrl Pts',(18.8656682926829,3.45292578700089,-4.38059386100381));
#68676=CARTESIAN_POINT('Origin',(18.8656682926829,0.,0.));
#68677=CARTESIAN_POINT('Origin',(16.5082437683087,0.,0.));
#68678=CARTESIAN_POINT('Ctrl Pts',(18.8656682926829,3.45292578700087,-4.38059386100382));
#68679=CARTESIAN_POINT('Ctrl Pts',(18.8991915960022,4.17945978894053,-3.8079162583704));
#68680=CARTESIAN_POINT('Ctrl Pts',(18.9662382026407,5.34139059168272,-2.29470092783305));
#68681=CARTESIAN_POINT('Ctrl Pts',(19.0668081125985,5.78874853530519,0.533337577335307));
#68682=CARTESIAN_POINT('Ctrl Pts',(19.1673780225563,4.83241525876795,3.23130860481921));
#68683=CARTESIAN_POINT('Ctrl Pts',(19.2679479325141,2.70419169563657,5.14605048923388));
#68684=CARTESIAN_POINT('Ctrl Pts',(19.3685178424719,-0.0797792217301073,
5.81269672472357));
#68685=CARTESIAN_POINT('Ctrl Pts',(19.4690877524298,-2.84441229285594,5.06986231595082));
#68686=CARTESIAN_POINT('Ctrl Pts',(19.5696576623875,-4.91927346795933,3.09754298939177));
#68687=CARTESIAN_POINT('Ctrl Pts',(19.6410430010139,-5.54528435432487,1.16441856903096));
#68688=CARTESIAN_POINT('Ctrl Pts',(19.678905036321,-5.57823027330273,0.119820339136794));
#68689=CARTESIAN_POINT('Ctrl Pts',(19.6832437683088,-5.57812419168581,0.000109767319341463));
#68690=CARTESIAN_POINT('Ctrl Pts',(18.4587229554446,3.88925862210691,-4.93415251147216));
#68691=CARTESIAN_POINT('Ctrl Pts',(18.4922462587639,4.70760190707855,-4.28910786205787));
#68692=CARTESIAN_POINT('Ctrl Pts',(18.5592928654024,6.01636139732571,-2.58467338114522));
#68693=CARTESIAN_POINT('Ctrl Pts',(18.6598627753602,6.52025022863267,0.600733377750014));
#68694=CARTESIAN_POINT('Ctrl Pts',(18.760432685318,5.44306882630348,3.63963653643918));
#68695=CARTESIAN_POINT('Ctrl Pts',(18.8610025952758,3.0459099085414,5.79633692400731));
#68696=CARTESIAN_POINT('Ctrl Pts',(18.9615725052336,-0.0898606124542653,
6.54722465783414));
#68697=CARTESIAN_POINT('Ctrl Pts',(19.0621424151914,-3.20384963860623,5.71052114685986));
#68698=CARTESIAN_POINT('Ctrl Pts',(19.1627123251492,-5.54090297039958,3.48896747917141));
#68699=CARTESIAN_POINT('Ctrl Pts',(19.263282235107,-6.53429461288024,0.421369638803437));
#68700=CARTESIAN_POINT('Ctrl Pts',(19.3638521450648,-5.94312415339177,-2.74842399726426));
#68701=CARTESIAN_POINT('Ctrl Pts',(19.4644220550226,-3.91075185848052,-5.25172001492936));
#68702=CARTESIAN_POINT('Ctrl Pts',(19.5649919649804,-0.930025269268408,
-6.48148211124559));
#68703=CARTESIAN_POINT('Ctrl Pts',(19.6655618749382,2.27623147590318,-6.13948850396696));
#68704=CARTESIAN_POINT('Ctrl Pts',(19.7661317848961,4.9305041351233,-4.30867517567208));
#68705=CARTESIAN_POINT('Ctrl Pts',(19.8667016948538,6.38913374117629,-1.43301133769862));
#68706=CARTESIAN_POINT('Ctrl Pts',(19.9672716048117,6.29840393779587,1.79015626640114));
#68707=CARTESIAN_POINT('Ctrl Pts',(20.0678415147694,4.68031658966875,4.57921264451185));
#68708=CARTESIAN_POINT('Ctrl Pts',(20.1684114247272,1.92725650346534,6.2578138330424));
#68709=CARTESIAN_POINT('Ctrl Pts',(20.2689813346851,-1.29316162884032,6.41890058728604));
#68710=CARTESIAN_POINT('Ctrl Pts',(20.3695512446428,-4.19998917778443,5.02340945765924));
#68711=CARTESIAN_POINT('Ctrl Pts',(20.4701211546007,-6.08832296738331,2.40974586754627));
#68712=CARTESIAN_POINT('Ctrl Pts',(20.5706910645584,-6.5002436779878,-0.788279025514826));
#68713=CARTESIAN_POINT('Ctrl Pts',(20.6712609745163,-5.33586089248439,-3.79514693118953));
#68714=CARTESIAN_POINT('Ctrl Pts',(20.771830884474,-2.87753643370932,-5.88169497418324));
#68715=CARTESIAN_POINT('Ctrl Pts',(20.8724007944319,0.278588133120066,-6.54193704847586));
#68716=CARTESIAN_POINT('Ctrl Pts',(20.9729707043896,3.36715531751224,-5.61576502030334));
#68717=CARTESIAN_POINT('Ctrl Pts',(21.0735406143475,5.63919023593738,-3.32777480876387));
#68718=CARTESIAN_POINT('Ctrl Pts',(21.1741105243053,6.54372637653163,-0.232802070822349));
#68719=CARTESIAN_POINT('Ctrl Pts',(21.2746804342631,5.86141450384058,2.91862496893136));
#68720=CARTESIAN_POINT('Ctrl Pts',(21.3752503442209,3.75771465964378,5.36228796613461));
#68721=CARTESIAN_POINT('Ctrl Pts',(21.4758202541787,0.74277224523095,6.50560074757205));
#68722=CARTESIAN_POINT('Ctrl Pts',(21.5763901641365,-2.45229179925024,6.07131094792556));
#68723=CARTESIAN_POINT('Ctrl Pts',(21.6769600740943,-5.05267719341661,4.16473346976847));
#68724=CARTESIAN_POINT('Ctrl Pts',(21.7775299840521,-6.42779271766877,1.24821171031312));
#68725=CARTESIAN_POINT('Ctrl Pts',(21.8780998940099,-6.24417404111461,-1.97100031439601));
#68726=CARTESIAN_POINT('Ctrl Pts',(21.9786698039676,-4.54634853475423,-4.71224645955806));
#68727=CARTESIAN_POINT('Ctrl Pts',(22.0792397139255,-1.74603742234317,-6.31077689471399));
#68728=CARTESIAN_POINT('Ctrl Pts',(22.1798096238833,1.47768626194704,-6.37894936539961));
#68729=CARTESIAN_POINT('Ctrl Pts',(22.2803795338411,4.34307229974981,-4.90023210615833));
#68730=CARTESIAN_POINT('Ctrl Pts',(22.3809494437989,6.15526704350443,-2.233212779434));
#68731=CARTESIAN_POINT('Ctrl Pts',(22.4815193537567,6.47481482783961,0.975358723889488));
#68732=CARTESIAN_POINT('Ctrl Pts',(22.5820892637145,5.22422559012998,3.94740657628651));
#68733=CARTESIAN_POINT('Ctrl Pts',(22.6826591736723,2.70676614397705,5.96221173197486));
#68734=CARTESIAN_POINT('Ctrl Pts',(22.7832290836301,-0.467081762028401,
6.53118567510214));
#68735=CARTESIAN_POINT('Ctrl Pts',(22.8837989935879,-3.52766274281934,5.51635271424909));
#68736=CARTESIAN_POINT('Ctrl Pts',(22.9843689035457,-5.73278854518983,3.16380896882526));
#68737=CARTESIAN_POINT('Ctrl Pts',(23.0849388135035,-6.5477180603006,0.0440442719588136));
#68738=CARTESIAN_POINT('Ctrl Pts',(23.1855087234613,-5.77483158225196,-3.08640112294309));
#68739=CARTESIAN_POINT('Ctrl Pts',(23.2860786334191,-3.60155341664784,-5.46839690239391));
#68740=CARTESIAN_POINT('Ctrl Pts',(23.3866485433769,-0.554901647827081,
-6.52431114036706));
#68741=CARTESIAN_POINT('Ctrl Pts',(23.4872184533347,2.62631329291648,-5.99808554311534));
#68742=CARTESIAN_POINT('Ctrl Pts',(23.5877883632925,5.17064952093358,-4.0173293649822));
#68743=CARTESIAN_POINT('Ctrl Pts',(23.6883582732503,6.46110769116769,-1.06237427407322));
#68744=CARTESIAN_POINT('Ctrl Pts',(23.7889281832081,6.18475280820045,2.15020566377629));
#68745=CARTESIAN_POINT('Ctrl Pts',(23.8894980931659,4.40860069325718,4.84136257911875));
#68746=CARTESIAN_POINT('Ctrl Pts',(23.9900680031237,1.56336670524895,6.35849323660865));
#68747=CARTESIAN_POINT('Ctrl Pts',(24.0906379130815,-1.66098236299125,6.33369475779431));
#68748=CARTESIAN_POINT('Ctrl Pts',(24.1912078230393,-4.48254463802734,4.77298075244091));
#68749=CARTESIAN_POINT('Ctrl Pts',(24.2917777329971,-6.21709369704475,2.05482302333931));
#68750=CARTESIAN_POINT('Ctrl Pts',(24.392347642955,-6.44400288638139,-1.16162752007148));
#68751=CARTESIAN_POINT('Ctrl Pts',(24.4929175529127,-5.108246922953,-4.09638438982722));
#68752=CARTESIAN_POINT('Ctrl Pts',(24.5934874628705,-2.53374547803398,-6.03777157133502));
#68753=CARTESIAN_POINT('Ctrl Pts',(24.6940573728283,0.655187064187529,-6.51500434428101));
#68754=CARTESIAN_POINT('Ctrl Pts',(24.7946272827861,3.68523730734736,-5.41235417204141));
#68755=CARTESIAN_POINT('Ctrl Pts',(24.8951971927439,5.82162067583343,-2.99721277219148));
#68756=CARTESIAN_POINT('Ctrl Pts',(24.9957671027017,6.54626604184792,0.144750144828189));
#68757=CARTESIAN_POINT('Ctrl Pts',(25.0963370126595,5.68344752792784,3.25161127633209));
#68758=CARTESIAN_POINT('Ctrl Pts',(25.1969069226173,3.44239788095986,5.5699594724057));
#68759=CARTESIAN_POINT('Ctrl Pts',(25.2974768325752,0.366569711173962,6.53759729120178));
#68760=CARTESIAN_POINT('Ctrl Pts',(25.3980467425329,-2.79815129801792,5.91987339463266));
#68761=CARTESIAN_POINT('Ctrl Pts',(25.4986166524908,-5.28432302616933,3.86658529586191));
#68762=CARTESIAN_POINT('Ctrl Pts',(25.5991865624485,-6.48905096937149,0.875653591312175));
#68763=CARTESIAN_POINT('Ctrl Pts',(25.6997564724063,-6.12018963846224,-2.32762335534304));
#68764=CARTESIAN_POINT('Ctrl Pts',(25.8003263823641,-4.26718758866067,-4.96645364201252));
#68765=CARTESIAN_POINT('Ctrl Pts',(25.9008962923219,-1.37939622192631,-6.40092319575969));
#68766=CARTESIAN_POINT('Ctrl Pts',(26.0014662022797,1.84289754120135,-6.28317438463338));
#68767=CARTESIAN_POINT('Ctrl Pts',(26.1020361122376,4.61829023700673,-4.64176119397017));
#68768=CARTESIAN_POINT('Ctrl Pts',(26.2026060221954,6.27375152589464,-1.87472490953036));
#68769=CARTESIAN_POINT('Ctrl Pts',(26.3031759321531,6.40783347037835,1.34693055165358));
#68770=CARTESIAN_POINT('Ctrl Pts',(26.403745842111,4.98802131434215,4.241956513538));
#68771=CARTESIAN_POINT('Ctrl Pts',(26.5043157520688,2.35861828340975,6.10831167248727));
#68772=CARTESIAN_POINT('Ctrl Pts',(26.6048856620265,-0.842747650883239,
6.49340650906823));
#68773=CARTESIAN_POINT('Ctrl Pts',(26.7054555719844,-3.8397480052984,5.30385585691071));
#68774=CARTESIAN_POINT('Ctrl Pts',(26.8060254819422,-5.90561277379389,2.82812472516355));
#68775=CARTESIAN_POINT('Ctrl Pts',(26.9065953918999,-6.5393715283652,-0.333424217904892));
#68776=CARTESIAN_POINT('Ctrl Pts',(27.0071653018578,-5.58733831658651,-3.41411807515254));
#68777=CARTESIAN_POINT('Ctrl Pts',(27.1077352118155,-3.28038037277664,-5.66689123814643));
#68778=CARTESIAN_POINT('Ctrl Pts',(27.2083051217734,-0.177933012413939,
-6.54544815411231));
#68779=CARTESIAN_POINT('Ctrl Pts',(27.3088750317312,2.96766295028931,-5.83673952721545));
#68780=CARTESIAN_POINT('Ctrl Pts',(27.4094449416889,5.39360320219676,-3.7126265894016));
#68781=CARTESIAN_POINT('Ctrl Pts',(27.5100148516468,6.51159932053983,-0.68820489959331));
#68782=CARTESIAN_POINT('Ctrl Pts',(27.6105847616046,6.05053820902341,2.50310588593983));
#68783=CARTESIAN_POINT('Ctrl Pts',(27.7111546715624,4.12222679029566,5.0874156488779));
#68784=CARTESIAN_POINT('Ctrl Pts',(27.8117245815202,1.19427892345224,6.43803149635638));
#68785=CARTESIAN_POINT('Ctrl Pts',(27.912294491478,-2.02328055425881,6.22743024801059));
#68786=CARTESIAN_POINT('Ctrl Pts',(28.0128644014358,-4.75019623926001,4.50668252527276));
#68787=CARTESIAN_POINT('Ctrl Pts',(28.1134343113936,-6.32519342534584,1.69306816963788));
#68788=CARTESIAN_POINT('Ctrl Pts',(28.2140042213514,-6.36633665069315,-1.53111375969258));
#68789=CARTESIAN_POINT('Ctrl Pts',(28.3145741313092,-4.86364871857258,-4.3840019203242));
#68790=CARTESIAN_POINT('Ctrl Pts',(28.415144041267,-2.18153015896644,-6.1737733891518));
#68791=CARTESIAN_POINT('Ctrl Pts',(28.5157139512248,1.02960758626534,-6.46641012567126));
#68792=CARTESIAN_POINT('Ctrl Pts',(28.6162838611825,3.99106637814351,-5.19094797318673));
#68793=CARTESIAN_POINT('Ctrl Pts',(28.7168537711404,5.98469500894628,-2.6566854057213));
#68794=CARTESIAN_POINT('Ctrl Pts',(28.8174236810982,6.52704025187666,0.521821085680566));
#68795=CARTESIAN_POINT('Ctrl Pts',(28.917993591056,5.48658385239039,3.57378641300344));
#68796=CARTESIAN_POINT('Ctrl Pts',(29.0185635010138,3.1156355917082,5.7591116115908));
#68797=CARTESIAN_POINT('Ctrl Pts',(29.1191334109716,-0.0108516179347542,
6.54785720197586));
#68798=CARTESIAN_POINT('Ctrl Pts',(29.2197033209294,-3.13470731956994,5.74875305746505));
#68799=CARTESIAN_POINT('Ctrl Pts',(29.3202732308872,-5.49839919465536,3.55558124521044));
#68800=CARTESIAN_POINT('Ctrl Pts',(29.420843140845,-6.52873399821658,0.500184041738617));
#68801=CARTESIAN_POINT('Ctrl Pts',(29.5214130508028,-5.97585642733173,-2.67650736128206));
#68802=CARTESIAN_POINT('Ctrl Pts',(29.6219829607606,-3.97383881700753,-5.20414803320613));
#68803=CARTESIAN_POINT('Ctrl Pts',(29.7225528707184,-1.00816871435342,-6.46978728695758));
#68804=CARTESIAN_POINT('Ctrl Pts',(29.8231227806762,2.20198143367085,-6.16650869300027));
#68805=CARTESIAN_POINT('Ctrl Pts',(29.923692690634,4.87815297955871,-4.36785704929791));
#68806=CARTESIAN_POINT('Ctrl Pts',(30.0242626005918,6.37137662715756,-1.51000383111742));
#68807=CARTESIAN_POINT('Ctrl Pts',(30.1248325105496,6.31954692733444,1.71402401625443));
#68808=CARTESIAN_POINT('Ctrl Pts',(30.2254024205074,4.73523253767991,4.52240251516562));
#68809=CARTESIAN_POINT('Ctrl Pts',(30.3259723304652,2.00262833386201,6.23410229716292));
#68810=CARTESIAN_POINT('Ctrl Pts',(30.426542240423,-1.21561151699755,6.43403763859227));
#68811=CARTESIAN_POINT('Ctrl Pts',(30.5271121503808,-4.13906662141845,5.07372439126708));
#68812=CARTESIAN_POINT('Ctrl Pts',(30.6276820603386,-6.05880163317263,2.48303734666711));
#68813=CARTESIAN_POINT('Ctrl Pts',(30.7282519702964,-6.50928246447265,-0.709784117029887));
#68814=CARTESIAN_POINT('Ctrl Pts',(30.8288218802542,-5.38126790151506,-3.73048354334966));
#68815=CARTESIAN_POINT('Ctrl Pts',(30.929391790212,-2.94830050478984,-5.84654392171433));
#68816=CARTESIAN_POINT('Ctrl Pts',(31.0299617001698,0.199627226365273,-6.54482243193601));
#68817=CARTESIAN_POINT('Ctrl Pts',(31.1305316101276,3.29914552697168,-5.65598713638404));
#68818=CARTESIAN_POINT('Ctrl Pts',(31.2311015200854,5.59862387728656,-3.39557982909486));
#68819=CARTESIAN_POINT('Ctrl Pts',(31.3316714300432,6.54044075681541,-0.31174733626264));
#68820=CARTESIAN_POINT('Ctrl Pts',(31.432241340001,5.89620638301548,2.84768361725218));
#68821=CARTESIAN_POINT('Ctrl Pts',(31.5328112499588,3.82214703695784,5.31655374495108));
#68822=CARTESIAN_POINT('Ctrl Pts',(31.6333811599166,0.821220324651722,6.49616416614127));
#68823=CARTESIAN_POINT('Ctrl Pts',(31.7339510698744,-2.37885160945245,6.10046036912662));
#68824=CARTESIAN_POINT('Ctrl Pts',(31.8345209798322,-5.00205407604808,4.22540018405));
#68825=CARTESIAN_POINT('Ctrl Pts',(31.9350908897901,-6.41226273511366,1.32568409168691));
#68826=CARTESIAN_POINT('Ctrl Pts',(32.0356607997479,-6.26750320077382,-1.89550925172337));
#68827=CARTESIAN_POINT('Ctrl Pts',(32.1362307097056,-4.60287953549285,-4.65704323329943));
#68828=CARTESIAN_POINT('Ctrl Pts',(32.2368006196634,-1.8220615451456,-6.28924823971678));
#68829=CARTESIAN_POINT('Ctrl Pts',(32.3373705296213,1.40060480141665,-6.39631596196808));
#68830=CARTESIAN_POINT('Ctrl Pts',(32.4379404395791,4.28362568931618,-4.95228256957432));
#68831=CARTESIAN_POINT('Ctrl Pts',(32.5385103495368,6.12787103502435,-2.30732491712561));
#68832=CARTESIAN_POINT('Ctrl Pts',(32.6390802594947,6.48611292978621,0.897157041514567));
#68833=CARTESIAN_POINT('Ctrl Pts',(32.7396501694525,5.27147802250694,3.88407918988595));
#68834=CARTESIAN_POINT('Ctrl Pts',(32.8402200794102,2.77851423260925,5.92911547823676));
#68835=CARTESIAN_POINT('Ctrl Pts',(32.9407899893681,-0.388236866871482,
6.53634636706784));
#68836=CARTESIAN_POINT('Ctrl Pts',(33.0413598993259,-3.46084086034133,5.55851888855933));
#68837=CARTESIAN_POINT('Ctrl Pts',(33.1419298092837,-5.69419392436947,3.23275536450764));
#68838=CARTESIAN_POINT('Ctrl Pts',(33.2424997192415,-6.5467098634634,0.123051447411384));
#68839=CARTESIAN_POINT('Ctrl Pts',(33.3430696291993,-5.81165429626306,-3.01649233975588));
#68840=CARTESIAN_POINT('Ctrl Pts',(33.4436395391571,-3.66727756505767,-5.42453933121548));
#68841=CARTESIAN_POINT('Ctrl Pts',(33.5442094491149,-0.63358918122346,-6.51714020445437));
#68842=CARTESIAN_POINT('Ctrl Pts',(33.6447793590727,2.55374403364572,-6.02934018825426));
#68843=CARTESIAN_POINT('Ctrl Pts',(33.7453492690305,5.12179651869192,-4.0794303666314));
#68844=CARTESIAN_POINT('Ctrl Pts',(33.8459191789882,6.4478177569446,-1.14026219279109));
#68845=CARTESIAN_POINT('Ctrl Pts',(33.9464890889461,6.21024873960468,2.07541858123063));
#68846=CARTESIAN_POINT('Ctrl Pts',(34.0470589989039,4.46669974887087,4.78781213588376));
#68847=CARTESIAN_POINT('Ctrl Pts',(34.1476289088617,1.6399799140991,6.33916536907113));
#68848=CARTESIAN_POINT('Ctrl Pts',(34.2481988188195,-1.58443363809996,6.35327645719405));
#68849=CARTESIAN_POINT('Ctrl Pts',(34.3487687287773,-4.4246233969857,4.82672347353003));
#68850=CARTESIAN_POINT('Ctrl Pts',(34.4493386387351,-6.19184579094511,2.12969420251694));
#68851=CARTESIAN_POINT('Ctrl Pts',(34.5499085486929,-6.45755091071877,-1.08378407930465));
#68852=CARTESIAN_POINT('Ctrl Pts',(34.6504784586507,-5.15730549348813,-4.03444565484728));
#68853=CARTESIAN_POINT('Ctrl Pts',(34.7510483686085,-2.60641793364311,-6.00675763205597));
#68854=CARTESIAN_POINT('Ctrl Pts',(34.8516182785662,0.576523731431076,-6.52243605428032));
#68855=CARTESIAN_POINT('Ctrl Pts',(34.9521881885241,3.61965888792138,-5.45642934804169));
#68856=CARTESIAN_POINT('Ctrl Pts',(35.0527580984819,5.78502987999693,-3.06724322195383));
#68857=CARTESIAN_POINT('Ctrl Pts',(35.1533280084397,6.54753610609284,0.0657467450869154));
#68858=CARTESIAN_POINT('Ctrl Pts',(35.2538979183975,5.72227046276811,3.18279318304076));
#68859=CARTESIAN_POINT('Ctrl Pts',(35.3544678283553,3.50935915811661,5.52801501394688));
#68860=CARTESIAN_POINT('Ctrl Pts',(35.4550377383131,0.445431278578845,6.53269796264472));
#68861=CARTESIAN_POINT('Ctrl Pts',(35.5556076482709,-2.72651330257426,5.953207278935));
#68862=CARTESIAN_POINT('Ctrl Pts',(35.6561775582287,-5.23728075491397,3.93006895477507));
#68863=CARTESIAN_POINT('Ctrl Pts',(35.7567474681865,-6.47801213258849,0.953892292198258));
#68864=CARTESIAN_POINT('Ctrl Pts',(35.8573173781443,-6.14783114456894,-2.25360243009879));
#68865=CARTESIAN_POINT('Ctrl Pts',(35.9578872881021,-4.32680639622078,-4.91460050306248));
#68866=CARTESIAN_POINT('Ctrl Pts',(36.0584571980599,-1.4565348214281,-6.38381218466258));
#68867=CARTESIAN_POINT('Ctrl Pts',(36.1590271080177,1.76694519373391,-6.3049549068506));
#68868=CARTESIAN_POINT('Ctrl Pts',(36.2595970179755,4.56194252045255,-4.6971514916134));
#68869=CARTESIAN_POINT('Ctrl Pts',(36.3601669279333,6.25067271301243,-1.95029288310264));
#68870=CARTESIAN_POINT('Ctrl Pts',(36.4607368378911,6.42362015342513,1.26951007069249));
#68871=CARTESIAN_POINT('Ctrl Pts',(36.5613067478489,5.03884523626863,4.18145792517538));
#68872=CARTESIAN_POINT('Ctrl Pts',(36.6618766578068,2.4321546868995,6.07940583232208));
#68873=CARTESIAN_POINT('Ctrl Pts',(36.7624465677644,-0.764331280374237,
6.50310305845758));
#68874=CARTESIAN_POINT('Ctrl Pts',(36.8630164777223,-3.7754675701155,5.34980339097476));
#68875=CARTESIAN_POINT('Ctrl Pts',(36.9635863876801,-5.87105622413455,2.89918100644475));
#68876=CARTESIAN_POINT('Ctrl Pts',(37.0641562976379,-6.54291879777455,-0.254490276450008));
#68877=CARTESIAN_POINT('Ctrl Pts',(37.1647262075958,-5.62812919528632,-3.34644788637817));
#68878=CARTESIAN_POINT('Ctrl Pts',(37.2652961175535,-3.34852310779617,-5.62689476457788));
#68879=CARTESIAN_POINT('Ctrl Pts',(37.3658660275114,-0.256903049170209,
-6.54282450615985));
#68880=CARTESIAN_POINT('Ctrl Pts',(37.4664359374691,2.89701577773001,-5.87212493724906));
#68881=CARTESIAN_POINT('Ctrl Pts',(37.567005847427,5.348410772365,-3.77744012594893));
#68882=CARTESIAN_POINT('Ctrl Pts',(37.6675757573847,6.50282075876685,-0.766729335834957));
#68883=CARTESIAN_POINT('Ctrl Pts',(37.7681456673425,6.08030230898233,2.42991265819638));
#68884=CARTESIAN_POINT('Ctrl Pts',(37.8687155773003,4.18331578336822,5.03730292435361));
#68885=CARTESIAN_POINT('Ctrl Pts',(37.9692854872581,1.27187878140549,6.4231515676099));
#68886=CARTESIAN_POINT('Ctrl Pts',(38.0698553972159,-1.94798773017833,6.25139148495386));
#68887=CARTESIAN_POINT('Ctrl Pts',(38.1704253071738,-4.69546889407762,4.56367434857359));
#68888=CARTESIAN_POINT('Ctrl Pts',(38.2709952171315,-6.30430289315735,1.76927011120597));
#68889=CARTESIAN_POINT('Ctrl Pts',(38.3715651270894,-6.38434886757117,-1.45418060509064));
#68890=CARTESIAN_POINT('Ctrl Pts',(38.4721350370471,-4.91619573742957,-4.32499377645314));
#68891=CARTESIAN_POINT('Ctrl Pts',(38.572704947005,-2.25586937296357,-6.14699968010442));
#68892=CARTESIAN_POINT('Ctrl Pts',(38.6732748569627,0.95150337252903,-6.47836345284401));
#68893=CARTESIAN_POINT('Ctrl Pts',(38.7738447669205,3.92813736926474,-5.23872966502996));
#68894=CARTESIAN_POINT('Ctrl Pts',(38.8744146768784,5.95220143540704,-2.72870844309488));
#68895=CARTESIAN_POINT('Ctrl Pts',(38.9749845868361,6.53286177728884,0.44302222734022));
#68896=CARTESIAN_POINT('Ctrl Pts',(39.075554496794,5.52930876185287,3.50732038901156));
#68897=CARTESIAN_POINT('Ctrl Pts',(39.1761244067517,3.18490313145511,5.72109637554957));
#68898=CARTESIAN_POINT('Ctrl Pts',(39.2766943167096,0.068161233335458,6.54751141590063));
#68899=CARTESIAN_POINT('Ctrl Pts',(39.3772642266674,-3.06510970519291,5.78616057418141));
#68900=CARTESIAN_POINT('Ctrl Pts',(39.4778341366252,-5.45509417874633,3.62167077411613));
#68901=CARTESIAN_POINT('Ctrl Pts',(39.5784040465829,-6.52222300985525,0.578928928965803));
#68902=CARTESIAN_POINT('Ctrl Pts',(39.6789739565408,-6.00771837559096,-2.6042026831001));
#68903=CARTESIAN_POINT('Ctrl Pts',(39.7795438664985,-4.0363472068621,-5.15581738628664));
#68904=CARTESIAN_POINT('Ctrl Pts',(39.8801137764564,-1.0861653150726,-6.45715081157412));
#68905=CARTESIAN_POINT('Ctrl Pts',(39.9806836864142,2.12741073061978,-6.19263072355546));
#68906=CARTESIAN_POINT('Ctrl Pts',(40.081253596372,4.82509150547297,-4.42640301586869));
#68907=CARTESIAN_POINT('Ctrl Pts',(40.1818235063298,6.35269174382611,-1.58677638720847));
#68908=CARTESIAN_POINT('Ctrl Pts',(40.2823934162875,6.3397697028807,1.63764214940717));
#68909=CARTESIAN_POINT('Ctrl Pts',(40.3829633262454,4.78945896644229,4.46493387452094));
#68910=CARTESIAN_POINT('Ctrl Pts',(40.4835332362032,2.07770855354523,6.20948297860651));
#68911=CARTESIAN_POINT('Ctrl Pts',(40.584103146161,-1.13788439503546,6.44823780568102));
#68912=CARTESIAN_POINT('Ctrl Pts',(40.6846730561188,-4.07754135734353,5.12330051570587));
#68913=CARTESIAN_POINT('Ctrl Pts',(40.7852429660766,-6.02839805056031,2.5559672609561));
#68914=CARTESIAN_POINT('Ctrl Pts',(40.8858128760344,-6.51737340593419,-0.631185854325582));
#68915=CARTESIAN_POINT('Ctrl Pts',(40.9863827859922,-5.42589132071097,-3.66527694327624));
#68916=CARTESIAN_POINT('Ctrl Pts',(41.08695269595,-3.01863526097817,-5.81054152865792));
#68917=CARTESIAN_POINT('Ctrl Pts',(41.1875226059078,0.12063725101407,-6.54675479522083));
#68918=CARTESIAN_POINT('Ctrl Pts',(41.2880925158656,3.23065533348335,-5.69538565957693));
#68919=CARTESIAN_POINT('Ctrl Pts',(41.3886624258234,5.55724227862367,-3.46289040423696));
#68920=CARTESIAN_POINT('Ctrl Pts',(41.4892323357812,6.5362027550313,-0.39064720682494));
#68921=CARTESIAN_POINT('Ctrl Pts',(41.589802245739,5.93013968989465,2.77632760196186));
#68922=CARTESIAN_POINT('Ctrl Pts',(41.6903721556968,3.88602285479283,5.27004535721532));
#68923=CARTESIAN_POINT('Ctrl Pts',(41.7909420656546,0.899548822603686,6.48578164995024));
#68924=CARTESIAN_POINT('Ctrl Pts',(41.8915119756124,-2.30506502470944,6.12872147571909));
#68925=CARTESIAN_POINT('Ctrl Pts',(41.9920818855702,-4.9507025877966,4.28545161940524));
#68926=CARTESIAN_POINT('Ctrl Pts',(42.092651795528,-6.39579903504983,1.40296343442533));
#68927=CARTESIAN_POINT('Ctrl Pts',(42.1932217054858,-6.28991972199076,-1.81974217569154));
#68928=CARTESIAN_POINT('Ctrl Pts',(42.2937916154436,-4.65874029089223,-4.60116187468952));
#68929=CARTESIAN_POINT('Ctrl Pts',(42.3943615254014,-1.89782034962951,-6.26680377988744));
#68930=CARTESIAN_POINT('Ctrl Pts',(42.4949314353592,1.3233193927202,-6.41275116310696));
#68931=CARTESIAN_POINT('Ctrl Pts',(42.595501345317,4.22355532148648,-5.00361190955315));
#68932=CARTESIAN_POINT('Ctrl Pts',(42.6960712552748,6.09958272054981,-2.3811010751854));
#68933=CARTESIAN_POINT('Ctrl Pts',(42.7966411652326,6.4964665605756,0.818824720194698));
#68934=CARTESIAN_POINT('Ctrl Pts',(42.8972110751904,5.31796285200656,3.82018622579545));
#68935=CARTESIAN_POINT('Ctrl Pts',(42.9977809851482,2.84985772968081,5.8951558601667));
#68936=CARTESIAN_POINT('Ctrl Pts',(43.098350895106,-0.309335438853322,6.54055527316669));
#68937=CARTESIAN_POINT('Ctrl Pts',(43.1989208050639,-3.39351502975027,5.59987566272126));
#68938=CARTESIAN_POINT('Ctrl Pts',(43.2994907150216,-5.65477014716779,3.30123102459958));
#68939=CARTESIAN_POINT('Ctrl Pts',(43.4000606249794,-6.5447483716855,0.202040704806857));
#68940=CARTESIAN_POINT('Ctrl Pts',(43.5006305349372,-5.84763074997661,-2.94614431197915));
#68941=CARTESIAN_POINT('Ctrl Pts',(43.601200444895,-3.73246770520662,-5.37989186923573));
#68942=CARTESIAN_POINT('Ctrl Pts',(43.7017703548528,-0.712184454939265,
-6.50902027936784));
#68943=CARTESIAN_POINT('Ctrl Pts',(43.8023402648106,2.48080291258205,-6.05971687490459));
#68944=CARTESIAN_POINT('Ctrl Pts',(43.9029101747684,5.07219770934852,-4.14093734465504));
#68945=CARTESIAN_POINT('Ctrl Pts',(44.0034800847263,6.4335889278912,-1.21798407296426));
#68946=CARTESIAN_POINT('Ctrl Pts',(44.104049994684,6.23484036963815,2.00032928794473));
#68947=CARTESIAN_POINT('Ctrl Pts',(44.2046199046419,4.5241483888772,4.73356451846799));
#68948=CARTESIAN_POINT('Ctrl Pts',(44.3051898145997,1.71635431833013,6.3189144280508));
#68949=CARTESIAN_POINT('Ctrl Pts',(44.4057597245574,-1.5076541969249,6.37193302833398));
#68950=CARTESIAN_POINT('Ctrl Pts',(44.5063296345153,-4.36605786725757,4.87976335438894));
#68951=CARTESIAN_POINT('Ctrl Pts',(44.606899544473,-6.16569626320814,2.20425526764484));
#68952=CARTESIAN_POINT('Ctrl Pts',(44.7074694544309,-6.47015862293896,-1.00578282401701));
#68953=CARTESIAN_POINT('Ctrl Pts',(44.8080393643886,-5.20561308630515,-3.97191944666151));
#68954=CARTESIAN_POINT('Ctrl Pts',(44.9086092743465,-2.67871085738329,-5.97486902263271));
#68955=CARTESIAN_POINT('Ctrl Pts',(45.0091791843042,0.497776448542833,-6.52891800395401));
#68956=CARTESIAN_POINT('Ctrl Pts',(45.1097490942621,3.5535533941975,-5.49970998959639));
#68957=CARTESIAN_POINT('Ctrl Pts',(45.2103190042198,5.74759670075998,-3.13682703706976));
#68958=CARTESIAN_POINT('Ctrl Pts',(45.3108889141777,6.5478527550843,-0.0132662283243582));
#68959=CARTESIAN_POINT('Ctrl Pts',(45.4114588241354,5.76026015288009,3.11351162936983));
#68960=CARTESIAN_POINT('Ctrl Pts',(45.5120287340933,3.5758094221995,5.48526559714188));
#68961=CARTESIAN_POINT('Ctrl Pts',(45.612598644051,0.524227984794888,6.5268473794809));
#68962=CARTESIAN_POINT('Ctrl Pts',(45.7131685540089,-2.65447828765195,5.98567429079325));
#68963=CARTESIAN_POINT('Ctrl Pts',(45.8137384639667,-5.18947586039424,3.99298033922837));
#68964=CARTESIAN_POINT('Ctrl Pts',(45.9143083739244,-6.46603000424065,1.03199209267258));
#68965=CARTESIAN_POINT('Ctrl Pts',(46.0148782838823,-6.17457743820275,-2.17925334798793));
#68966=CARTESIAN_POINT('Ctrl Pts',(46.1154481938401,-4.38579515865401,-4.86203172772514));
#68967=CARTESIAN_POINT('Ctrl Pts',(46.2160181037979,-1.53346132854994,-6.36577159886536));
#68968=CARTESIAN_POINT('Ctrl Pts',(46.3165880137557,1.69073555368001,-6.32581733711948));
#68969=CARTESIAN_POINT('Ctrl Pts',(46.4171579237134,4.5049305195762,-4.75185781656709));
#68970=CARTESIAN_POINT('Ctrl Pts',(46.5177278336713,6.22668371244857,-2.02557686603268));
#68971=CARTESIAN_POINT('Ctrl Pts',(46.618297743629,6.43847146516005,1.19190473084001));
#68972=CARTESIAN_POINT('Ctrl Pts',(46.7188676535869,5.0889354299911,4.12035045650976));
#68973=CARTESIAN_POINT('Ctrl Pts',(46.8194375635447,2.50533693375088,6.04961474339174));
#68974=CARTESIAN_POINT('Ctrl Pts',(46.9200074735025,-0.685803612258052,
6.51185266268309));
#68975=CARTESIAN_POINT('Ctrl Pts',(47.0205773834603,-3.71063737265382,5.3949719168633));
#68976=CARTESIAN_POINT('Ctrl Pts',(47.1211472934181,-5.83564476440411,2.96981512535072));
#68977=CARTESIAN_POINT('Ctrl Pts',(47.2217172033759,-6.54551332427677,-0.175519277557393));
#68978=CARTESIAN_POINT('Ctrl Pts',(47.3222871133337,-5.66810053757789,-3.27829040674986));
#68979=CARTESIAN_POINT('Ctrl Pts',(47.4228570232914,-3.41617824977988,-5.58607893435188));
#68980=CARTESIAN_POINT('Ctrl Pts',(47.5234269332493,-0.335835677154444,
-6.53924812903053));
#68981=CARTESIAN_POINT('Ctrl Pts',(47.6239968432071,2.82594675808396,-5.90665528159158));
#68982=CARTESIAN_POINT('Ctrl Pts',(47.724566753165,5.30243953714302,-3.84170361298495));
#68983=CARTESIAN_POINT('Ctrl Pts',(47.8251366631226,6.49309529293691,-0.8451421252781));
#68984=CARTESIAN_POINT('Ctrl Pts',(47.9257065730806,6.10918102963623,2.3563656002861));
#68985=CARTESIAN_POINT('Ctrl Pts',(48.0262764830382,4.24379562560702,4.98645669620802));
#68986=CARTESIAN_POINT('Ctrl Pts',(48.1268463929962,1.34929343554907,6.40733633578441));
#68987=CARTESIAN_POINT('Ctrl Pts',(48.2274163029538,-1.87241125111904,6.27444242955194));
#68988=CARTESIAN_POINT('Ctrl Pts',(48.3279862129117,-4.64005782121609,4.62000163537314));
#68989=CARTESIAN_POINT('Ctrl Pts',(48.4285561228695,-6.28249436396308,1.84521442164623));
#68990=CARTESIAN_POINT('Ctrl Pts',(48.5291260328273,-6.40143143160032,-1.3770357009164));
#68991=CARTESIAN_POINT('Ctrl Pts',(48.6296959427851,-4.96802688761027,-4.26535585139861));
#68992=CARTESIAN_POINT('Ctrl Pts',(48.7302658527429,-2.32988009999474,-6.11933087965732));
#68993=CARTESIAN_POINT('Ctrl Pts',(48.8308357627007,0.873260606241912,-6.4893734372946));
#68994=CARTESIAN_POINT('Ctrl Pts',(48.9314056726586,3.86463636719267,-5.28574852262676));
#68995=CARTESIAN_POINT('Ctrl Pts',(49.0319755826163,5.91884113588903,-2.80033414134579));
#68996=CARTESIAN_POINT('Ctrl Pts',(49.1325454925741,6.53773202424047,0.364158858603563));
#68997=CARTESIAN_POINT('Ctrl Pts',(49.2331154025319,5.57122852458084,3.44034364881996));
#68998=CARTESIAN_POINT('Ctrl Pts',(49.3336853124897,3.25370690358363,5.68224806574399));
#68999=CARTESIAN_POINT('Ctrl Pts',(49.4342552224475,0.147164159351603,6.54621221816718));
#69000=CARTESIAN_POINT('Ctrl Pts',(49.5348251324053,-2.99506576684006,5.82272554285206));
#69001=CARTESIAN_POINT('Ctrl Pts',(49.6353950423632,-5.41099482281151,3.68723293576444));
#69002=CARTESIAN_POINT('Ctrl Pts',(49.7359649523209,-6.51476229219069,0.657589515829798));
#69003=CARTESIAN_POINT('Ctrl Pts',(49.8365348622787,-6.03870551380784,-2.53151879562165));
#69004=CARTESIAN_POINT('Ctrl Pts',(49.9371047722365,-4.09826784661749,-5.10673597833884));
#69005=CARTESIAN_POINT('Ctrl Pts',(50.0376746821944,-1.16400375452887,-6.44357408233362));
#69006=CARTESIAN_POINT('Ctrl Pts',(50.1382445921521,2.05253024602511,-6.21785101817589));
#69007=CARTESIAN_POINT('Ctrl Pts',(50.23881450211,4.77132742879492,-4.48430443461504));
#69008=CARTESIAN_POINT('Ctrl Pts',(50.3393844120677,6.33308181737752,-1.66331788587789));
#69009=CARTESIAN_POINT('Ctrl Pts',(50.4399543220256,6.35906931694452,1.56102181835299));
#69010=CARTESIAN_POINT('Ctrl Pts',(50.5405242319833,4.84298798122161,4.4068150754056));
#69011=CARTESIAN_POINT('Ctrl Pts',(50.6410941419412,2.15248622903544,6.18395947018508));
#69012=CARTESIAN_POINT('Ctrl Pts',(50.7416640518989,-1.05999158076988,6.46149901677434));
#69013=CARTESIAN_POINT('Ctrl Pts',(50.8422339618568,-4.01542234470967,5.17213061403956));
#69014=CARTESIAN_POINT('Ctrl Pts',(50.9428038718145,-5.99711664664814,2.62852498971853));
#69015=CARTESIAN_POINT('Ctrl Pts',(51.0433737817724,-6.52451532426444,-0.552495681899622));
#69016=CARTESIAN_POINT('Ctrl Pts',(51.1439436917301,-5.46972465223643,-3.59953662626124));
#69017=CARTESIAN_POINT('Ctrl Pts',(51.244513601688,-3.08853046053694,-5.77369303733878));
#69018=CARTESIAN_POINT('Ctrl Pts',(51.3450835116457,0.0416297091470886,
-6.54773385702222));
#69019=CARTESIAN_POINT('Ctrl Pts',(51.4456534216036,3.16169471019899,-5.73395485285493));
#69020=CARTESIAN_POINT('Ctrl Pts',(51.5462233315613,5.51505146570521,-3.52969673282309));
#69021=CARTESIAN_POINT('Ctrl Pts',(51.6467932415192,6.53101298829235,-0.469490193545743));
#69022=CARTESIAN_POINT('Ctrl Pts',(51.7473631514769,5.96320948330187,2.7045673135158));
#69023=CARTESIAN_POINT('Ctrl Pts',(51.8479330614348,3.94933281191226,5.22276957521886));
#69024=CARTESIAN_POINT('Ctrl Pts',(51.9485029713926,0.977746333333282,6.47445471084103));
#69025=CARTESIAN_POINT('Ctrl Pts',(52.0490728813504,-2.23094278940758,6.15609015248089));
#69026=CARTESIAN_POINT('Ctrl Pts',(52.1496427913082,-4.89863020617543,4.34487903148253));
#69027=CARTESIAN_POINT('Ctrl Pts',(52.2502127012659,-6.37840401482964,1.4800384855472));
#69028=CARTESIAN_POINT('Ctrl Pts',(52.3507826112238,-6.31142034059575,-1.74371011907603));
#69029=CARTESIAN_POINT('Ctrl Pts',(52.4513525211815,-4.71392266682865,-4.54461052085449));
#69030=CARTESIAN_POINT('Ctrl Pts',(52.5519224311394,-1.97330280421664,-6.24344678346548));
#69031=CARTESIAN_POINT('Ctrl Pts',(52.6524923410972,1.24584128970535,-6.42825257560717));
#69032=CARTESIAN_POINT('Ctrl Pts',(52.7530622510549,4.16286994340196,-5.05421265182165));
#69033=CARTESIAN_POINT('Ctrl Pts',(52.8536321610128,6.07040621920021,-2.45453051071525));
#69034=CARTESIAN_POINT('Ctrl Pts',(52.9542020709706,6.50587421269849,0.740373166181634));
#69035=CARTESIAN_POINT('Ctrl Pts',(53.0547719809284,5.36367330951959,3.75573698786384));
#69036=CARTESIAN_POINT('Ctrl Pts',(53.1553418908862,2.92078624704449,5.86033782254595));
#69037=CARTESIAN_POINT('Ctrl Pts',(53.2559118008439,-0.230388968113506,
6.54381178096489));
#69038=CARTESIAN_POINT('Ctrl Pts',(53.3564817108019,-3.3256950527764,5.64041701372739));
#69039=CARTESIAN_POINT('Ctrl Pts',(53.4570516207595,-5.61452295792606,3.36922597975961));
#69040=CARTESIAN_POINT('Ctrl Pts',(53.5576215307174,-6.54183386340029,0.281000538852744));
#69041=CARTESIAN_POINT('Ctrl Pts',(53.6581914406752,-5.88275571877033,-2.87536727679449));
#69042=CARTESIAN_POINT('Ctrl Pts',(53.758761350633,-3.79711431694879,-5.3344610304885));
#69043=CARTESIAN_POINT('Ctrl Pts',(53.8593312605908,-0.790676078238258,
-6.49995252258906));
#69044=CARTESIAN_POINT('Ctrl Pts',(53.9599011705485,2.40750065640528,-6.08921122850316));
#69045=CARTESIAN_POINT('Ctrl Pts',(54.0604710805064,5.02186010893717,-4.20184124741766));
#69046=CARTESIAN_POINT('Ctrl Pts',(54.1610409904642,6.41842367956464,-1.29552878373208));
#69047=CARTESIAN_POINT('Ctrl Pts',(54.261610900422,6.25852332754194,1.92494908307514));
#69048=CARTESIAN_POINT('Ctrl Pts',(54.3621808103799,4.58093979359666,4.67862691169207));
#69049=CARTESIAN_POINT('Ctrl Pts',(54.4627507203375,1.79247577205141,6.2977447603908));
#69050=CARTESIAN_POINT('Ctrl Pts',(54.5633206302954,-1.43064930071301,6.38965901879497));
#69051=CARTESIAN_POINT('Ctrl Pts',(54.6638905402532,-4.30686815961765,4.93209802530353));
#69052=CARTESIAN_POINT('Ctrl Pts',(54.7644604502111,-6.13862625381269,2.27848488382594));
#69053=CARTESIAN_POINT('Ctrl Pts',(54.8650303601687,-6.48186856325177,-0.927614594694319));
#69054=CARTESIAN_POINT('Ctrl Pts',(54.9656002701267,-5.25307563387778,-3.90885517127706));
#69055=CARTESIAN_POINT('Ctrl Pts',(55.0661701800844,-2.7507861368141,-5.94202989429022));
#69056=CARTESIAN_POINT('Ctrl Pts',(55.1667400900422,0.419316711856036,-6.53462427730853));
#69057=CARTESIAN_POINT('Ctrl Pts',(55.2337866966808,2.46375373567196,-5.87263820593936));
#69058=CARTESIAN_POINT('Ctrl Pts',(55.26731,3.34571636511773,-5.31774159209371));
#69059=CARTESIAN_POINT('Ctrl Pts',(18.5943714011907,3.74381434373823,-4.74963296131605));
#69060=CARTESIAN_POINT('Ctrl Pts',(18.62789470451,4.53155453436587,-4.12871066082871));
#69061=CARTESIAN_POINT('Ctrl Pts',(18.6949413111485,5.79137112877805,-2.48801589670783));
#69062=CARTESIAN_POINT('Ctrl Pts',(18.7955112211063,6.27641633085685,0.578268110945115));
#69063=CARTESIAN_POINT('Ctrl Pts',(18.8960811310641,5.23951763712497,3.50352722589919));
#69064=CARTESIAN_POINT('Ctrl Pts',(18.9966510410219,2.93200383757313,5.57957477908284));
#69065=CARTESIAN_POINT('Ctrl Pts',(19.0972209509797,-0.0865001488795471,
6.30238201346393));
#69066=CARTESIAN_POINT('Ctrl Pts',(19.1977908609375,-3.0840371900228,5.49696820322353));
#69067=CARTESIAN_POINT('Ctrl Pts',(19.2983607708953,-5.33369313625283,3.35849264924486));
#69068=CARTESIAN_POINT('Ctrl Pts',(19.3989306808531,-6.28993550566722,0.405611930459287));
#69069=CARTESIAN_POINT('Ctrl Pts',(19.499500590811,-5.72087269424937,-2.64564282898167));
#69070=CARTESIAN_POINT('Ctrl Pts',(19.6000705007687,-3.76450381040718,-5.05532458279635));
#69071=CARTESIAN_POINT('Ctrl Pts',(19.7006404107266,-0.895245670559178,
-6.23909800156691));
#69072=CARTESIAN_POINT('Ctrl Pts',(19.8012103206843,2.19110860890456,-5.90989372465953));
#69073=CARTESIAN_POINT('Ctrl Pts',(19.9017802306422,4.74612102111524,-4.14754622731969));
#69074=CARTESIAN_POINT('Ctrl Pts',(20.0023501405999,6.1502031282558,-1.37942186984454));
#69075=CARTESIAN_POINT('Ctrl Pts',(20.1029200505578,6.06286629306327,1.7232108632711));
#69076=CARTESIAN_POINT('Ctrl Pts',(20.2034899605155,4.50528958965082,4.40796656825658));
#69077=CARTESIAN_POINT('Ctrl Pts',(20.3040598704734,1.85518404477503,6.02379411217868));
#69078=CARTESIAN_POINT('Ctrl Pts',(20.4046297804312,-1.24480203689863,6.17885680142634));
#69079=CARTESIAN_POINT('Ctrl Pts',(20.505199690389,-4.04292469468554,4.83555201887475));
#69080=CARTESIAN_POINT('Ctrl Pts',(20.6057696003468,-5.86064159504332,2.31963004270374));
#69081=CARTESIAN_POINT('Ctrl Pts',(20.7063395103045,-6.25715795321971,-0.758800226299075));
#69082=CARTESIAN_POINT('Ctrl Pts',(20.8069094202624,-5.13631889428152,-3.65322209143408));
#69083=CARTESIAN_POINT('Ctrl Pts',(20.9074793302201,-2.76992692486838,-5.66174074531242));
#69084=CARTESIAN_POINT('Ctrl Pts',(21.008049240178,0.268169939340544,-6.29729214167012));
#69085=CARTESIAN_POINT('Ctrl Pts',(21.1086191501357,3.24123582413446,-5.40575561485436));
#69086=CARTESIAN_POINT('Ctrl Pts',(21.2091890600936,5.42830481171089,-3.20332800471673));
#69087=CARTESIAN_POINT('Ctrl Pts',(21.3097589700514,6.29901455529484,-0.224096111028122));
#69088=CARTESIAN_POINT('Ctrl Pts',(21.4103288800092,5.64221869158862,2.8094788967154));
#69089=CARTESIAN_POINT('Ctrl Pts',(21.510898789967,3.61718965215762,5.16175769046553));
#69090=CARTESIAN_POINT('Ctrl Pts',(21.6114686999248,0.714995235858073,6.26231468767699));
#69091=CARTESIAN_POINT('Ctrl Pts',(21.7120386098826,-2.36058490964819,5.84426576390167));
#69092=CARTESIAN_POINT('Ctrl Pts',(21.8126085198403,-4.86372524662418,4.00898742329443));
#69093=CARTESIAN_POINT('Ctrl Pts',(21.9131784297982,-6.18741639812789,1.20153308358827));
#69094=CARTESIAN_POINT('Ctrl Pts',(22.0137483397559,-6.0106643993911,-1.89729199457321));
#69095=CARTESIAN_POINT('Ctrl Pts',(22.1143182497138,-4.37633145795426,-4.5360253972944));
#69096=CARTESIAN_POINT('Ctrl Pts',(22.2148881596715,-1.68074190523514,-6.07477654591226));
#69097=CARTESIAN_POINT('Ctrl Pts',(22.3154580696294,1.42242611267267,-6.14039961148838));
#69098=CARTESIAN_POINT('Ctrl Pts',(22.4160279795871,4.18065702272256,-4.71698105711057));
#69099=CARTESIAN_POINT('Ctrl Pts',(22.516597889545,5.92508220359168,-2.14969865689606));
#69100=CARTESIAN_POINT('Ctrl Pts',(22.6171677995028,6.23268005057049,0.938883817093518));
#69101=CARTESIAN_POINT('Ctrl Pts',(22.7177377094606,5.0288583505557,3.79978777365601));
#69102=CARTESIAN_POINT('Ctrl Pts',(22.8183076194184,2.60554282951664,5.73924646607323));
#69103=CARTESIAN_POINT('Ctrl Pts',(22.9188775293762,-0.449614584754226,
6.28694283097562));
#69104=CARTESIAN_POINT('Ctrl Pts',(23.019447439334,-3.39574084926331,5.31006097134712));
#69105=CARTESIAN_POINT('Ctrl Pts',(23.1200173492918,-5.51840288097714,3.04549389721973));
#69106=CARTESIAN_POINT('Ctrl Pts',(23.2205872592497,-6.30285696445349,0.0423971746650429));
#69107=CARTESIAN_POINT('Ctrl Pts',(23.3211571692074,-5.55887365972991,-2.97098082624923));
#69108=CARTESIAN_POINT('Ctrl Pts',(23.4217270791652,-3.46686827775967,-5.26389853430357));
#69109=CARTESIAN_POINT('Ctrl Pts',(23.522296989123,-0.53415032281234,-6.28032537910409));
#69110=CARTESIAN_POINT('Ctrl Pts',(23.6228668990808,2.52809862560505,-5.77377872575607));
#69111=CARTESIAN_POINT('Ctrl Pts',(23.7234368090386,4.97728583357301,-3.86709570164651));
#69112=CARTESIAN_POINT('Ctrl Pts',(23.8240067189964,6.2194855114899,-1.02264529879458));
#69113=CARTESIAN_POINT('Ctrl Pts',(23.9245766289542,5.95346530678201,2.06979570869266));
#69114=CARTESIAN_POINT('Ctrl Pts',(24.025146538912,4.24373489009314,4.66031303856144));
#69115=CARTESIAN_POINT('Ctrl Pts',(24.1257164488698,1.50490241568538,6.12070846831016));
#69116=CARTESIAN_POINT('Ctrl Pts',(24.2262863588276,-1.59886759906292,6.09683736337508));
#69117=CARTESIAN_POINT('Ctrl Pts',(24.3268562687854,-4.31491359738955,4.59448844615397));
#69118=CARTESIAN_POINT('Ctrl Pts',(24.4274261787432,-5.98459676275057,1.97798003580794));
#69119=CARTESIAN_POINT('Ctrl Pts',(24.5279960887011,-6.20302036485712,-1.11818683051956));
#69120=CARTESIAN_POINT('Ctrl Pts',(24.6285659986588,-4.91721686822363,-3.94319435301338));
#69121=CARTESIAN_POINT('Ctrl Pts',(24.7291359086166,-2.4389925139272,-5.81198063931621));
#69122=CARTESIAN_POINT('Ctrl Pts',(24.8297058185745,0.630685425441865,-6.27136662370451));
#69123=CARTESIAN_POINT('Ctrl Pts',(24.9302757285322,3.54742269205338,-5.20995160041667));
#69124=CARTESIAN_POINT('Ctrl Pts',(25.03084563849,5.60391300956513,-2.88512779890356));
#69125=CARTESIAN_POINT('Ctrl Pts',(25.1314155484478,6.30145924626639,0.139337010242921));
#69126=CARTESIAN_POINT('Ctrl Pts',(25.2319854584056,5.47090704022486,3.13001271435079));
#69127=CARTESIAN_POINT('Ctrl Pts',(25.3325553683634,3.31366458644248,5.36166302963329));
#69128=CARTESIAN_POINT('Ctrl Pts',(25.4331252783213,0.352861322945316,6.29311467570303));
#69129=CARTESIAN_POINT('Ctrl Pts',(25.533695188279,-2.69351050761294,5.69849143020836));
#69130=CARTESIAN_POINT('Ctrl Pts',(25.6342650982368,-5.08670835872616,3.72198891831302));
#69131=CARTESIAN_POINT('Ctrl Pts',(25.7348350081946,-6.24638381163271,0.842907297721581));
#69132=CARTESIAN_POINT('Ctrl Pts',(25.8354049181524,-5.89131656728466,-2.24057861696856));
#69133=CARTESIAN_POINT('Ctrl Pts',(25.9359748281103,-4.10761012678435,-4.78072614579817));
#69134=CARTESIAN_POINT('Ctrl Pts',(26.036544738068,-1.3278117664874,-6.1615516996579));
#69135=CARTESIAN_POINT('Ctrl Pts',(26.1371146480258,1.77397980416429,-6.04820627039098));
#69136=CARTESIAN_POINT('Ctrl Pts',(26.2376845579837,4.44558279939882,-4.46817602702365));
#69137=CARTESIAN_POINT('Ctrl Pts',(26.3382544679414,6.03913579266429,-1.80461694343717));
#69138=CARTESIAN_POINT('Ctrl Pts',(26.4388243778993,6.16820355486997,1.2965601954668));
#69139=CARTESIAN_POINT('Ctrl Pts',(26.539394287857,4.80148726478621,4.0833226030863));
#69140=CARTESIAN_POINT('Ctrl Pts',(26.6399641978149,2.27041444624971,5.87988279449855));
#69141=CARTESIAN_POINT('Ctrl Pts',(26.7405341077726,-0.811231921064463,
6.25057646981665));
#69142=CARTESIAN_POINT('Ctrl Pts',(26.8411040177305,-3.69615524585221,5.10551073187969));
#69143=CARTESIAN_POINT('Ctrl Pts',(26.9416739276882,-5.68476410527724,2.72236303643196));
#69144=CARTESIAN_POINT('Ctrl Pts',(27.0422438376461,-6.29482256278049,-0.320955351862344));
#69145=CARTESIAN_POINT('Ctrl Pts',(27.1428137476039,-5.37839196757329,-3.2864423436176));
#69146=CARTESIAN_POINT('Ctrl Pts',(27.2433836575617,-3.15770595010358,-5.45496989610942));
#69147=CARTESIAN_POINT('Ctrl Pts',(27.3439535675194,-0.171278957977622,
-6.3006719445892));
#69148=CARTESIAN_POINT('Ctrl Pts',(27.4445234774773,2.8566830340161,-5.61846647030524));
#69149=CARTESIAN_POINT('Ctrl Pts',(27.5450933874351,5.19190184937557,-3.57378771350929));
#69150=CARTESIAN_POINT('Ctrl Pts',(27.6456632973929,6.26808893559948,-0.662468512606323));
#69151=CARTESIAN_POINT('Ctrl Pts',(27.7462332073507,5.82426985069124,2.4094987323318));
#69152=CARTESIAN_POINT('Ctrl Pts',(27.8468031173085,3.9680703406889,4.89716460884505));
#69153=CARTESIAN_POINT('Ctrl Pts',(27.9473730272663,1.14961718889825,6.19727228333315));
#69154=CARTESIAN_POINT('Ctrl Pts',(28.0479429372241,-1.94761714157679,5.99454676390265));
#69155=CARTESIAN_POINT('Ctrl Pts',(28.1485128471819,-4.57255599178413,4.33814881450354));
#69156=CARTESIAN_POINT('Ctrl Pts',(28.2490827571397,-6.08865395017118,1.62975351199023));
#69157=CARTESIAN_POINT('Ctrl Pts',(28.3496526670975,-6.12825856692962,-1.47385561424216));
#69158=CARTESIAN_POINT('Ctrl Pts',(28.4502225770553,-4.68176575658838,-4.22005602275799));
#69159=CARTESIAN_POINT('Ctrl Pts',(28.5507924870131,-2.09994878047266,-5.94289647850027));
#69160=CARTESIAN_POINT('Ctrl Pts',(28.6513623969709,0.991103967211534,-6.22458965402194));
#69161=CARTESIAN_POINT('Ctrl Pts',(28.7519323069287,3.84181485601765,-4.99682519674859));
#69162=CARTESIAN_POINT('Ctrl Pts',(28.8525022168865,5.7608889493839,-2.55733493067413));
#69163=CARTESIAN_POINT('Ctrl Pts',(28.9530721268443,6.28295243166296,0.502306854661562));
#69164=CARTESIAN_POINT('Ctrl Pts',(29.0536420368021,5.2814053578094,3.44013966014196));
#69165=CARTESIAN_POINT('Ctrl Pts',(29.1542119467599,2.99912203107227,5.5437415594088));
#69166=CARTESIAN_POINT('Ctrl Pts',(29.2547818567177,-0.0104458064696189,
6.30299090273076));
#69167=CARTESIAN_POINT('Ctrl Pts',(29.3553517666755,-3.01748054493469,5.53377037793584));
#69168=CARTESIAN_POINT('Ctrl Pts',(29.4559216766333,-5.2927788487869,3.42261530011971));
#69169=CARTESIAN_POINT('Ctrl Pts',(29.5564915865911,-6.28458283798409,0.481478958309967));
#69170=CARTESIAN_POINT('Ctrl Pts',(29.6570614965489,-5.7523808989193,-2.57641561641906));
#69171=CARTESIAN_POINT('Ctrl Pts',(29.7576314065067,-3.825231543681,-5.00953162201891));
#69172=CARTESIAN_POINT('Ctrl Pts',(29.8582013164645,-0.970466831969092,
-6.22784052162765));
#69173=CARTESIAN_POINT('Ctrl Pts',(29.9587712264223,2.11963525108966,-5.93590345584543));
#69174=CARTESIAN_POINT('Ctrl Pts',(30.0593411363801,4.69572761040196,-4.2045149118166));
#69175=CARTESIAN_POINT('Ctrl Pts',(30.1599110463379,6.13311006640879,-1.45353512103927));
#69176=CARTESIAN_POINT('Ctrl Pts',(30.2604809562957,6.08321861086852,1.64992568534537));
#69177=CARTESIAN_POINT('Ctrl Pts',(30.3610508662535,4.55815187880167,4.3532809333371));
#69178=CARTESIAN_POINT('Ctrl Pts',(30.4616207762113,1.92773723991327,6.00096930242366));
#69179=CARTESIAN_POINT('Ctrl Pts',(30.5621906861691,-1.1701520202026,6.19342778147895));
#69180=CARTESIAN_POINT('Ctrl Pts',(30.6627605961269,-3.98428042271975,4.88398535500585));
#69181=CARTESIAN_POINT('Ctrl Pts',(30.7633305060847,-5.83222425251021,2.39018068421849));
#69182=CARTESIAN_POINT('Ctrl Pts',(30.8639004160425,-6.26585872161285,-0.683240744955771));
#69183=CARTESIAN_POINT('Ctrl Pts',(30.9644703260003,-5.18002784455525,-3.5909768816315));
#69184=CARTESIAN_POINT('Ctrl Pts',(31.0650402359581,-2.83804467430954,-5.62790421572743));
#69185=CARTESIAN_POINT('Ctrl Pts',(31.1656101459159,0.192161886385956,-6.30006962217086));
#69186=CARTESIAN_POINT('Ctrl Pts',(31.2661800558737,3.17576935505136,-5.44447356851846));
#69187=CARTESIAN_POINT('Ctrl Pts',(31.3667499658315,5.38925548891016,-3.26859736125931));
#69188=CARTESIAN_POINT('Ctrl Pts',(31.4673198757894,6.2958518059339,-0.300089107597089));
#69189=CARTESIAN_POINT('Ctrl Pts',(31.5678897857471,5.67570947966844,2.74119049633208));
#69190=CARTESIAN_POINT('Ctrl Pts',(31.668459695705,3.67921249039688,5.11773376459612));
#69191=CARTESIAN_POINT('Ctrl Pts',(31.7690296056627,0.790509639375698,6.25323100043758));
#69192=CARTESIAN_POINT('Ctrl Pts',(31.8695995156205,-2.28989111870072,5.87232510163352));
#69193=CARTESIAN_POINT('Ctrl Pts',(31.9701694255784,-4.81499525169616,4.06738542074917));
#69194=CARTESIAN_POINT('Ctrl Pts',(32.0707393355361,-6.17246718104128,1.27610827665518));
#69195=CARTESIAN_POINT('Ctrl Pts',(32.171309245494,-6.03312113242065,-1.8246240260171));
#69196=CARTESIAN_POINT('Ctrl Pts',(32.2718791554517,-4.43074840267172,-4.48288657306889));
#69197=CARTESIAN_POINT('Ctrl Pts',(32.3724490654096,-1.75392299939023,-6.05405298514883));
#69198=CARTESIAN_POINT('Ctrl Pts',(32.4730189753674,1.34822722141622,-6.15711675983263));
#69199=CARTESIAN_POINT('Ctrl Pts',(32.5735888853251,4.12343350162191,-4.76708502047968));
#69200=CARTESIAN_POINT('Ctrl Pts',(32.674158795283,5.89871070725407,-2.22103926730387));
#69201=CARTESIAN_POINT('Ctrl Pts',(32.7747287052407,6.24355564415645,0.863606596258802));
#69202=CARTESIAN_POINT('Ctrl Pts',(32.8752986151986,5.07434371198264,3.73882860364601));
#69203=CARTESIAN_POINT('Ctrl Pts',(32.9758685251564,2.67460779779369,5.70738789313997));
#69204=CARTESIAN_POINT('Ctrl Pts',(33.0764384351141,-0.37371820498118,6.2919105316307));
#69205=CARTESIAN_POINT('Ctrl Pts',(33.177008345072,-3.33141786475548,5.35065028245797));
#69206=CARTESIAN_POINT('Ctrl Pts',(33.2775782550298,-5.4812515601066,3.11186194578239));
#69207=CARTESIAN_POINT('Ctrl Pts',(33.3781481649876,-6.30188647055037,0.118449766034587));
#69208=CARTESIAN_POINT('Ctrl Pts',(33.4787180749453,-5.59431933673029,-2.9036863800116));
#69209=CARTESIAN_POINT('Ctrl Pts',(33.5792879849032,-3.53013457950368,-5.22168107848151));
#69210=CARTESIAN_POINT('Ctrl Pts',(33.679857894861,-0.609895225588482,-6.2734226103925));
#69211=CARTESIAN_POINT('Ctrl Pts',(33.7804278048187,2.45824319551665,-5.8038645596254));
#69212=CARTESIAN_POINT('Ctrl Pts',(33.8809977147766,4.93025975783522,-3.92687434928215));
#69213=CARTESIAN_POINT('Ctrl Pts',(33.9815676247343,6.20669257298772,-1.09762048960406));
#69214=CARTESIAN_POINT('Ctrl Pts',(34.0821375346922,5.97800778208965,1.99780539393979));
#69215=CARTESIAN_POINT('Ctrl Pts',(34.1827074446499,4.29966125007543,4.60876518922143));
#69216=CARTESIAN_POINT('Ctrl Pts',(34.2832773546078,1.57865056618961,6.10210339347416));
#69217=CARTESIAN_POINT('Ctrl Pts',(34.3838472645656,-1.52518152104951,6.11568677767498));
#69218=CARTESIAN_POINT('Ctrl Pts',(34.4844171745234,-4.25915840235411,4.64622138284819));
#69219=CARTESIAN_POINT('Ctrl Pts',(34.5849870844812,-5.96029303749356,2.05005130228134));
#69220=CARTESIAN_POINT('Ctrl Pts',(34.685556994439,-6.21606174183198,-1.04325445434579));
#69221=CARTESIAN_POINT('Ctrl Pts',(34.7861269043968,-4.96444082474036,-3.88357190385742));
#69222=CARTESIAN_POINT('Ctrl Pts',(34.8866968143546,-2.50894728118225,-5.7821265097737));
#69223=CARTESIAN_POINT('Ctrl Pts',(34.9872667243123,0.554963818288801,-6.27852041449017));
#69224=CARTESIAN_POINT('Ctrl Pts',(35.0878366342702,3.48429666955357,-5.25237852342321));
#69225=CARTESIAN_POINT('Ctrl Pts',(35.188406544228,5.56869057783411,-2.95253936182418));
#69226=CARTESIAN_POINT('Ctrl Pts',(35.2889764541858,6.30268181467842,0.0632880533866562));
#69227=CARTESIAN_POINT('Ctrl Pts',(35.3895463641436,5.50827813699247,3.06376817013139));
#69228=CARTESIAN_POINT('Ctrl Pts',(35.4901162741014,3.37812175276964,5.32128714299879));
#69229=CARTESIAN_POINT('Ctrl Pts',(35.5906861840592,0.428773751484242,6.28839856440554));
#69230=CARTESIAN_POINT('Ctrl Pts',(35.691256094017,-2.62455151543532,5.73057874717778));
#69231=CARTESIAN_POINT('Ctrl Pts',(35.7918260039748,-5.04142529915106,3.78309851680594));
#69232=CARTESIAN_POINT('Ctrl Pts',(35.8923959139326,-6.23575778762611,0.918220152708348));
#69233=CARTESIAN_POINT('Ctrl Pts',(35.9929658238904,-5.91792438052098,-2.16932580799077));
#69234=CARTESIAN_POINT('Ctrl Pts',(36.0935357338482,-4.16499940545854,-4.73081212767));
#69235=CARTESIAN_POINT('Ctrl Pts',(36.194105643806,-1.40206565992333,-6.145080578808));
#69236=CARTESIAN_POINT('Ctrl Pts',(36.2946755537638,1.70086780120493,-6.06917227944665));
#69237=CARTESIAN_POINT('Ctrl Pts',(36.3952454637217,4.39134228469678,-4.52149492683709));
#69238=CARTESIAN_POINT('Ctrl Pts',(36.4958153736794,6.01692004434307,-1.87735894670202));
#69239=CARTESIAN_POINT('Ctrl Pts',(36.5963852836372,6.18339987277349,1.2220349619239));
#69240=CARTESIAN_POINT('Ctrl Pts',(36.696955193595,4.85041055490425,4.02508644424602));
#69241=CARTESIAN_POINT('Ctrl Pts',(36.7975251035529,2.34120085284323,5.85205792874828));
#69242=CARTESIAN_POINT('Ctrl Pts',(36.8980950135106,-0.735748040659395,
6.25991040314837));
#69243=CARTESIAN_POINT('Ctrl Pts',(36.9986649234685,-3.63427866765513,5.14973999349544));
#69244=CARTESIAN_POINT('Ctrl Pts',(37.0992348334262,-5.65149984623585,2.79076206846371));
#69245=CARTESIAN_POINT('Ctrl Pts',(37.199804743384,-6.29823717707749,-0.244973255802475));
#69246=CARTESIAN_POINT('Ctrl Pts',(37.3003746533419,-5.41765741418102,-3.22130277641656));
#69247=CARTESIAN_POINT('Ctrl Pts',(37.4009445632996,-3.2233003920205,-5.41646914673941));
#69248=CARTESIAN_POINT('Ctrl Pts',(37.5015144732574,-0.247295799504477,
-6.29814641162992));
#69249=CARTESIAN_POINT('Ctrl Pts',(37.6020843832152,2.78867781151207,-5.65252859332527));
#69250=CARTESIAN_POINT('Ctrl Pts',(37.7026542931731,5.14839945381081,-3.63617745699796));
#69251=CARTESIAN_POINT('Ctrl Pts',(37.8032242031308,6.25963866045032,-0.738056417474464));
#69252=CARTESIAN_POINT('Ctrl Pts',(37.9037941130887,5.8529208804071,2.33904266794645));
#69253=CARTESIAN_POINT('Ctrl Pts',(38.0043640230464,4.02687482522731,4.84892591990536));
#69254=CARTESIAN_POINT('Ctrl Pts',(38.1049339330043,1.22431509137923,6.18294881038171));
#69255=CARTESIAN_POINT('Ctrl Pts',(38.205503842962,-1.87513999820277,6.01761193680014));
#69256=CARTESIAN_POINT('Ctrl Pts',(38.3060737529198,-4.51987525239489,4.39300934867749));
#69257=CARTESIAN_POINT('Ctrl Pts',(38.4066436628776,-6.06854464871948,1.70310577512895));
#69258=CARTESIAN_POINT('Ctrl Pts',(38.5072135728354,-6.14559719170687,-1.39979948280604));
#69259=CARTESIAN_POINT('Ctrl Pts',(38.6077834827933,-4.73234770601166,-4.16325457114813));
#69260=CARTESIAN_POINT('Ctrl Pts',(38.7083533927511,-2.17150797534923,-5.9171240098357));
#69261=CARTESIAN_POINT('Ctrl Pts',(38.8089233027088,0.915920570039041,-6.23609596976817));
#69262=CARTESIAN_POINT('Ctrl Pts',(38.9094932126667,3.78123916564354,-5.04282002524212));
#69263=CARTESIAN_POINT('Ctrl Pts',(39.0100631226244,5.72961051857859,-2.62666456559893));
#69264=CARTESIAN_POINT('Ctrl Pts',(39.1106330325823,6.28855625297138,0.426454790093798));
#69265=CARTESIAN_POINT('Ctrl Pts',(39.21120294254,5.3225325093882,3.3761592262933));
#69266=CARTESIAN_POINT('Ctrl Pts',(39.3117728524979,3.06579921406697,5.50714795641135));
#69267=CARTESIAN_POINT('Ctrl Pts',(39.4123427624557,0.0656122484624124,
6.30265804781056));
#69268=CARTESIAN_POINT('Ctrl Pts',(39.5129126724135,-2.95048563091339,5.5697789881245));
#69269=CARTESIAN_POINT('Ctrl Pts',(39.6134825823713,-5.25109328465533,3.48623331844373));
#69270=CARTESIAN_POINT('Ctrl Pts',(39.7140524923291,-6.27831533716003,0.557279070090006));
#69271=CARTESIAN_POINT('Ctrl Pts',(39.8146224022869,-5.78305132495739,-2.50681487303874));
#69272=CARTESIAN_POINT('Ctrl Pts',(39.9151923122446,-3.88540234466897,-4.96300836739375));
#69273=CARTESIAN_POINT('Ctrl Pts',(40.0157622222025,-1.04554664046408,-6.21567660495573));
#69274=CARTESIAN_POINT('Ctrl Pts',(40.1163321321602,2.04785322401683,-5.96104861644857));
#69275=CARTESIAN_POINT('Ctrl Pts',(40.2169020421181,4.64465044452441,-4.26087146989424));
#69276=CARTESIAN_POINT('Ctrl Pts',(40.3174719520758,6.1151239304831,-1.52743665977094));
#69277=CARTESIAN_POINT('Ctrl Pts',(40.4180418620337,6.10268512737375,1.57640022548551));
#69278=CARTESIAN_POINT('Ctrl Pts',(40.5186117719914,4.61035043424262,4.2979614130723));
#69279=CARTESIAN_POINT('Ctrl Pts',(40.6191816819493,2.00000972952951,5.97727065779749));
#69280=CARTESIAN_POINT('Ctrl Pts',(40.7197515919071,-1.0953316129288,6.20709691341278));
#69281=CARTESIAN_POINT('Ctrl Pts',(40.8203215018649,-3.9250559821447,4.93170751077247));
#69282=CARTESIAN_POINT('Ctrl Pts',(40.9208914118227,-5.80295765449124,2.46038328212514));
#69283=CARTESIAN_POINT('Ctrl Pts',(41.0214613217805,-6.27364709097608,-0.607581774469037));
#69284=CARTESIAN_POINT('Ctrl Pts',(41.1220312317383,-5.22298250843454,-3.52820877377832));
#69285=CARTESIAN_POINT('Ctrl Pts',(41.2226011416961,-2.90574916369074,-5.59324818262967));
#69286=CARTESIAN_POINT('Ctrl Pts',(41.323171051654,0.116125851895876,-6.30192972202175));
#69287=CARTESIAN_POINT('Ctrl Pts',(41.4237409616116,3.10984044836217,-5.48239872870535));
#69288=CARTESIAN_POINT('Ctrl Pts',(41.5243108715695,5.34942141314046,-3.333390763084));
#69289=CARTESIAN_POINT('Ctrl Pts',(41.6248807815273,6.29177229016759,-0.376038406893155));
#69290=CARTESIAN_POINT('Ctrl Pts',(41.7254506914851,5.70837380296712,2.67250293926466));
#69291=CARTESIAN_POINT('Ctrl Pts',(41.8260206014429,3.74069958247899,5.07296462321797));
#69292=CARTESIAN_POINT('Ctrl Pts',(41.9265905114007,0.865908933341185,6.24323675299435));
#69293=CARTESIAN_POINT('Ctrl Pts',(42.0271604213585,-2.21886388673261,5.89952934452685));
#69294=CARTESIAN_POINT('Ctrl Pts',(42.1277303313163,-4.76556412433542,4.12519114849563));
#69295=CARTESIAN_POINT('Ctrl Pts',(42.2283002412741,-6.15661916412113,1.35049765003709));
#69296=CARTESIAN_POINT('Ctrl Pts',(42.3288701512319,-6.05469935640187,-1.75169036600829));
#69297=CARTESIAN_POINT('Ctrl Pts',(42.4294400611897,-4.484520166814,-4.42909497620203));
#69298=CARTESIAN_POINT('Ctrl Pts',(42.5300099711475,-1.82684869717725,-6.03244786735878));
#69299=CARTESIAN_POINT('Ctrl Pts',(42.6305798811053,1.27383200892127,-6.17293734358508));
#69300=CARTESIAN_POINT('Ctrl Pts',(42.7311497910632,4.06560954940742,-4.81649482783347));
#69301=CARTESIAN_POINT('Ctrl Pts',(42.8317197010208,5.87148027395556,-2.29205646250919));
#69302=CARTESIAN_POINT('Ctrl Pts',(42.9322896109788,6.25352208640813,0.788203621905611));
#69303=CARTESIAN_POINT('Ctrl Pts',(43.0328595209364,5.11909017611791,3.67732500651664));
#69304=CARTESIAN_POINT('Ctrl Pts',(43.1334294308944,2.74328330477867,5.67469824259427));
#69305=CARTESIAN_POINT('Ctrl Pts',(43.2339993408521,-0.297767406472493,
6.29596203978567));
#69306=CARTESIAN_POINT('Ctrl Pts',(43.3345692508099,-3.26660977798073,5.39046046207373));
#69307=CARTESIAN_POINT('Ctrl Pts',(43.4351391607677,-5.44330209031999,3.17777686257191));
#69308=CARTESIAN_POINT('Ctrl Pts',(43.5357090707255,-6.29999833150725,0.1944851094179));
#69309=CARTESIAN_POINT('Ctrl Pts',(43.6362789806833,-5.62895040052328,-2.83596911535165));
#69310=CARTESIAN_POINT('Ctrl Pts',(43.7368488906411,-3.59288684297432,-5.17870327093198));
#69311=CARTESIAN_POINT('Ctrl Pts',(43.8374188005989,-0.685551318864139,
-6.26560634128757));
#69312=CARTESIAN_POINT('Ctrl Pts',(43.9379887105567,2.38802980992837,-5.83310526749458));
#69313=CARTESIAN_POINT('Ctrl Pts',(44.0385586205146,4.88251576549779,-3.98608118763844));
#69314=CARTESIAN_POINT('Ctrl Pts',(44.1391285304723,6.19299585094358,-1.17243585111297));
#69315=CARTESIAN_POINT('Ctrl Pts',(44.2396984404301,6.001679773644,1.92552417004097));
#69316=CARTESIAN_POINT('Ctrl Pts',(44.3402683503879,4.35496151765379,4.55654623750647));
#69317=CARTESIAN_POINT('Ctrl Pts',(44.4408382603457,1.65216884250822,6.08260976478227));
#69318=CARTESIAN_POINT('Ctrl Pts',(44.5414081703036,-1.4512733547112,6.13364566018324));
#69319=CARTESIAN_POINT('Ctrl Pts',(44.6419780802613,-4.20278301271083,4.69727776300792));
#69320=CARTESIAN_POINT('Ctrl Pts',(44.7425479902192,-5.93512140800427,2.12182405185462));
#69321=CARTESIAN_POINT('Ctrl Pts',(44.8431179001769,-6.22819797097945,-0.968170165346456));
#69322=CARTESIAN_POINT('Ctrl Pts',(44.9436878101347,-5.01094188740351,-3.82338395087974));
#69323=CARTESIAN_POINT('Ctrl Pts',(45.0442577200926,-2.57853670969462,-5.75143041960318));
#69324=CARTESIAN_POINT('Ctrl Pts',(45.1448276300503,0.479161400436802,-6.28475996256904));
#69325=CARTESIAN_POINT('Ctrl Pts',(45.2453975400082,3.42066328343813,-5.29404062471357));
#69326=CARTESIAN_POINT('Ctrl Pts',(45.3459674499659,5.53265726481079,-3.0195209926271));
#69327=CARTESIAN_POINT('Ctrl Pts',(45.4465373599238,6.30298662213694,-0.0127701191187959));
#69328=CARTESIAN_POINT('Ctrl Pts',(45.5471072698816,5.5448471493865,2.99707749728301));
#69329=CARTESIAN_POINT('Ctrl Pts',(45.6476771798394,3.4420870160732,5.28013640056389));
#69330=CARTESIAN_POINT('Ctrl Pts',(45.7482470897972,0.504623744409411,6.28276677200082));
#69331=CARTESIAN_POINT('Ctrl Pts',(45.8488169997549,-2.55521035087901,5.76183160961339));
#69332=CARTESIAN_POINT('Ctrl Pts',(45.9493869097128,-4.99540813567764,3.84365724184467));
#69333=CARTESIAN_POINT('Ctrl Pts',(46.0499568196706,-6.22422374776511,0.993399301658971));
#69334=CARTESIAN_POINT('Ctrl Pts',(46.1505267296283,-5.9436704590098,-2.09775711403243));
#69335=CARTESIAN_POINT('Ctrl Pts',(46.2510966395862,-4.22178220042662,-4.68020923538044));
#69336=CARTESIAN_POINT('Ctrl Pts',(46.3516665495439,-1.47611539247118,-6.12771464600704));
#69337=CARTESIAN_POINT('Ctrl Pts',(46.4522364595018,1.62750812747607,-6.08925452988943));
#69338=CARTESIAN_POINT('Ctrl Pts',(46.5528063694595,4.33646232751603,-4.57415543207854));
#69339=CARTESIAN_POINT('Ctrl Pts',(46.6533762794174,5.99382814608451,-1.94982757955281));
#69340=CARTESIAN_POINT('Ctrl Pts',(46.7539461893752,6.19769579888664,1.147331782547));
#69341=CARTESIAN_POINT('Ctrl Pts',(46.8545160993329,4.89862755561304,3.96626417503526));
#69342=CARTESIAN_POINT('Ctrl Pts',(46.9550860092908,2.41164634698237,5.82338091935141));
#69343=CARTESIAN_POINT('Ctrl Pts',(47.0556559192485,-0.660157024777184,
6.26833280365816));
#69344=CARTESIAN_POINT('Ctrl Pts',(47.1562258292064,-3.57187288631038,5.19321937903841));
#69345=CARTESIAN_POINT('Ctrl Pts',(47.2567957391642,-5.61741264768391,2.85875472547407));
#69346=CARTESIAN_POINT('Ctrl Pts',(47.357365649122,-6.30073467762402,-0.168955488119712));
#69347=CARTESIAN_POINT('Ctrl Pts',(47.4579355590798,-5.45613397209338,-3.15569414128618));
#69348=CARTESIAN_POINT('Ctrl Pts',(47.5585054690376,-3.28842547512672,-5.37717968170277));
#69349=CARTESIAN_POINT('Ctrl Pts',(47.6590753789954,-0.323276631212769,
-6.29470377813694));
#69350=CARTESIAN_POINT('Ctrl Pts',(47.7596452889532,2.72026651748448,-5.68576762703438));
#69351=CARTESIAN_POINT('Ctrl Pts',(47.8602151989109,5.10414737737517,-3.69803772084787));
#69352=CARTESIAN_POINT('Ctrl Pts',(47.9607851088689,6.25027689204883,-0.813536850732643));
#69353=CARTESIAN_POINT('Ctrl Pts',(48.0613550188265,5.88071964081822,2.26824600536938));
#69354=CARTESIAN_POINT('Ctrl Pts',(48.1619249287844,4.08509293898134,4.79998115774056));
#69355=CARTESIAN_POINT('Ctrl Pts',(48.2624948387422,1.29883471600662,6.16772501132107));
#69356=CARTESIAN_POINT('Ctrl Pts',(48.3630647487,-1.80238980752552,6.03980085901079));
#69357=CARTESIAN_POINT('Ctrl Pts',(48.4636346586578,-4.46653635428158,4.4472301976242));
#69358=CARTESIAN_POINT('Ctrl Pts',(48.5642045686156,-6.04755168004692,1.77621004161703));
#69359=CARTESIAN_POINT('Ctrl Pts',(48.6647744785734,-6.16204092930681,-1.32553952046974));
#69360=CARTESIAN_POINT('Ctrl Pts',(48.7653443885312,-4.78224055767135,-4.10584688990502));
#69361=CARTESIAN_POINT('Ctrl Pts',(48.8659142984891,-2.24275096749041,-5.89048992296909));
#69362=CARTESIAN_POINT('Ctrl Pts',(48.9664842084468,0.840603801682614,-6.2466942204158));
#69363=CARTESIAN_POINT('Ctrl Pts',(49.0670541184046,3.72011287256346,-5.08808054674523));
#69364=CARTESIAN_POINT('Ctrl Pts',(49.1676240283624,5.69749777422752,-2.69561172045457));
#69365=CARTESIAN_POINT('Ctrl Pts',(49.2681939383202,6.29324437021086,0.350540627586432));
#69366=CARTESIAN_POINT('Ctrl Pts',(49.3687638482779,5.36288462382333,3.31168717519316));
#69367=CARTESIAN_POINT('Ctrl Pts',(49.4693337582359,3.13202997268351,5.46975243361084));
#69368=CARTESIAN_POINT('Ctrl Pts',(49.5699036681935,0.141660749309164,6.30140743539763));
#69369=CARTESIAN_POINT('Ctrl Pts',(49.6704735781515,-2.88306108382702,5.60497655853276));
#69370=CARTESIAN_POINT('Ctrl Pts',(49.7710434881091,-5.20864308595681,3.54934369114824));
#69371=CARTESIAN_POINT('Ctrl Pts',(49.8716133980671,-6.27113362349142,0.632998034037112));
#69372=CARTESIAN_POINT('Ctrl Pts',(49.9721833080248,-5.81287965570103,-2.43684910142515));
#69373=CARTESIAN_POINT('Ctrl Pts',(50.0727532179827,-3.94500737529666,-4.91576242750141));
#69374=CARTESIAN_POINT('Ctrl Pts',(50.1733231279404,-1.12047420235831,-6.20260759653784));
#69375=CARTESIAN_POINT('Ctrl Pts',(50.2738930378982,1.97577300011552,-5.98532576279636));
#69376=CARTESIAN_POINT('Ctrl Pts',(50.374462947856,4.59289695086342,-4.3166075839169));
#69377=CARTESIAN_POINT('Ctrl Pts',(50.4750328578138,6.09624734472443,-1.60111578179717));
#69378=CARTESIAN_POINT('Ctrl Pts',(50.5756027677717,6.12126300531428,1.50264521912207));
#69379=CARTESIAN_POINT('Ctrl Pts',(50.6761726777294,4.66187765647411,4.24201604792428));
#69380=CARTESIAN_POINT('Ctrl Pts',(50.7767425876873,2.07199098901695,5.95270163675385));
#69381=CARTESIAN_POINT('Ctrl Pts',(50.877312497645,-1.02035170964748,6.21986220292691));
#69382=CARTESIAN_POINT('Ctrl Pts',(50.9778824076029,-3.86525999707042,4.97871153912603));
#69383=CARTESIAN_POINT('Ctrl Pts',(51.0784523175607,-5.77284606253051,2.53022761290473));
#69384=CARTESIAN_POINT('Ctrl Pts',(51.1790222275184,-6.28052192725839,-0.531834331353529));
#69385=CARTESIAN_POINT('Ctrl Pts',(51.2795921374763,-5.26517663107943,-3.4649269080768));
#69386=CARTESIAN_POINT('Ctrl Pts',(51.380162047434,-2.97303053427876,-5.55777769229983));
#69387=CARTESIAN_POINT('Ctrl Pts',(51.4807319573919,0.0400729078145031,
-6.30287217043457));
#69388=CARTESIAN_POINT('Ctrl Pts',(51.5813018673496,3.04345870425864,-5.51952557293213));
#69389=CARTESIAN_POINT('Ctrl Pts',(51.6818717773075,5.30880838481668,-3.39769877535954));
#69390=CARTESIAN_POINT('Ctrl Pts',(51.7824416872652,6.28677660203117,-0.451932949598734));
#69391=CARTESIAN_POINT('Ctrl Pts',(51.8830115972231,5.74020690509067,2.6034262274029));
#69392=CARTESIAN_POINT('Ctrl Pts',(51.9835815071808,3.80164197500026,5.02745678536328));
#69393=CARTESIAN_POINT('Ctrl Pts',(52.0841514171387,0.941182138535105,6.2323334006519));
#69394=CARTESIAN_POINT('Ctrl Pts',(52.1847213270964,-2.14751355632885,5.92587453125411));
#69395=CARTESIAN_POINT('Ctrl Pts',(52.2852912370543,-4.71543906242315,4.18239618918938));
#69396=CARTESIAN_POINT('Ctrl Pts',(52.3858611470121,-6.13987465506746,1.42469037157386));
#69397=CARTESIAN_POINT('Ctrl Pts',(52.4864310569698,-6.07539592923327,-1.6785016347362));
#69398=CARTESIAN_POINT('Ctrl Pts',(52.5870009669278,-4.53763892044433,-4.37465843952072));
#69399=CARTESIAN_POINT('Ctrl Pts',(52.6875708768854,-1.89950837955927,-6.00996433856127));
#69400=CARTESIAN_POINT('Ctrl Pts',(52.7881407868433,1.19925130818209,-6.18785905903403));
#69401=CARTESIAN_POINT('Ctrl Pts',(52.888710696801,4.00719358610876,-4.8652032844097));
#69402=CARTESIAN_POINT('Ctrl Pts',(52.9892806067589,5.84339486877529,-2.36273990135964));
#69403=CARTESIAN_POINT('Ctrl Pts',(53.0898505167167,6.26257792619167,0.712685873732938));
#69404=CARTESIAN_POINT('Ctrl Pts',(53.1904204266745,5.1630912269926,3.61528593818628));
#69405=CARTESIAN_POINT('Ctrl Pts',(53.2909903366323,2.81155935080371,5.64118227430033));
#69406=CARTESIAN_POINT('Ctrl Pts',(53.3915602465901,-0.221773249677871,
6.29909676590961));
#69407=CARTESIAN_POINT('Ctrl Pts',(53.4921301565479,-3.20132602411989,5.42948571242569));
#69408=CARTESIAN_POINT('Ctrl Pts',(53.5927000665056,-5.40456000114086,3.24322905106435));
#69409=CARTESIAN_POINT('Ctrl Pts',(53.6932699764635,-6.2971928153451,0.27049212977903));
#69410=CARTESIAN_POINT('Ctrl Pts',(53.7938398864213,-5.66276182186868,-2.76783888661719));
#69411=CARTESIAN_POINT('Ctrl Pts',(53.8944097963791,-3.65511590404492,-5.13497138208737));
#69412=CARTESIAN_POINT('Ctrl Pts',(53.9949797063369,-0.761107637875617,
-6.25687768598526));
#69413=CARTESIAN_POINT('Ctrl Pts',(54.0955496162947,2.31746879438081,-5.86149663839339));
#69414=CARTESIAN_POINT('Ctrl Pts',(54.1961195262525,4.83406061022007,-4.04470750357852));
#69415=CARTESIAN_POINT('Ctrl Pts',(54.2966894362103,6.17839772833774,-1.24708066871483));
#69416=CARTESIAN_POINT('Ctrl Pts',(54.3972593461681,6.0244770741368,1.85296291360496));
#69417=CARTESIAN_POINT('Ctrl Pts',(54.4978292561259,4.40962912818019,4.50366309955075));
#69418=CARTESIAN_POINT('Ctrl Pts',(54.5983991660837,1.725443627756,6.06223176652131));
#69419=CARTESIAN_POINT('Ctrl Pts',(54.6989690760415,-1.37714816454321,6.15070876238158));
#69420=CARTESIAN_POINT('Ctrl Pts',(54.7995389859993,-4.14580678716376,4.74765530553779));
#69421=CARTESIAN_POINT('Ctrl Pts',(54.9001088959571,-5.90906371955852,2.19327774747913));
#69422=CARTESIAN_POINT('Ctrl Pts',(55.0006788059149,-6.23947000165856,-0.892925146540183));
#69423=CARTESIAN_POINT('Ctrl Pts',(55.1012487158727,-5.05662950647384,-3.76267805248054));
#69424=CARTESIAN_POINT('Ctrl Pts',(55.2018186258305,-2.64791663301169,-5.71981935650092));
#69425=CARTESIAN_POINT('Ctrl Pts',(55.3023885357883,0.403635775592951,-6.29025284183206));
#69426=CARTESIAN_POINT('Ctrl Pts',(55.3694351424269,2.37161821088939,-5.65302266761336));
#69427=CARTESIAN_POINT('Ctrl Pts',(55.4029584457461,3.22059861141916,-5.11887719052968));
#69428=CARTESIAN_POINT('Ctrl Pts',(18.7300198469368,3.59837006536955,-4.56511341115994));
#69429=CARTESIAN_POINT('Ctrl Pts',(18.7635431502561,4.3555071616532,-3.96831345959956));
#69430=CARTESIAN_POINT('Ctrl Pts',(18.8305897568946,5.56638086023038,-2.39135841227044));
#69431=CARTESIAN_POINT('Ctrl Pts',(18.9311596668524,6.03258243308101,0.555802844140216));
#69432=CARTESIAN_POINT('Ctrl Pts',(19.0317295768102,5.03596644794646,3.36741791535919));
#69433=CARTESIAN_POINT('Ctrl Pts',(19.1322994867681,2.81809776660485,5.36281263415837));
#69434=CARTESIAN_POINT('Ctrl Pts',(19.2328693967258,-0.0831396853048251,
6.05753936909375));
#69435=CARTESIAN_POINT('Ctrl Pts',(19.3334393066836,-2.96422474143937,5.28341525958718));
#69436=CARTESIAN_POINT('Ctrl Pts',(19.4340092166414,-5.12648330210607,3.22801781931831));
#69437=CARTESIAN_POINT('Ctrl Pts',(19.5345791265992,-6.04557639845419,0.389854222115132));
#69438=CARTESIAN_POINT('Ctrl Pts',(19.635149036557,-5.49862123510697,-2.54286166069909));
#69439=CARTESIAN_POINT('Ctrl Pts',(19.7357189465149,-3.61825576233384,-4.85892915066333));
#69440=CARTESIAN_POINT('Ctrl Pts',(19.8362888564726,-0.860466071849947,
-5.99671389188823));
#69441=CARTESIAN_POINT('Ctrl Pts',(19.9368587664304,2.10598574190594,-5.68029894535209));
#69442=CARTESIAN_POINT('Ctrl Pts',(20.0374286763883,4.56173790710718,-3.98641727896731));
#69443=CARTESIAN_POINT('Ctrl Pts',(20.137998586346,5.91127251533532,-1.32583240199046));
#69444=CARTESIAN_POINT('Ctrl Pts',(20.2385684963039,5.82732864833066,1.65626546014106));
#69445=CARTESIAN_POINT('Ctrl Pts',(20.3391384062616,4.33026258963291,4.23672049200133));
#69446=CARTESIAN_POINT('Ctrl Pts',(20.4397083162195,1.7831115860847,5.78977439131494));
#69447=CARTESIAN_POINT('Ctrl Pts',(20.5402782261772,-1.19644244495693,5.93881301556665));
#69448=CARTESIAN_POINT('Ctrl Pts',(20.6408481361351,-3.88586021158666,4.64769458009025));
#69449=CARTESIAN_POINT('Ctrl Pts',(20.7414180460928,-5.63296022270332,2.22951421786122));
#69450=CARTESIAN_POINT('Ctrl Pts',(20.8419879560507,-6.01407222845162,-0.729321427083321));
#69451=CARTESIAN_POINT('Ctrl Pts',(20.9425578660084,-4.93677689607866,-3.51129725167865));
#69452=CARTESIAN_POINT('Ctrl Pts',(21.0431277759663,-2.66231741602744,-5.44178651644161));
#69453=CARTESIAN_POINT('Ctrl Pts',(21.1436976859241,0.257751745561017,-6.05264723486437));
#69454=CARTESIAN_POINT('Ctrl Pts',(21.2442675958819,3.11531633075669,-5.19574620940539));
#69455=CARTESIAN_POINT('Ctrl Pts',(21.3448375058397,5.2174193874844,-3.07888120066958));
#69456=CARTESIAN_POINT('Ctrl Pts',(21.4454074157975,6.05430273405806,-0.215390151233893));
#69457=CARTESIAN_POINT('Ctrl Pts',(21.5459773257553,5.42302287933666,2.70033282449942));
#69458=CARTESIAN_POINT('Ctrl Pts',(21.6465472357131,3.47666464467147,4.96122741479645));
#69459=CARTESIAN_POINT('Ctrl Pts',(21.7471171456709,0.687218226485192,6.01902862778194));
#69460=CARTESIAN_POINT('Ctrl Pts',(21.8476870556287,-2.26887802004612,5.61722057987778));
#69461=CARTESIAN_POINT('Ctrl Pts',(21.9482569655865,-4.67477329983176,3.85324137682038));
#69462=CARTESIAN_POINT('Ctrl Pts',(22.0488268755443,-5.947040078587,1.15485445686342));
#69463=CARTESIAN_POINT('Ctrl Pts',(22.1493967855021,-5.77715475766761,-1.82358367475042));
#69464=CARTESIAN_POINT('Ctrl Pts',(22.2499666954599,-4.20631438115428,-4.35980433503075));
#69465=CARTESIAN_POINT('Ctrl Pts',(22.3505366054177,-1.61544638812712,-5.83877619711054));
#69466=CARTESIAN_POINT('Ctrl Pts',(22.4511065153755,1.36716596339831,-5.90184985757714));
#69467=CARTESIAN_POINT('Ctrl Pts',(22.5516764253333,4.01824174569531,-4.53373000806282));
#69468=CARTESIAN_POINT('Ctrl Pts',(22.6522463352911,5.69489736367894,-2.06618453435812));
#69469=CARTESIAN_POINT('Ctrl Pts',(22.7528162452489,5.99054527330138,0.902408910297553));
#69470=CARTESIAN_POINT('Ctrl Pts',(22.8533861552067,4.83349111098141,3.65216897102551));
#69471=CARTESIAN_POINT('Ctrl Pts',(22.9539560651645,2.50431951505622,5.51628120017159));
#69472=CARTESIAN_POINT('Ctrl Pts',(23.0545259751223,-0.432147407480051,
6.0426999868491));
#69473=CARTESIAN_POINT('Ctrl Pts',(23.1550958850801,-3.26381895570729,5.10376922844516));
#69474=CARTESIAN_POINT('Ctrl Pts',(23.2556657950379,-5.30401721676446,2.92717882561419));
#69475=CARTESIAN_POINT('Ctrl Pts',(23.3562357049957,-6.05799586860639,0.0407500773712745));
#69476=CARTESIAN_POINT('Ctrl Pts',(23.4568056149535,-5.34291573720787,-2.85556052955536));
#69477=CARTESIAN_POINT('Ctrl Pts',(23.5573755249113,-3.3321831388715,-5.05940016621322));
#69478=CARTESIAN_POINT('Ctrl Pts',(23.6579454348691,-0.513398997797603,
-6.03633961784113));
#69479=CARTESIAN_POINT('Ctrl Pts',(23.7585153448269,2.42988395829362,-5.54947190839679));
#69480=CARTESIAN_POINT('Ctrl Pts',(23.8590852547847,4.78392214621243,-3.71686203831083));
#69481=CARTESIAN_POINT('Ctrl Pts',(23.9596551647425,5.9778633318121,-0.982916323515933));
#69482=CARTESIAN_POINT('Ctrl Pts',(24.0602250747003,5.72217780536357,1.98938575360903));
#69483=CARTESIAN_POINT('Ctrl Pts',(24.1607949846581,4.07886908692909,4.47926349800412));
#69484=CARTESIAN_POINT('Ctrl Pts',(24.2613648946159,1.44643812612182,5.88292370001167));
#69485=CARTESIAN_POINT('Ctrl Pts',(24.3619348045737,-1.53675283513459,5.85997996895585));
#69486=CARTESIAN_POINT('Ctrl Pts',(24.4625047145315,-4.14728255675176,4.41599613986702));
#69487=CARTESIAN_POINT('Ctrl Pts',(24.5630746244893,-5.7520998284564,1.90113704827657));
#69488=CARTESIAN_POINT('Ctrl Pts',(24.6636445344472,-5.96203784333286,-1.07474614096765));
#69489=CARTESIAN_POINT('Ctrl Pts',(24.7642144444049,-4.72618681349424,-3.79000431619953));
#69490=CARTESIAN_POINT('Ctrl Pts',(24.8647843543628,-2.34423954982043,-5.58618970729741));
#69491=CARTESIAN_POINT('Ctrl Pts',(24.9653542643205,0.606183786696204,-6.027728903128));
#69492=CARTESIAN_POINT('Ctrl Pts',(25.0659241742783,3.40960807675939,-5.00754902879192));
#69493=CARTESIAN_POINT('Ctrl Pts',(25.1664940842361,5.38620534329685,-2.77304282561564));
#69494=CARTESIAN_POINT('Ctrl Pts',(25.267063994194,6.05665245068485,0.133923875657654));
#69495=CARTESIAN_POINT('Ctrl Pts',(25.3676339041517,5.25836655252189,3.00841415236948));
#69496=CARTESIAN_POINT('Ctrl Pts',(25.4682038141095,3.1849312919251,5.15336658686088));
#69497=CARTESIAN_POINT('Ctrl Pts',(25.5687737240673,0.339152934716677,6.04863206020427));
#69498=CARTESIAN_POINT('Ctrl Pts',(25.6693436340251,-2.58886971720797,5.47710946578407));
#69499=CARTESIAN_POINT('Ctrl Pts',(25.7699135439829,-4.88909369128298,3.57739254076412));
#69500=CARTESIAN_POINT('Ctrl Pts',(25.8704834539407,-6.00371665389393,0.810161004130993));
#69501=CARTESIAN_POINT('Ctrl Pts',(25.9710533638985,-5.66244349610708,-2.15353387859408));
#69502=CARTESIAN_POINT('Ctrl Pts',(26.0716232738563,-3.94803266490803,-4.59499864958382));
#69503=CARTESIAN_POINT('Ctrl Pts',(26.1721931838141,-1.27622731104849,-5.92218020355611));
#69504=CARTESIAN_POINT('Ctrl Pts',(26.272763093772,1.70506206712723,-5.81323815614858));
#69505=CARTESIAN_POINT('Ctrl Pts',(26.3733330037297,4.27287536179091,-4.29459086007714));
#69506=CARTESIAN_POINT('Ctrl Pts',(26.4739029136876,5.80452005943394,-1.73450897734397));
#69507=CARTESIAN_POINT('Ctrl Pts',(26.5744728236454,5.92857363936159,1.24618983928002));
#69508=CARTESIAN_POINT('Ctrl Pts',(26.6750427336032,4.61495321523026,3.92468869263458));
#69509=CARTESIAN_POINT('Ctrl Pts',(26.775612643561,2.18221060908968,5.65145391650984));
#69510=CARTESIAN_POINT('Ctrl Pts',(26.8761825535188,-0.779716191245683,
6.00774643056506));
#69511=CARTESIAN_POINT('Ctrl Pts',(26.9767524634766,-3.55256248640603,4.90716560684868));
#69512=CARTESIAN_POINT('Ctrl Pts',(27.0773223734343,-5.46391543676058,2.61660134770037));
#69513=CARTESIAN_POINT('Ctrl Pts',(27.1778922833921,-6.05027359719579,-0.308486485819792));
#69514=CARTESIAN_POINT('Ctrl Pts',(27.27846219335,-5.16944561856005,-3.15876661208267));
#69515=CARTESIAN_POINT('Ctrl Pts',(27.3790321033077,-3.03503152743054,-5.24304855407239));
#69516=CARTESIAN_POINT('Ctrl Pts',(27.4796020132656,-0.164624903541294,
-6.05589573506611));
#69517=CARTESIAN_POINT('Ctrl Pts',(27.5801719232234,2.74570311774287,-5.40019341339503));
#69518=CARTESIAN_POINT('Ctrl Pts',(27.6807418331811,4.99020049655438,-3.434948837617));
#69519=CARTESIAN_POINT('Ctrl Pts',(27.781311743139,6.02457855065914,-0.636732125619322));
#69520=CARTESIAN_POINT('Ctrl Pts',(27.8818816530968,5.59800149235906,2.31589157872376));
#69521=CARTESIAN_POINT('Ctrl Pts',(27.9824515630546,3.81391389108215,4.7069135688122));
#69522=CARTESIAN_POINT('Ctrl Pts',(28.0830214730124,1.10495545434426,5.95651307030991));
#69523=CARTESIAN_POINT('Ctrl Pts',(28.1835913829702,-1.87195372889476,5.76166327979473));
#69524=CARTESIAN_POINT('Ctrl Pts',(28.284161292928,-4.39491574430826,4.16961510373431));
#69525=CARTESIAN_POINT('Ctrl Pts',(28.3847312028858,-5.85211447499653,1.56643885434258));
#69526=CARTESIAN_POINT('Ctrl Pts',(28.4853011128436,-5.89018048316609,-1.41659746879174));
#69527=CARTESIAN_POINT('Ctrl Pts',(28.5858710228014,-4.49988279460417,-4.05611012519177));
#69528=CARTESIAN_POINT('Ctrl Pts',(28.6864409327592,-2.01836740197889,-5.71201956784875));
#69529=CARTESIAN_POINT('Ctrl Pts',(28.787010842717,0.952600348157724,-5.98276918237263));
#69530=CARTESIAN_POINT('Ctrl Pts',(28.8875807526748,3.69256333389179,-4.80270242031044));
#69531=CARTESIAN_POINT('Ctrl Pts',(28.9881506626326,5.53708288982151,-2.45798445562696));
#69532=CARTESIAN_POINT('Ctrl Pts',(29.0887205725904,6.03886461144926,0.482792623642562));
#69533=CARTESIAN_POINT('Ctrl Pts',(29.1892904825482,5.07622686322841,3.30649290728049));
#69534=CARTESIAN_POINT('Ctrl Pts',(29.289860392506,2.88260847043635,5.32837150722681));
#69535=CARTESIAN_POINT('Ctrl Pts',(29.3904303024638,-0.0100399950044803,
6.05812460348565));
#69536=CARTESIAN_POINT('Ctrl Pts',(29.4910002124216,-2.90025377029946,5.31878769840664));
#69537=CARTESIAN_POINT('Ctrl Pts',(29.5915701223794,-5.08715850291843,3.28964935502898));
#69538=CARTESIAN_POINT('Ctrl Pts',(29.6921400323372,-6.04043167775162,0.462773874881315));
#69539=CARTESIAN_POINT('Ctrl Pts',(29.792709942295,-5.52890537050686,-2.47632387155606));
#69540=CARTESIAN_POINT('Ctrl Pts',(29.8932798522528,-3.67662427035448,-4.81491521083168));
#69541=CARTESIAN_POINT('Ctrl Pts',(29.9938497622106,-0.932764949584756,
-5.98589375629772));
#69542=CARTESIAN_POINT('Ctrl Pts',(30.0944196721684,2.03728906850845,-5.70529821869058));
#69543=CARTESIAN_POINT('Ctrl Pts',(30.1949895821262,4.51330224124522,-4.04117277433529));
#69544=CARTESIAN_POINT('Ctrl Pts',(30.295559492084,5.89484350566002,-1.39706641096112));
#69545=CARTESIAN_POINT('Ctrl Pts',(30.3961294020418,5.84689029440262,1.5858273544363));
#69546=CARTESIAN_POINT('Ctrl Pts',(30.4966993119996,4.38107121992341,4.18415935150857));
#69547=CARTESIAN_POINT('Ctrl Pts',(30.5972692219574,1.85284614596454,5.76783630768438));
#69548=CARTESIAN_POINT('Ctrl Pts',(30.6978391319152,-1.12469252340764,5.95281792436565));
#69549=CARTESIAN_POINT('Ctrl Pts',(30.798409041873,-3.82949422402105,4.69424631874461));
#69550=CARTESIAN_POINT('Ctrl Pts',(30.8989789518308,-5.6056468718478,2.29732402176987));
#69551=CARTESIAN_POINT('Ctrl Pts',(30.9995488617886,-6.02243497875305,-0.656697372881666));
#69552=CARTESIAN_POINT('Ctrl Pts',(31.1001187717465,-4.97878778759543,-3.45147021991332));
#69553=CARTESIAN_POINT('Ctrl Pts',(31.2006886817042,-2.72778884382925,-5.40926450974054));
#69554=CARTESIAN_POINT('Ctrl Pts',(31.301258591662,0.18469654640664,-6.05531681240572));
#69555=CARTESIAN_POINT('Ctrl Pts',(31.4018285016198,3.05239318313103,-5.2329600006529));
#69556=CARTESIAN_POINT('Ctrl Pts',(31.5023984115776,5.17988710053376,-3.14161489342376));
#69557=CARTESIAN_POINT('Ctrl Pts',(31.6029683215354,6.05126285505238,-0.288430878931537));
#69558=CARTESIAN_POINT('Ctrl Pts',(31.7035382314933,5.45521257632139,2.63469737541198));
#69559=CARTESIAN_POINT('Ctrl Pts',(31.804108141451,3.53627794383591,4.91891378424115));
#69560=CARTESIAN_POINT('Ctrl Pts',(31.9046780514089,0.759798954099677,6.0102978347339));
#69561=CARTESIAN_POINT('Ctrl Pts',(32.0052479613666,-2.20093062794899,5.64418983414041));
#69562=CARTESIAN_POINT('Ctrl Pts',(32.1058178713245,-4.62793642734424,3.90937065744835));
#69563=CARTESIAN_POINT('Ctrl Pts',(32.2063877812822,-5.9326716269689,1.22653246162345));
#69564=CARTESIAN_POINT('Ctrl Pts',(32.3069576912401,-5.79873906406749,-1.75373880031083));
#69565=CARTESIAN_POINT('Ctrl Pts',(32.4075276011978,-4.25861726985059,-4.30872991283835));
#69566=CARTESIAN_POINT('Ctrl Pts',(32.5080975111556,-1.68578445363485,-5.81885773058089));
#69567=CARTESIAN_POINT('Ctrl Pts',(32.6086674211135,1.29584964141577,-5.91791755769718));
#69568=CARTESIAN_POINT('Ctrl Pts',(32.7092373310713,3.96324131392763,-4.58188747138504));
#69569=CARTESIAN_POINT('Ctrl Pts',(32.809807241029,5.6695503794838,-2.13475361748213));
#69570=CARTESIAN_POINT('Ctrl Pts',(32.9103771509869,6.00099835852668,0.830056151003031));
#69571=CARTESIAN_POINT('Ctrl Pts',(33.0109470609446,4.87720940145834,3.59357801740607));
#69572=CARTESIAN_POINT('Ctrl Pts',(33.1115169709025,2.57070136297812,5.48566030804317));
#69573=CARTESIAN_POINT('Ctrl Pts',(33.2120868808602,-0.359199543090878,
6.04747469619355));
#69574=CARTESIAN_POINT('Ctrl Pts',(33.3126567908181,-3.20199486916962,5.14278167635662));
#69575=CARTESIAN_POINT('Ctrl Pts',(33.4132267007758,-5.26830919584373,2.99096852705713));
#69576=CARTESIAN_POINT('Ctrl Pts',(33.5137966107337,-6.05706307763735,0.113848084657791));
#69577=CARTESIAN_POINT('Ctrl Pts',(33.6143665206914,-5.37698437719752,-2.79088042026733));
#69578=CARTESIAN_POINT('Ctrl Pts',(33.7149364306493,-3.39299159394969,-5.01882282574756));
#69579=CARTESIAN_POINT('Ctrl Pts',(33.815506340607,-0.586201269953505,-6.02970501633063));
#69580=CARTESIAN_POINT('Ctrl Pts',(33.9160762505649,2.36274235738757,-5.57838893099654));
#69581=CARTESIAN_POINT('Ctrl Pts',(34.0166461605227,4.73872299697853,-3.7743183319329));
#69582=CARTESIAN_POINT('Ctrl Pts',(34.1172160704805,5.96556738903081,-1.05497878641703));
#69583=CARTESIAN_POINT('Ctrl Pts',(34.2177859804382,5.74576682457463,1.92019220664896));
#69584=CARTESIAN_POINT('Ctrl Pts',(34.3183558903961,4.13262275128,4.4297182425591));
#69585=CARTESIAN_POINT('Ctrl Pts',(34.4189258003539,1.51732121828013,5.86504141787719));
#69586=CARTESIAN_POINT('Ctrl Pts',(34.5194957103117,-1.46592940399906,5.8780970981559));
#69587=CARTESIAN_POINT('Ctrl Pts',(34.6200656202695,-4.09369340772253,4.46571929216637));
#69588=CARTESIAN_POINT('Ctrl Pts',(34.7206355302273,-5.72874028404199,1.97040840204573));
#69589=CARTESIAN_POINT('Ctrl Pts',(34.8212054401851,-5.97457257294518,-1.00272482938694));
#69590=CARTESIAN_POINT('Ctrl Pts',(34.9217753501429,-4.77157615599258,-3.73269815286756));
#69591=CARTESIAN_POINT('Ctrl Pts',(35.0223452601007,-2.41147662872138,-5.55749538749143));
#69592=CARTESIAN_POINT('Ctrl Pts',(35.1229151700585,0.533403905146523,-6.03460477470002));
#69593=CARTESIAN_POINT('Ctrl Pts',(35.2234850800163,3.34893445118577,-5.04832769880472));
#69594=CARTESIAN_POINT('Ctrl Pts',(35.3240549899741,5.35235127567129,-2.83783550169453));
#69595=CARTESIAN_POINT('Ctrl Pts',(35.4246248999319,6.05782752326399,0.0608293616863961));
#69596=CARTESIAN_POINT('Ctrl Pts',(35.5251948098897,5.29428581121683,2.94474315722203));
#69597=CARTESIAN_POINT('Ctrl Pts',(35.6257647198475,3.24688434742266,5.11455927205068));
#69598=CARTESIAN_POINT('Ctrl Pts',(35.7263346298053,0.412116224389641,6.04409916616635));
#69599=CARTESIAN_POINT('Ctrl Pts',(35.8269045397631,-2.52258972829639,5.50795021542056));
#69600=CARTESIAN_POINT('Ctrl Pts',(35.9274744497208,-4.84556984338814,3.63612807883681));
#69601=CARTESIAN_POINT('Ctrl Pts',(36.0280443596788,-5.99350344266373,0.882548013218436));
#69602=CARTESIAN_POINT('Ctrl Pts',(36.1286142696365,-5.68801761647303,-2.08504918588275));
#69603=CARTESIAN_POINT('Ctrl Pts',(36.2291841795943,-4.00319241469631,-4.54702375227752));
#69604=CARTESIAN_POINT('Ctrl Pts',(36.3297540895521,-1.34759649841855,-5.90634897295342));
#69605=CARTESIAN_POINT('Ctrl Pts',(36.4303239995099,1.63479040867594,-5.83338965204271));
#69606=CARTESIAN_POINT('Ctrl Pts',(36.5308939094677,4.22074204894102,-4.34583836206078));
#69607=CARTESIAN_POINT('Ctrl Pts',(36.6314638194255,5.78316737567371,-1.80442501030139));
#69608=CARTESIAN_POINT('Ctrl Pts',(36.7320337293833,5.94317959212186,1.17455985315532));
#69609=CARTESIAN_POINT('Ctrl Pts',(36.8326036393411,4.66197587353986,3.86871496331666));
#69610=CARTESIAN_POINT('Ctrl Pts',(36.9331735492989,2.25024701878697,5.62471002517447));
#69611=CARTESIAN_POINT('Ctrl Pts',(37.0337434592567,-0.707164800944547,
6.01671774783917));
#69612=CARTESIAN_POINT('Ctrl Pts',(37.1343133692145,-3.49308976519476,4.94967659601609));
#69613=CARTESIAN_POINT('Ctrl Pts',(37.2348832791723,-5.43194346833712,2.68234313048267));
#69614=CARTESIAN_POINT('Ctrl Pts',(37.3354531891302,-6.05355555638045,-0.235456235154939));
#69615=CARTESIAN_POINT('Ctrl Pts',(37.4360230990879,-5.20718563307572,-3.09615766645496));
#69616=CARTESIAN_POINT('Ctrl Pts',(37.5365930090458,-3.09807767624484,-5.20604352890092));
#69617=CARTESIAN_POINT('Ctrl Pts',(37.6371629190035,-0.237688549838743,
-6.05346831709999));
#69618=CARTESIAN_POINT('Ctrl Pts',(37.7377328289614,2.68033984529413,-5.43293224940147));
#69619=CARTESIAN_POINT('Ctrl Pts',(37.8383027389191,4.94838813525662,-3.49491478804698));
#69620=CARTESIAN_POINT('Ctrl Pts',(37.9388726488769,6.01645656213379,-0.709383499113968));
#69621=CARTESIAN_POINT('Ctrl Pts',(38.0394425588348,5.62553945183186,2.24817267769651));
#69622=CARTESIAN_POINT('Ctrl Pts',(38.1400124687925,3.87043386708642,4.66054891545712));
#69623=CARTESIAN_POINT('Ctrl Pts',(38.2405823787503,1.17675140135296,5.94274605315352));
#69624=CARTESIAN_POINT('Ctrl Pts',(38.3411522887081,-1.80229226622721,5.78383238864642));
#69625=CARTESIAN_POINT('Ctrl Pts',(38.441722198666,-4.34428161071217,4.22234434878138));
#69626=CARTESIAN_POINT('Ctrl Pts',(38.5422921086237,-5.83278640428161,1.63694143905193));
#69627=CARTESIAN_POINT('Ctrl Pts',(38.6428620185816,-5.90684551584258,-1.34541836052145));
#69628=CARTESIAN_POINT('Ctrl Pts',(38.7434319285394,-4.54849967459375,-4.00151536584311));
#69629=CARTESIAN_POINT('Ctrl Pts',(38.8440018384971,-2.08714657773488,-5.68724833956698));
#69630=CARTESIAN_POINT('Ctrl Pts',(38.944571748455,0.880337767549051,-5.99382848669234));
#69631=CARTESIAN_POINT('Ctrl Pts',(39.0451416584127,3.63434096202235,-4.84691038545427));
#69632=CARTESIAN_POINT('Ctrl Pts',(39.1457115683706,5.50701960175014,-2.52462068810298));
#69633=CARTESIAN_POINT('Ctrl Pts',(39.2462814783283,6.04425072865394,0.409887352847377));
#69634=CARTESIAN_POINT('Ctrl Pts',(39.3468513882862,5.11575625692352,3.24499806357505));
#69635=CARTESIAN_POINT('Ctrl Pts',(39.4474212982439,2.94669529667884,5.29319953727315));
#69636=CARTESIAN_POINT('Ctrl Pts',(39.5479912082018,0.0630632635893668,
6.05780467972048));
#69637=CARTESIAN_POINT('Ctrl Pts',(39.6485611181596,-2.83586155663387,5.35339740206759));
#69638=CARTESIAN_POINT('Ctrl Pts',(39.7491310281174,-5.04709239056434,3.35079586277132));
#69639=CARTESIAN_POINT('Ctrl Pts',(39.8497009380752,-6.03440766446482,0.535629211214205));
#69640=CARTESIAN_POINT('Ctrl Pts',(39.950270848033,-5.55838427432381,-2.40942706297736));
#69641=CARTESIAN_POINT('Ctrl Pts',(40.0508407579908,-3.73445748247584,-4.77019934850087));
#69642=CARTESIAN_POINT('Ctrl Pts',(40.1514106679486,-1.00492796585556,-5.97420239833732));
#69643=CARTESIAN_POINT('Ctrl Pts',(40.2519805779064,1.96829571741389,-5.7294665093417));
#69644=CARTESIAN_POINT('Ctrl Pts',(40.3525504878642,4.46420938357584,-4.09533992391978));
#69645=CARTESIAN_POINT('Ctrl Pts',(40.453120397822,5.8775561171401,-1.46809693233341));
#69646=CARTESIAN_POINT('Ctrl Pts',(40.5536903077798,5.86560055186679,1.51515830156386));
#69647=CARTESIAN_POINT('Ctrl Pts',(40.6542602177375,4.43124190204296,4.13098895162365));
#69648=CARTESIAN_POINT('Ctrl Pts',(40.7548301276954,1.92231090551379,5.74505833698848));
#69649=CARTESIAN_POINT('Ctrl Pts',(40.8554000376532,-1.05277883082213,5.96595602114453));
#69650=CARTESIAN_POINT('Ctrl Pts',(40.955969947611,-3.77257060694586,4.74011450583907));
#69651=CARTESIAN_POINT('Ctrl Pts',(41.0565398575688,-5.57751725842217,2.36479930329417));
#69652=CARTESIAN_POINT('Ctrl Pts',(41.1571097675266,-6.02992077601796,-0.583977694612491));
#69653=CARTESIAN_POINT('Ctrl Pts',(41.2576796774844,-5.02007369615812,-3.39114060428041));
#69654=CARTESIAN_POINT('Ctrl Pts',(41.3582495874422,-2.79286306640333,-5.37595483660142));
#69655=CARTESIAN_POINT('Ctrl Pts',(41.4588194974,0.111614452777684,-6.05710464882267));
#69656=CARTESIAN_POINT('Ctrl Pts',(41.5593894073578,2.98902556324098,-5.26941179783377));
#69657=CARTESIAN_POINT('Ctrl Pts',(41.6599593173156,5.14160054765725,-3.20389112193102));
#69658=CARTESIAN_POINT('Ctrl Pts',(41.7605292272734,6.04734182530387,-0.361429606961375));
#69659=CARTESIAN_POINT('Ctrl Pts',(41.8610991372312,5.4866079160396,2.56867827656746));
#69660=CARTESIAN_POINT('Ctrl Pts',(41.961669047189,3.59537631016514,4.87588388922062));
#69661=CARTESIAN_POINT('Ctrl Pts',(42.0622389571468,0.832269044078688,6.00069185603845));
#69662=CARTESIAN_POINT('Ctrl Pts',(42.1628088671046,-2.13266274875579,5.67033721333462));
#69663=CARTESIAN_POINT('Ctrl Pts',(42.2633787770624,-4.58042566087425,3.964930677586));
#69664=CARTESIAN_POINT('Ctrl Pts',(42.3639486870202,-5.91743929319244,1.29803186564886));
#69665=CARTESIAN_POINT('Ctrl Pts',(42.464518596978,-5.81947899081297,-1.68363855632504));
#69666=CARTESIAN_POINT('Ctrl Pts',(42.5650885069358,-4.31030004273577,-4.25702807771454));
#69667=CARTESIAN_POINT('Ctrl Pts',(42.6656584168936,-1.75587704472498,-5.79809195483013));
#69668=CARTESIAN_POINT('Ctrl Pts',(42.7662283268514,1.22434462512233,-5.9331235240632));
#69669=CARTESIAN_POINT('Ctrl Pts',(42.8667982368092,3.90766377732837,-4.62937774611378));
#69670=CARTESIAN_POINT('Ctrl Pts',(42.967368146767,5.64337782736131,-2.20301184983298));
#69671=CARTESIAN_POINT('Ctrl Pts',(43.0679380567248,6.01057761224065,0.757582523616525));
#69672=CARTESIAN_POINT('Ctrl Pts',(43.1685079666826,4.92021750022926,3.53446378723784));
#69673=CARTESIAN_POINT('Ctrl Pts',(43.2690778766404,2.63670887987654,5.45424062502182));
#69674=CARTESIAN_POINT('Ctrl Pts',(43.3696477865982,-0.286199374091665,
6.05136880640467));
#69675=CARTESIAN_POINT('Ctrl Pts',(43.470217696556,-3.1397045262112,5.18104526142618));
#69676=CARTESIAN_POINT('Ctrl Pts',(43.5707876065138,-5.23183403347219,3.05432270054425));
#69677=CARTESIAN_POINT('Ctrl Pts',(43.6713575164717,-6.05524829132899,0.186929514028943));
#69678=CARTESIAN_POINT('Ctrl Pts',(43.7719274264294,-5.41027005106995,-2.72579391872415));
#69679=CARTESIAN_POINT('Ctrl Pts',(43.8724973363873,-3.45330598074203,-4.97751467262823));
#69680=CARTESIAN_POINT('Ctrl Pts',(43.973067246345,-0.658918182789008,-6.0221924032073));
#69681=CARTESIAN_POINT('Ctrl Pts',(44.0736371563029,2.29525670727468,-5.60649366008458));
#69682=CARTESIAN_POINT('Ctrl Pts',(44.1742070662606,4.69283382164707,-3.83122503062184));
#69683=CARTESIAN_POINT('Ctrl Pts',(44.2747769762185,5.95240277399595,-1.1268876292617));
#69684=CARTESIAN_POINT('Ctrl Pts',(44.3753468861762,5.76851917764986,1.85071905213722));
#69685=CARTESIAN_POINT('Ctrl Pts',(44.4759167961341,4.18577464643037,4.37952795654495));
#69686=CARTESIAN_POINT('Ctrl Pts',(44.5764867060918,1.58798336668632,5.84630510151374));
#69687=CARTESIAN_POINT('Ctrl Pts',(44.6770566160497,-1.39489251249749,5.89535829203248));
#69688=CARTESIAN_POINT('Ctrl Pts',(44.7776265260074,-4.03950815816409,4.5147921716269));
#69689=CARTESIAN_POINT('Ctrl Pts',(44.8781964359653,-5.70454655280041,2.03939283606441));
#69690=CARTESIAN_POINT('Ctrl Pts',(44.978766345923,-5.98623731901994,-0.9305575066759));
#69691=CARTESIAN_POINT('Ctrl Pts',(45.0793362558809,-4.81627068850187,-3.67484845509796));
#69692=CARTESIAN_POINT('Ctrl Pts',(45.1799061658386,-2.47836256200596,-5.52799181657365));
#69693=CARTESIAN_POINT('Ctrl Pts',(45.2804760757965,0.460546352330777,-6.04060192118407));
#69694=CARTESIAN_POINT('Ctrl Pts',(45.3810459857542,3.28777317267875,-5.08837125983076));
#69695=CARTESIAN_POINT('Ctrl Pts',(45.481615895712,5.3177178288616,-2.90221494818445));
#69696=CARTESIAN_POINT('Ctrl Pts',(45.5821858056699,6.05812048918958,-0.0122740099132358));
#69697=CARTESIAN_POINT('Ctrl Pts',(45.6827557156276,5.32943414589292,2.88064336519618));
#69698=CARTESIAN_POINT('Ctrl Pts',(45.7833256255855,3.30836460994689,5.07500720398591));
#69699=CARTESIAN_POINT('Ctrl Pts',(45.8838955355433,0.485019504023933,6.03868616452074));
#69700=CARTESIAN_POINT('Ctrl Pts',(45.984465445501,-2.45594241410608,5.53798892843354));
#69701=CARTESIAN_POINT('Ctrl Pts',(46.0850353554589,-4.80134041096105,3.69433414446097));
#69702=CARTESIAN_POINT('Ctrl Pts',(46.1856052654166,-5.98241749128956,0.954806510645358));
#69703=CARTESIAN_POINT('Ctrl Pts',(46.2861751753745,-5.71276347981686,-2.01626088007693));
#69704=CARTESIAN_POINT('Ctrl Pts',(46.3867450853323,-4.05776924219922,-4.49838674303575));
#69705=CARTESIAN_POINT('Ctrl Pts',(46.4873149952901,-1.41876945639242,-5.88965769314871));
#69706=CARTESIAN_POINT('Ctrl Pts',(46.5878849052479,1.56428070127213,-5.85269172265938));
#69707=CARTESIAN_POINT('Ctrl Pts',(46.6884548152057,4.16799413545586,-4.39645304758999));
#69708=CARTESIAN_POINT('Ctrl Pts',(46.7890247251635,5.76097257972044,-1.87407829307293));
#69709=CARTESIAN_POINT('Ctrl Pts',(46.8895946351213,5.95692013261322,1.102758834254));
#69710=CARTESIAN_POINT('Ctrl Pts',(46.9901645450792,4.70831968123497,3.81217789356075));
#69711=CARTESIAN_POINT('Ctrl Pts',(47.0907344550368,2.31795576021386,5.59714709531108));
#69712=CARTESIAN_POINT('Ctrl Pts',(47.1913043649948,-0.634510437296323,
6.02481294463323));
#69713=CARTESIAN_POINT('Ctrl Pts',(47.2918742749524,-3.43310839996693,4.99146684121354));
#69714=CARTESIAN_POINT('Ctrl Pts',(47.3924441849103,-5.39918053096372,2.74769432559742));
#69715=CARTESIAN_POINT('Ctrl Pts',(47.493014094868,-6.05595603097126,-0.16239169868203));
#69716=CARTESIAN_POINT('Ctrl Pts',(47.593584004826,-5.24416740660887,-3.03309787582251));
#69717=CARTESIAN_POINT('Ctrl Pts',(47.6941539147836,-3.16067270047356,-5.16828042905366));
#69718=CARTESIAN_POINT('Ctrl Pts',(47.7947238247416,-0.310717585271087,
-6.05015942724333));
#69719=CARTESIAN_POINT('Ctrl Pts',(47.8952937346992,2.61458627688499,-5.4648799724772));
#69720=CARTESIAN_POINT('Ctrl Pts',(47.9958636446571,4.90585521760734,-3.55437182871079));
#69721=CARTESIAN_POINT('Ctrl Pts',(48.0964335546149,6.00745849116074,-0.781931576187193));
#69722=CARTESIAN_POINT('Ctrl Pts',(48.1970034645728,5.65225825200023,2.18012641045266));
#69723=CARTESIAN_POINT('Ctrl Pts',(48.2975733745305,3.92639025235566,4.61350561927309));
#69724=CARTESIAN_POINT('Ctrl Pts',(48.3981432844883,1.24837599646418,5.92811368685774));
#69725=CARTESIAN_POINT('Ctrl Pts',(48.4987131944461,-1.73236836393201,5.80515928846964));
#69726=CARTESIAN_POINT('Ctrl Pts',(48.599283104404,-4.29301488734706,4.27445875987527));
#69727=CARTESIAN_POINT('Ctrl Pts',(48.6998530143617,-5.81260899613078,1.70720566158783));
#69728=CARTESIAN_POINT('Ctrl Pts',(48.8004229243196,-5.92265042701329,-1.27404334002308));
#69729=CARTESIAN_POINT('Ctrl Pts',(48.9009928342773,-4.59645422773243,-3.94633792841142));
#69730=CARTESIAN_POINT('Ctrl Pts',(49.0015627442352,-2.15562183498608,-5.66164896628087));
#69731=CARTESIAN_POINT('Ctrl Pts',(49.1021326541929,0.807946997123318,-6.00401500353698));
#69732=CARTESIAN_POINT('Ctrl Pts',(49.2027025641508,3.57558937793424,-4.89041257086371));
#69733=CARTESIAN_POINT('Ctrl Pts',(49.3032724741085,5.47615441256601,-2.59088929956335));
#69734=CARTESIAN_POINT('Ctrl Pts',(49.4038423840664,6.04875671618125,0.336922396569298));
#69735=CARTESIAN_POINT('Ctrl Pts',(49.5044122940241,5.15454072306582,3.18303070156636));
#69736=CARTESIAN_POINT('Ctrl Pts',(49.6049822039819,3.0103530417834,5.25725680147769));
#69737=CARTESIAN_POINT('Ctrl Pts',(49.7055521139397,0.136157339266722,6.05660265262809));
#69738=CARTESIAN_POINT('Ctrl Pts',(49.8061220238975,-2.77105640081398,5.38722757421346));
#69739=CARTESIAN_POINT('Ctrl Pts',(49.9066919338553,-5.00629134910212,3.41145444653204));
#69740=CARTESIAN_POINT('Ctrl Pts',(50.0072618438131,-6.02750495479215,0.608406552244426));
#69741=CARTESIAN_POINT('Ctrl Pts',(50.1078317537709,-5.58705379759421,-2.34217940722865));
#69742=CARTESIAN_POINT('Ctrl Pts',(50.2084016637287,-3.79174690397582,-4.72478887666399));
#69743=CARTESIAN_POINT('Ctrl Pts',(50.3089715736866,-1.07694465018776,-5.96164111074206));
#69744=CARTESIAN_POINT('Ctrl Pts',(50.4095414836443,1.89901575420593,-5.75280050741684));
#69745=CARTESIAN_POINT('Ctrl Pts',(50.5101113936022,4.41446647293192,-4.14891073321875));
#69746=CARTESIAN_POINT('Ctrl Pts',(50.6106813035599,5.85941287207133,-1.53891367771645));
#69747=CARTESIAN_POINT('Ctrl Pts',(50.7112512135178,5.88345669368406,1.44426861989114));
#69748=CARTESIAN_POINT('Ctrl Pts',(50.8118211234755,4.4807673317266,4.07721702044296));
#69749=CARTESIAN_POINT('Ctrl Pts',(50.9123910334334,1.99149574899846,5.72144380332262));
#69750=CARTESIAN_POINT('Ctrl Pts',(51.0129609433911,-0.980711838525075,
5.97822538907948));
#69751=CARTESIAN_POINT('Ctrl Pts',(51.113530853349,-3.71509764943117,4.78529246421249));
#69752=CARTESIAN_POINT('Ctrl Pts',(51.2141007633067,-5.54857547841287,2.43193023609094));
#69753=CARTESIAN_POINT('Ctrl Pts',(51.3146706732646,-6.03652853025234,-0.511172980807434));
#69754=CARTESIAN_POINT('Ctrl Pts',(51.4152405832223,-5.06062860992243,-3.33031718989236));
#69755=CARTESIAN_POINT('Ctrl Pts',(51.5158104931802,-2.85753060802056,-5.34186234726087));
#69756=CARTESIAN_POINT('Ctrl Pts',(51.6163804031379,0.0385161064819134,
-6.05801048384692));
#69757=CARTESIAN_POINT('Ctrl Pts',(51.7169503130958,2.9252226983183,-5.30509629300932));
#69758=CARTESIAN_POINT('Ctrl Pts',(51.8175202230535,5.10256530392816,-3.26570081789599));
#69759=CARTESIAN_POINT('Ctrl Pts',(51.9180901330113,6.04254021576997,-0.43437570565172));
#69760=CARTESIAN_POINT('Ctrl Pts',(52.0186600429692,5.51720432687948,2.50228514129));
#69761=CARTESIAN_POINT('Ctrl Pts',(52.119229952927,3.65395113808825,4.8321439955077));
#69762=CARTESIAN_POINT('Ctrl Pts',(52.2197998628847,0.90461794373694,5.99021209046278));
#69763=CARTESIAN_POINT('Ctrl Pts',(52.3203697728426,-2.06408432325012,5.69565891002731));
#69764=CARTESIAN_POINT('Ctrl Pts',(52.4209396828003,-4.53224791867086,4.01991334689623));
#69765=CARTESIAN_POINT('Ctrl Pts',(52.5215095927582,-5.90134529530529,1.36934225760051));
#69766=CARTESIAN_POINT('Ctrl Pts',(52.6220795027159,-5.83937151787078,-1.61329315039637));
#69767=CARTESIAN_POINT('Ctrl Pts',(52.7226494126738,-4.36135517406001,-4.20470635818695));
#69768=CARTESIAN_POINT('Ctrl Pts',(52.8232193226315,-1.82571395490191,-5.77648189365705));
#69769=CARTESIAN_POINT('Ctrl Pts',(52.9237892325894,1.15266132665882,-5.94746554246089));
#69770=CARTESIAN_POINT('Ctrl Pts',(53.0243591425472,3.85151722881557,-4.67619391699774));
#69771=CARTESIAN_POINT('Ctrl Pts',(53.124929052505,5.61638351835037,-2.27094929200402));
#69772=CARTESIAN_POINT('Ctrl Pts',(53.2254989624628,6.01928163968487,0.68499858128424));
#69773=CARTESIAN_POINT('Ctrl Pts',(53.3260688724206,4.96250914446559,3.47483488850872));
#69774=CARTESIAN_POINT('Ctrl Pts',(53.4266387823784,2.70233245456293,5.42202672605472));
#69775=CARTESIAN_POINT('Ctrl Pts',(53.5272086923362,-0.213157531242237,
6.05438175085432));
#69776=CARTESIAN_POINT('Ctrl Pts',(53.627778602294,-3.07695699546339,5.21855441112398));
#69777=CARTESIAN_POINT('Ctrl Pts',(53.7283485122518,-5.19459704435567,3.11723212236909));
#69778=CARTESIAN_POINT('Ctrl Pts',(53.8289184222096,-6.05255176728989,0.259983720705316));
#69779=CARTESIAN_POINT('Ctrl Pts',(53.9294883321674,-5.44276792496704,-2.6603104964399));
#69780=CARTESIAN_POINT('Ctrl Pts',(54.0300582421252,-3.51311749114105,-4.93548173368623));
#69781=CARTESIAN_POINT('Ctrl Pts',(54.1306281520831,-0.731539197512978,
-6.01380284938146));
#69782=CARTESIAN_POINT('Ctrl Pts',(54.2311980620408,2.22743693235633,-5.63378204828362));
#69783=CARTESIAN_POINT('Ctrl Pts',(54.3317679719986,4.64626111150299,-3.88757375973938));
#69784=CARTESIAN_POINT('Ctrl Pts',(54.4323378819564,5.93837177711084,-1.19863255369758));
#69785=CARTESIAN_POINT('Ctrl Pts',(54.5329077919142,5.79043082073166,1.78097674413478));
#69786=CARTESIAN_POINT('Ctrl Pts',(54.633477701872,4.23831846276371,4.32869928740943));
#69787=CARTESIAN_POINT('Ctrl Pts',(54.7340476118298,1.65841148346058,5.82671877265184));
#69788=CARTESIAN_POINT('Ctrl Pts',(54.8346175217877,-1.32364702837341,5.91175850596819));
#69789=CARTESIAN_POINT('Ctrl Pts',(54.9351874317454,-3.98474541470989,4.56321258577206));
#69790=CARTESIAN_POINT('Ctrl Pts',(55.0357573417033,-5.67950118530435,2.10807061113231));
#69791=CARTESIAN_POINT('Ctrl Pts',(55.136327251661,-5.99707144006536,-0.858235698386034));
#69792=CARTESIAN_POINT('Ctrl Pts',(55.2368971616188,-4.86018337906989,-3.61650093368403));
#69793=CARTESIAN_POINT('Ctrl Pts',(55.3374670715766,-2.54504712920928,-5.4976088187116));
#69794=CARTESIAN_POINT('Ctrl Pts',(55.4380369815344,0.387954839329869,-6.04588140635559));
#69795=CARTESIAN_POINT('Ctrl Pts',(55.505083588173,2.27948268610681,-5.43340712928736));
#69796=CARTESIAN_POINT('Ctrl Pts',(55.5386068914922,3.09548085772058,-4.92001278896564));
#69797=CARTESIAN_POINT('Ctrl Pts',(18.8656682926829,3.45292578700087,-4.38059386100382));
#69798=CARTESIAN_POINT('Ctrl Pts',(18.8991915960022,4.17945978894053,-3.8079162583704));
#69799=CARTESIAN_POINT('Ctrl Pts',(18.9662382026407,5.34139059168272,-2.29470092783305));
#69800=CARTESIAN_POINT('Ctrl Pts',(19.0668081125985,5.78874853530519,0.533337577335307));
#69801=CARTESIAN_POINT('Ctrl Pts',(19.1673780225563,4.83241525876795,3.23130860481921));
#69802=CARTESIAN_POINT('Ctrl Pts',(19.2679479325141,2.70419169563657,5.14605048923388));
#69803=CARTESIAN_POINT('Ctrl Pts',(19.3685178424719,-0.0797792217301073,
5.81269672472357));
#69804=CARTESIAN_POINT('Ctrl Pts',(19.4690877524298,-2.84441229285594,5.06986231595082));
#69805=CARTESIAN_POINT('Ctrl Pts',(19.5696576623875,-4.91927346795933,3.09754298939177));
#69806=CARTESIAN_POINT('Ctrl Pts',(19.6702275723453,-5.80121729124116,0.374096513770974));
#69807=CARTESIAN_POINT('Ctrl Pts',(19.7707974823032,-5.27636977596458,-2.44008049241649));
#69808=CARTESIAN_POINT('Ctrl Pts',(19.8713673922609,-3.4720077142605,-4.66253371853033));
#69809=CARTESIAN_POINT('Ctrl Pts',(19.9719373022187,-0.825686473140719,
-5.75432978220954));
#69810=CARTESIAN_POINT('Ctrl Pts',(20.0725072121766,2.02086287490732,-5.45070416604466));
#69811=CARTESIAN_POINT('Ctrl Pts',(20.1730771221344,4.37735479309912,-3.82528833061492));
#69812=CARTESIAN_POINT('Ctrl Pts',(20.2736470320921,5.67234190241483,-1.27224293413637));
#69813=CARTESIAN_POINT('Ctrl Pts',(20.37421694205,5.59179100359806,1.58932005701102));
#69814=CARTESIAN_POINT('Ctrl Pts',(20.4747868520077,4.15523558961498,4.06547441574607));
#69815=CARTESIAN_POINT('Ctrl Pts',(20.5753567619656,1.71103912739439,5.55575467045122));
#69816=CARTESIAN_POINT('Ctrl Pts',(20.6759266719234,-1.14808285301524,5.69876922970695));
#69817=CARTESIAN_POINT('Ctrl Pts',(20.7764965818812,-3.72879572848776,4.45983714130576));
#69818=CARTESIAN_POINT('Ctrl Pts',(20.877066491839,-5.40527885036333,2.13939839301869));
#69819=CARTESIAN_POINT('Ctrl Pts',(20.9776364017968,-5.77098650368354,-0.699842627867562));
#69820=CARTESIAN_POINT('Ctrl Pts',(21.0782063117546,-4.7372348978758,-3.36937241192321));
#69821=CARTESIAN_POINT('Ctrl Pts',(21.1787762217124,-2.5547079071865,-5.22183228757078));
#69822=CARTESIAN_POINT('Ctrl Pts',(21.2793461316702,0.247333551781491,-5.80800232805862));
#69823=CARTESIAN_POINT('Ctrl Pts',(21.379916041628,2.98939683737892,-4.98573680395642));
#69824=CARTESIAN_POINT('Ctrl Pts',(21.4804859515858,5.0065339632579,-2.95443439662243));
#69825=CARTESIAN_POINT('Ctrl Pts',(21.5810558615436,5.80959091282129,-0.206684191439672));
#69826=CARTESIAN_POINT('Ctrl Pts',(21.6816257715014,5.20382706708468,2.59118675228346));
#69827=CARTESIAN_POINT('Ctrl Pts',(21.7821956814592,3.33613963718532,4.76069713912736));
#69828=CARTESIAN_POINT('Ctrl Pts',(21.882765591417,0.659441217112314,5.77574256788688));
#69829=CARTESIAN_POINT('Ctrl Pts',(21.9833355013748,-2.17717113044407,5.39017539585389));
#69830=CARTESIAN_POINT('Ctrl Pts',(22.0839054113326,-4.48582135303932,3.69749533034633));
#69831=CARTESIAN_POINT('Ctrl Pts',(22.1844753212904,-5.70666375904613,1.10817583013857));
#69832=CARTESIAN_POINT('Ctrl Pts',(22.2850452312482,-5.5436451159441,-1.74987535492763));
#69833=CARTESIAN_POINT('Ctrl Pts',(22.385615141206,-4.03629730435431,-4.18358327276709));
#69834=CARTESIAN_POINT('Ctrl Pts',(22.4861850511638,-1.5501508710191,-5.60277584830882));
#69835=CARTESIAN_POINT('Ctrl Pts',(22.5867549611216,1.31190581412394,-5.66330010366589));
#69836=CARTESIAN_POINT('Ctrl Pts',(22.6873248710794,3.85582646866807,-4.35047895901507));
#69837=CARTESIAN_POINT('Ctrl Pts',(22.7878947810372,5.46471252376619,-1.98267041182017));
#69838=CARTESIAN_POINT('Ctrl Pts',(22.888464690995,5.74841049603226,0.865934003501583));
#69839=CARTESIAN_POINT('Ctrl Pts',(22.9890346009528,4.63812387140712,3.50455016839501));
#69840=CARTESIAN_POINT('Ctrl Pts',(23.0896045109106,2.40309620059581,5.29331593426996));
#69841=CARTESIAN_POINT('Ctrl Pts',(23.1901744208684,-0.414680230205875,
5.79845714272258));
#69842=CARTESIAN_POINT('Ctrl Pts',(23.2907443308262,-3.13189706215126,4.89747748554319));
#69843=CARTESIAN_POINT('Ctrl Pts',(23.391314240784,-5.08963155255177,2.80886375400866));
#69844=CARTESIAN_POINT('Ctrl Pts',(23.4918841507418,-5.81313477275929,0.0391029800775002));
#69845=CARTESIAN_POINT('Ctrl Pts',(23.5924540606996,-5.12695781468582,-2.74014023286149));
#69846=CARTESIAN_POINT('Ctrl Pts',(23.6930239706574,-3.19749799998333,-4.85490179812288));
#69847=CARTESIAN_POINT('Ctrl Pts',(23.7935938806152,-0.492647672782865,
-5.79235385657815));
#69848=CARTESIAN_POINT('Ctrl Pts',(23.894163790573,2.33166929098219,-5.32516509103753));
#69849=CARTESIAN_POINT('Ctrl Pts',(23.9947337005308,4.59055845885185,-3.56662837497514));
#69850=CARTESIAN_POINT('Ctrl Pts',(24.0953036104886,5.73624115213431,-0.94318734823729));
#69851=CARTESIAN_POINT('Ctrl Pts',(24.1958735204464,5.49089030394512,1.90897579852541));
#69852=CARTESIAN_POINT('Ctrl Pts',(24.2964434304042,3.91400328376506,4.2982139574468));
#69853=CARTESIAN_POINT('Ctrl Pts',(24.397013340362,1.38797383655825,5.64513893171319));
#69854=CARTESIAN_POINT('Ctrl Pts',(24.4975832503198,-1.47463807120625,5.62312257453662));
#69855=CARTESIAN_POINT('Ctrl Pts',(24.5981531602776,-3.97965151611398,4.23750383358008));
#69856=CARTESIAN_POINT('Ctrl Pts',(24.6987230702354,-5.51960289416221,1.82429406074521));
#69857=CARTESIAN_POINT('Ctrl Pts',(24.7992929801933,-5.7210553218086,-1.03130545141574));
#69858=CARTESIAN_POINT('Ctrl Pts',(24.899862890151,-4.53515675876486,-3.63681427938567));
#69859=CARTESIAN_POINT('Ctrl Pts',(25.0004328001089,-2.24948658571366,-5.36039877527861));
#69860=CARTESIAN_POINT('Ctrl Pts',(25.1010027100666,0.581682147950543,-5.78409118255149));
#69861=CARTESIAN_POINT('Ctrl Pts',(25.2015726200244,3.27179346146541,-4.80514645716718));
#69862=CARTESIAN_POINT('Ctrl Pts',(25.3021425299822,5.16849767702856,-2.66095785232772));
#69863=CARTESIAN_POINT('Ctrl Pts',(25.40271243994,5.81184565510331,0.128510741072388));
#69864=CARTESIAN_POINT('Ctrl Pts',(25.5032823498978,5.04582606481892,2.88681559038817));
#69865=CARTESIAN_POINT('Ctrl Pts',(25.6038522598556,3.05619799740772,4.94507014408847));
#69866=CARTESIAN_POINT('Ctrl Pts',(25.7044221698135,0.325444546488037,5.80414944470552));
#69867=CARTESIAN_POINT('Ctrl Pts',(25.8049920797712,-2.484228926803,5.25572750135977));
#69868=CARTESIAN_POINT('Ctrl Pts',(25.9055619897291,-4.69147902383981,3.43279616321523));
#69869=CARTESIAN_POINT('Ctrl Pts',(26.0061318996869,-5.76104949615515,0.777414710540404));
#69870=CARTESIAN_POINT('Ctrl Pts',(26.1067018096446,-5.4335704249295,-2.0664891402196));
#69871=CARTESIAN_POINT('Ctrl Pts',(26.2072717196025,-3.78845520303171,-4.40927115336947));
#69872=CARTESIAN_POINT('Ctrl Pts',(26.3078416295602,-1.22464285560959,-5.68280870745432));
#69873=CARTESIAN_POINT('Ctrl Pts',(26.408411539518,1.63614433009017,-5.57827004190617));
#69874=CARTESIAN_POINT('Ctrl Pts',(26.5089814494759,4.100167924183,-4.12100569313063));
#69875=CARTESIAN_POINT('Ctrl Pts',(26.6095513594336,5.56990432620359,-1.66440101125078));
#69876=CARTESIAN_POINT('Ctrl Pts',(26.7101212693915,5.6889437238532,1.19581948309323));
#69877=CARTESIAN_POINT('Ctrl Pts',(26.8106911793493,4.42841916567433,3.76605478218288));
#69878=CARTESIAN_POINT('Ctrl Pts',(26.911261089307,2.09400677192963,5.42302503852111));
#69879=CARTESIAN_POINT('Ctrl Pts',(27.0118309992649,-0.748200461426902,
5.76491639131348));
#69880=CARTESIAN_POINT('Ctrl Pts',(27.1124009092227,-3.40896972695984,4.70882048181766));
#69881=CARTESIAN_POINT('Ctrl Pts',(27.2129708191805,-5.24306676824391,2.51083965896878));
#69882=CARTESIAN_POINT('Ctrl Pts',(27.3135407291383,-5.80572463161107,-0.29601761977724));
#69883=CARTESIAN_POINT('Ctrl Pts',(27.4141106390961,-4.96049926954682,-3.03109088054774));
#69884=CARTESIAN_POINT('Ctrl Pts',(27.5146805490538,-2.91235710475748,-5.03112721203537));
#69885=CARTESIAN_POINT('Ctrl Pts',(27.6152504590117,-0.157970849104978,
-5.81111952554301));
#69886=CARTESIAN_POINT('Ctrl Pts',(27.7158203689695,2.63472320146966,-5.18192035648482));
#69887=CARTESIAN_POINT('Ctrl Pts',(27.8163902789273,4.78849914373318,-3.2961099617247));
#69888=CARTESIAN_POINT('Ctrl Pts',(27.9169601888851,5.7810681657188,-0.610995738632328));
#69889=CARTESIAN_POINT('Ctrl Pts',(28.0175300988429,5.37173313402688,2.22228442511572));
#69890=CARTESIAN_POINT('Ctrl Pts',(28.1181000088007,3.65975744147539,4.51666252877937));
#69891=CARTESIAN_POINT('Ctrl Pts',(28.2186699187585,1.06029371979028,5.71575385728667));
#69892=CARTESIAN_POINT('Ctrl Pts',(28.3192398287163,-1.79629031621274,5.52877979568679));
#69893=CARTESIAN_POINT('Ctrl Pts',(28.4198097386741,-4.21727549683238,4.00108139296507));
#69894=CARTESIAN_POINT('Ctrl Pts',(28.5203796486319,-5.61557499982187,1.50312419669493));
#69895=CARTESIAN_POINT('Ctrl Pts',(28.6209495585897,-5.65210239940256,-1.35933932334132));
#69896=CARTESIAN_POINT('Ctrl Pts',(28.7215194685475,-4.31799983261996,-3.89216422762556));
#69897=CARTESIAN_POINT('Ctrl Pts',(28.8220893785053,-1.93678602348512,-5.48114265719722));
#69898=CARTESIAN_POINT('Ctrl Pts',(28.9226592884631,0.91409672910392,-5.74094871072331));
#69899=CARTESIAN_POINT('Ctrl Pts',(29.0232291984209,3.54331181176593,-4.60857964387231));
#69900=CARTESIAN_POINT('Ctrl Pts',(29.1237991083787,5.31327683025914,-2.35863398057979));
#69901=CARTESIAN_POINT('Ctrl Pts',(29.2243690183365,5.79477679123556,0.463278392623556));
#69902=CARTESIAN_POINT('Ctrl Pts',(29.3249389282943,4.87104836864741,3.17284615441902));
#69903=CARTESIAN_POINT('Ctrl Pts',(29.4255088382521,2.76609490980042,5.11300145504481));
#69904=CARTESIAN_POINT('Ctrl Pts',(29.5260787482099,-0.00963418353934693,
5.81325830424054));
#69905=CARTESIAN_POINT('Ctrl Pts',(29.6266486581677,-2.78302699566422,5.10380501887743));
#69906=CARTESIAN_POINT('Ctrl Pts',(29.7272185681255,-4.88153815704996,3.15668340993825));
#69907=CARTESIAN_POINT('Ctrl Pts',(29.8277884780833,-5.79628051751914,0.444068791452662));
#69908=CARTESIAN_POINT('Ctrl Pts',(29.9283583880411,-5.30542984209442,-2.37623212669306));
#69909=CARTESIAN_POINT('Ctrl Pts',(30.0289282979989,-3.52801699702796,-4.62029879964445));
#69910=CARTESIAN_POINT('Ctrl Pts',(30.1294982079567,-0.895063067200426,
-5.74394699096779));
#69911=CARTESIAN_POINT('Ctrl Pts',(30.2300681179145,1.95494288592725,-5.47469298153573));
#69912=CARTESIAN_POINT('Ctrl Pts',(30.3306380278723,4.33087687208847,-3.87783063685398));
#69913=CARTESIAN_POINT('Ctrl Pts',(30.4312079378301,5.65657694491125,-1.34059770088297));
#69914=CARTESIAN_POINT('Ctrl Pts',(30.5317778477879,5.61056197793671,1.52172902352723));
#69915=CARTESIAN_POINT('Ctrl Pts',(30.6323477577457,4.20399056104516,4.01503776968005));
#69916=CARTESIAN_POINT('Ctrl Pts',(30.7329176677035,1.77795505201581,5.53470331294511));
#69917=CARTESIAN_POINT('Ctrl Pts',(30.8334875776613,-1.07923302661269,5.71220806725234));
#69918=CARTESIAN_POINT('Ctrl Pts',(30.9340574876192,-3.67470802532234,4.50450728248337));
#69919=CARTESIAN_POINT('Ctrl Pts',(31.0346273975769,-5.37906949118538,2.20446735932125));
#69920=CARTESIAN_POINT('Ctrl Pts',(31.1351973075348,-5.77901123589326,-0.63015400080755));
#69921=CARTESIAN_POINT('Ctrl Pts',(31.2357672174925,-4.7775477306356,-3.31196355819516));
#69922=CARTESIAN_POINT('Ctrl Pts',(31.3363371274504,-2.61753301334895,-5.19062480375363));
#69923=CARTESIAN_POINT('Ctrl Pts',(31.4369070374081,0.177231206427325,-5.81056400264058));
#69924=CARTESIAN_POINT('Ctrl Pts',(31.537476947366,2.92901701121071,-5.02144643278732));
#69925=CARTESIAN_POINT('Ctrl Pts',(31.6380468573237,4.97051871215735,-3.01463242558821));
#69926=CARTESIAN_POINT('Ctrl Pts',(31.7386167672815,5.80667390417087,-0.276772650265986));
#69927=CARTESIAN_POINT('Ctrl Pts',(31.8391866772394,5.23471567297435,2.52820425449188));
#69928=CARTESIAN_POINT('Ctrl Pts',(31.9397565871971,3.39334339727493,4.72009380388618));
#69929=CARTESIAN_POINT('Ctrl Pts',(32.040326497155,0.729088268823663,5.76736466903021));
#69930=CARTESIAN_POINT('Ctrl Pts',(32.1408964071127,-2.11197013719727,5.4160545666473));
#69931=CARTESIAN_POINT('Ctrl Pts',(32.2414663170706,-4.44087760299231,3.75135589414753));
#69932=CARTESIAN_POINT('Ctrl Pts',(32.3420362270283,-5.69287607289654,1.17695664659171));
#69933=CARTESIAN_POINT('Ctrl Pts',(32.4426061369862,-5.5643569957143,-1.68285357460456));
#69934=CARTESIAN_POINT('Ctrl Pts',(32.5431760469439,-4.08648613702948,-4.13457325260782));
#69935=CARTESIAN_POINT('Ctrl Pts',(32.6437459569018,-1.61764590787947,-5.58366247601294));
#69936=CARTESIAN_POINT('Ctrl Pts',(32.7443158668595,1.24347206141533,-5.67871835556173));
#69937=CARTESIAN_POINT('Ctrl Pts',(32.8448857768174,3.80304912623336,-4.39668992229039));
#69938=CARTESIAN_POINT('Ctrl Pts',(32.9454556867751,5.44039005171353,-2.04846796766039));
#69939=CARTESIAN_POINT('Ctrl Pts',(33.046025596733,5.75844107289692,0.796505705747263));
#69940=CARTESIAN_POINT('Ctrl Pts',(33.1465955066908,4.68007509093404,3.44832743116613));
#69941=CARTESIAN_POINT('Ctrl Pts',(33.2471654166486,2.46679492816254,5.26393272294638));
#69942=CARTESIAN_POINT('Ctrl Pts',(33.3477353266064,-0.344680881200578,
5.80303886075641));
#69943=CARTESIAN_POINT('Ctrl Pts',(33.4483052365642,-3.07257187358376,4.93491307025526));
#69944=CARTESIAN_POINT('Ctrl Pts',(33.548875146522,-5.05536683158087,2.87007510833188));
#69945=CARTESIAN_POINT('Ctrl Pts',(33.6494450564798,-5.81223968472432,0.109246403280997));
#69946=CARTESIAN_POINT('Ctrl Pts',(33.7500149664376,-5.15964941766476,-2.67807446052305));
#69947=CARTESIAN_POINT('Ctrl Pts',(33.8505848763954,-3.2558486083957,-4.81596457301359));
#69948=CARTESIAN_POINT('Ctrl Pts',(33.9511547863532,-0.562507314318525,
-5.78598742226877));
#69949=CARTESIAN_POINT('Ctrl Pts',(34.051724696311,2.26724151925849,-5.35291330236766));
#69950=CARTESIAN_POINT('Ctrl Pts',(34.1522946062688,4.54718623612184,-3.62176231458366));
#69951=CARTESIAN_POINT('Ctrl Pts',(34.2528645162266,5.72444220507391,-1.01233708322999));
#69952=CARTESIAN_POINT('Ctrl Pts',(34.3534344261844,5.5135258670596,1.84257901935812));
#69953=CARTESIAN_POINT('Ctrl Pts',(34.4540043361422,3.96558425248456,4.25067129589676));
#69954=CARTESIAN_POINT('Ctrl Pts',(34.5545742461,1.45599187037064,5.62797944228023));
#69955=CARTESIAN_POINT('Ctrl Pts',(34.6551441560578,-1.40667728694861,5.64050741863682));
#69956=CARTESIAN_POINT('Ctrl Pts',(34.7557140660156,-3.92822841309095,4.28521720148455));
#69957=CARTESIAN_POINT('Ctrl Pts',(34.8562839759734,-5.49718753059043,1.89076550181013));
#69958=CARTESIAN_POINT('Ctrl Pts',(34.9568538859312,-5.73308340405839,-0.962195204428082));
#69959=CARTESIAN_POINT('Ctrl Pts',(35.057423795889,-4.57871148724481,-3.58182440187771));
#69960=CARTESIAN_POINT('Ctrl Pts',(35.1579937058468,-2.31400597626052,-5.33286426520916));
#69961=CARTESIAN_POINT('Ctrl Pts',(35.2585636158045,0.511843992004246,-5.79068913490987));
#69962=CARTESIAN_POINT('Ctrl Pts',(35.3591335257624,3.21357223281796,-4.84427687418623));
#69963=CARTESIAN_POINT('Ctrl Pts',(35.4597034357202,5.13601197350847,-2.72313164156489));
#69964=CARTESIAN_POINT('Ctrl Pts',(35.560273345678,5.81297323184956,0.0583706699861391));
#69965=CARTESIAN_POINT('Ctrl Pts',(35.6608432556358,5.08029348544121,2.82571814431267));
#69966=CARTESIAN_POINT('Ctrl Pts',(35.7614131655936,3.11564694207568,4.9078314011026));
#69967=CARTESIAN_POINT('Ctrl Pts',(35.8619830755514,0.395458697295045,5.79979976792715));
#69968=CARTESIAN_POINT('Ctrl Pts',(35.9625529855092,-2.42062794115745,5.28532168366335));
#69969=CARTESIAN_POINT('Ctrl Pts',(36.063122895467,-4.64971438762522,3.48915764086767));
#69970=CARTESIAN_POINT('Ctrl Pts',(36.1636928054248,-5.75124909770136,0.846875873728528));
#69971=CARTESIAN_POINT('Ctrl Pts',(36.2642627153826,-5.45811085242508,-2.00077256377473));
#69972=CARTESIAN_POINT('Ctrl Pts',(36.3648326253404,-3.84138542393408,-4.36323537688503));
#69973=CARTESIAN_POINT('Ctrl Pts',(36.4654025352982,-1.29312733691379,-5.66761736709884));
#69974=CARTESIAN_POINT('Ctrl Pts',(36.565972445256,1.56871301614697,-5.59760702463875));
#69975=CARTESIAN_POINT('Ctrl Pts',(36.6665423552138,4.05014181318524,-4.17018179728447));
#69976=CARTESIAN_POINT('Ctrl Pts',(36.7671122651716,5.54941470700435,-1.73149107390076));
#69977=CARTESIAN_POINT('Ctrl Pts',(36.8676821751295,5.70295931147022,1.12708474438672));
#69978=CARTESIAN_POINT('Ctrl Pts',(36.9682520850872,4.47354119217547,3.71234348238731));
#69979=CARTESIAN_POINT('Ctrl Pts',(37.068821995045,2.15929318473071,5.39736212160066));
#69980=CARTESIAN_POINT('Ctrl Pts',(37.1693919050028,-0.678581561229704,
5.77352509252997));
#69981=CARTESIAN_POINT('Ctrl Pts',(37.2699618149606,-3.35190086273439,4.74961319853676));
#69982=CARTESIAN_POINT('Ctrl Pts',(37.3705317249185,-5.21238709043842,2.57392419250163));
#69983=CARTESIAN_POINT('Ctrl Pts',(37.4711016348762,-5.8088739356834,-0.225939214507409));
#69984=CARTESIAN_POINT('Ctrl Pts',(37.5716715448341,-4.99671385197042,-2.97101255649336));
#69985=CARTESIAN_POINT('Ctrl Pts',(37.6722414547918,-2.97285496046918,-4.99561791106246));
#69986=CARTESIAN_POINT('Ctrl Pts',(37.7728113647497,-0.228081300173006,
-5.80879022257005));
#69987=CARTESIAN_POINT('Ctrl Pts',(37.8733812747074,2.57200187907619,-5.21333590547767));
#69988=CARTESIAN_POINT('Ctrl Pts',(37.9739511846653,4.74837681670243,-3.35365211909601));
#69989=CARTESIAN_POINT('Ctrl Pts',(38.074521094623,5.77327446381726,-0.680710580753474));
#69990=CARTESIAN_POINT('Ctrl Pts',(38.1750910045808,5.39815802325663,2.15730268744658));
#69991=CARTESIAN_POINT('Ctrl Pts',(38.2756609145386,3.71399290894551,4.47217191100887));
#69992=CARTESIAN_POINT('Ctrl Pts',(38.3762308244964,1.1291877113267,5.70254329592533));
#69993=CARTESIAN_POINT('Ctrl Pts',(38.4768007344543,-1.72944453425166,5.55005284049271));
#69994=CARTESIAN_POINT('Ctrl Pts',(38.5773706444121,-4.16868796902945,4.05167934888527));
#69995=CARTESIAN_POINT('Ctrl Pts',(38.6779405543699,-5.59702815984374,1.57077710297491));
#69996=CARTESIAN_POINT('Ctrl Pts',(38.7785104643277,-5.6680938399783,-1.29103723823687));
#69997=CARTESIAN_POINT('Ctrl Pts',(38.8790803742854,-4.36465164317584,-3.8397761605381));
#69998=CARTESIAN_POINT('Ctrl Pts',(38.9796502842433,-2.00278518012054,-5.45737266929827));
#69999=CARTESIAN_POINT('Ctrl Pts',(39.080220194201,0.844754965059067,-5.75156100361652));
#70000=CARTESIAN_POINT('Ctrl Pts',(39.1807901041589,3.48744275840115,-4.65100074566642));
#70001=CARTESIAN_POINT('Ctrl Pts',(39.2813600141166,5.28442868492169,-2.42257681060703));
#70002=CARTESIAN_POINT('Ctrl Pts',(39.3819299240745,5.79994520433648,0.39331991560096));
#70003=CARTESIAN_POINT('Ctrl Pts',(39.4824998340322,4.90898000445885,3.11383690085679));
#70004=CARTESIAN_POINT('Ctrl Pts',(39.5830697439901,2.8275913792907,5.07925111813494));
#70005=CARTESIAN_POINT('Ctrl Pts',(39.6836396539479,0.0605142787163216,
5.8129513116304));
#70006=CARTESIAN_POINT('Ctrl Pts',(39.7842095639056,-2.72123748235436,5.13701581601069));
#70007=CARTESIAN_POINT('Ctrl Pts',(39.8847794738635,-4.84309149647335,3.21535840709891));
#70008=CARTESIAN_POINT('Ctrl Pts',(39.9853493838212,-5.79049999176961,0.513979352338406));
#70009=CARTESIAN_POINT('Ctrl Pts',(40.0859192937791,-5.33371722369023,-2.31203925291599));
#70010=CARTESIAN_POINT('Ctrl Pts',(40.1864892037368,-3.58351262028272,-4.57739032960799));
#70011=CARTESIAN_POINT('Ctrl Pts',(40.2870591136947,-0.964309291247043,
-5.73272819171892));
#70012=CARTESIAN_POINT('Ctrl Pts',(40.3876290236525,1.88873821081094,-5.49788440223482));
#70013=CARTESIAN_POINT('Ctrl Pts',(40.4881989336103,4.28376832262728,-3.92980837794532));
#70014=CARTESIAN_POINT('Ctrl Pts',(40.5887688435681,5.63998830379708,-1.40875720489588));
#70015=CARTESIAN_POINT('Ctrl Pts',(40.6893387535259,5.62851597635984,1.45391637764221));
#70016=CARTESIAN_POINT('Ctrl Pts',(40.7899086634837,4.25213336984329,3.964016490175));
#70017=CARTESIAN_POINT('Ctrl Pts',(40.8904785734415,1.84461208149807,5.51284601617945));
#70018=CARTESIAN_POINT('Ctrl Pts',(40.9910484833993,-1.01022604871547,5.7248151288763));
#70019=CARTESIAN_POINT('Ctrl Pts',(41.0916183933571,-3.62008523174703,4.54852150090567));
#70020=CARTESIAN_POINT('Ctrl Pts',(41.1921883033149,-5.3520768623531,2.2692153244632));
#70021=CARTESIAN_POINT('Ctrl Pts',(41.2927582132727,-5.78619446105984,-0.560373614755946));
#70022=CARTESIAN_POINT('Ctrl Pts',(41.3933281232305,-4.81716488388169,-3.25407243478249));
#70023=CARTESIAN_POINT('Ctrl Pts',(41.4938980331883,-2.6799769691159,-5.15866149057317));
#70024=CARTESIAN_POINT('Ctrl Pts',(41.5944679431461,0.107103053659489,-5.81227957562358));
#70025=CARTESIAN_POINT('Ctrl Pts',(41.6950378531039,2.8682106781198,-5.0564248669622));
#70026=CARTESIAN_POINT('Ctrl Pts',(41.7956077630617,4.93377968217404,-3.07439148077804));
#70027=CARTESIAN_POINT('Ctrl Pts',(41.8961776730195,5.80291136044017,-0.346820807029599));
#70028=CARTESIAN_POINT('Ctrl Pts',(41.9967475829773,5.26484202911207,2.46485361387027));
#70029=CARTESIAN_POINT('Ctrl Pts',(42.0973174929351,3.4500530378513,4.67880315522326));
#70030=CARTESIAN_POINT('Ctrl Pts',(42.1978874028929,0.798629154816186,5.75814695908256));
#70031=CARTESIAN_POINT('Ctrl Pts',(42.2984573128507,-2.04646161077897,5.44114508214238));
#70032=CARTESIAN_POINT('Ctrl Pts',(42.3990272228085,-4.39528719741307,3.80467020667639));
#70033=CARTESIAN_POINT('Ctrl Pts',(42.4995971327662,-5.67825942226375,1.24556608126063));
#70034=CARTESIAN_POINT('Ctrl Pts',(42.6001670427242,-5.58425862522408,-1.61558674664179));
#70035=CARTESIAN_POINT('Ctrl Pts',(42.7007369526818,-4.13607991865755,-4.08496117922704));
#70036=CARTESIAN_POINT('Ctrl Pts',(42.8013068626397,-1.68490539227271,-5.56373604230149));
#70037=CARTESIAN_POINT('Ctrl Pts',(42.9018767725975,1.1748572413234,-5.69330970454131));
#70038=CARTESIAN_POINT('Ctrl Pts',(43.0024466825553,3.74971800524932,-4.4422606643941));
#70039=CARTESIAN_POINT('Ctrl Pts',(43.1030165925131,5.41527538076706,-2.11396723715677));
#70040=CARTESIAN_POINT('Ctrl Pts',(43.2035865024709,5.76763313807318,0.726961425327436));
#70041=CARTESIAN_POINT('Ctrl Pts',(43.3041564124287,4.72134482434061,3.39160256795904));
#70042=CARTESIAN_POINT('Ctrl Pts',(43.4047263223865,2.5301344549744,5.23378300744937));
#70043=CARTESIAN_POINT('Ctrl Pts',(43.5052962323444,-0.274631341710833,
5.80677557302366));
#70044=CARTESIAN_POINT('Ctrl Pts',(43.6058661423021,-3.01279927444167,4.97163006077864));
#70045=CARTESIAN_POINT('Ctrl Pts',(43.7064360522599,-5.02036597662438,2.93086853851659));
#70046=CARTESIAN_POINT('Ctrl Pts',(43.8070059622177,-5.81049825115074,0.179373918639988));
#70047=CARTESIAN_POINT('Ctrl Pts',(43.9075758721755,-5.19158970161661,-2.61561872209666));
#70048=CARTESIAN_POINT('Ctrl Pts',(44.0081457821333,-3.31372511850974,-4.77632607432447));
#70049=CARTESIAN_POINT('Ctrl Pts',(44.1087156920912,-0.632285046713879,
-5.77877846512705));
#70050=CARTESIAN_POINT('Ctrl Pts',(44.2092856020489,2.202483604621,-5.37988205267457));
#70051=CARTESIAN_POINT('Ctrl Pts',(44.3098555120068,4.50315187779634,-3.67636887360525));
#70052=CARTESIAN_POINT('Ctrl Pts',(44.4104254219645,5.71180969704834,-1.08133940741041));
#70053=CARTESIAN_POINT('Ctrl Pts',(44.5109953319224,5.53535858165572,1.77591393423347));
#70054=CARTESIAN_POINT('Ctrl Pts',(44.6115652418801,4.01658777520697,4.20250967558343));
#70055=CARTESIAN_POINT('Ctrl Pts',(44.712135151838,1.52379789086441,5.61000043824521));
#70056=CARTESIAN_POINT('Ctrl Pts',(44.8127050617957,-1.33851167028378,5.65707092388173));
#70057=CARTESIAN_POINT('Ctrl Pts',(44.9132749717536,-3.87623330361735,4.33230658024589));
#70058=CARTESIAN_POINT('Ctrl Pts',(45.0138448817113,-5.47397169759653,1.95696162027419));
#70059=CARTESIAN_POINT('Ctrl Pts',(45.1144147916692,-5.74427666706043,-0.892944848005343));
#70060=CARTESIAN_POINT('Ctrl Pts',(45.2149847016269,-4.62159948960023,-3.52631295931618));
#70061=CARTESIAN_POINT('Ctrl Pts',(45.3155546115848,-2.3781884143173,-5.30455321354411));
#70062=CARTESIAN_POINT('Ctrl Pts',(45.4161245215426,0.441931304224746,-5.79644387979909));
#70063=CARTESIAN_POINT('Ctrl Pts',(45.5166944315003,3.15488306191939,-4.88270189494794));
#70064=CARTESIAN_POINT('Ctrl Pts',(45.6172643414582,5.1027783929124,-2.78490890374179));
#70065=CARTESIAN_POINT('Ctrl Pts',(45.717834251416,5.81325435624223,-0.0117779007076735));
#70066=CARTESIAN_POINT('Ctrl Pts',(45.8184041613737,5.11402114239932,2.76420923310936));
#70067=CARTESIAN_POINT('Ctrl Pts',(45.9189740713316,3.1746422038206,4.86987800740792));
#70068=CARTESIAN_POINT('Ctrl Pts',(46.0195439812894,0.465415263638452,5.79460555704065));
#70069=CARTESIAN_POINT('Ctrl Pts',(46.1201138912472,-2.35667447733314,5.3141462472537));
#70070=CARTESIAN_POINT('Ctrl Pts',(46.220683801205,-4.60727268624445,3.54501104707727));
#70071=CARTESIAN_POINT('Ctrl Pts',(46.3212537111628,-5.74061123481401,0.91621371963175));
#70072=CARTESIAN_POINT('Ctrl Pts',(46.4218236211205,-5.48185650062392,-1.93476464612143));
#70073=CARTESIAN_POINT('Ctrl Pts',(46.5223935310784,-3.89375628397183,-4.31656425069105));
#70074=CARTESIAN_POINT('Ctrl Pts',(46.6229634410361,-1.36142352031365,-5.65160074029039));
#70075=CARTESIAN_POINT('Ctrl Pts',(46.723533350994,1.50105327506819,-5.61612891542932));
#70076=CARTESIAN_POINT('Ctrl Pts',(46.8241032609517,3.99952594339569,-4.21875066310145));
#70077=CARTESIAN_POINT('Ctrl Pts',(46.9246731709096,5.52811701335638,-1.79832900659305));
#70078=CARTESIAN_POINT('Ctrl Pts',(47.0252430808674,5.71614446633981,1.05818588596099));
#70079=CARTESIAN_POINT('Ctrl Pts',(47.1258129908252,4.5180118068569,3.65809161208624));
#70080=CARTESIAN_POINT('Ctrl Pts',(47.226382900783,2.22426517344535,5.37091327127076));
#70081=CARTESIAN_POINT('Ctrl Pts',(47.3269528107408,-0.608863849815457,
5.78129308560828));
#70082=CARTESIAN_POINT('Ctrl Pts',(47.4275227206986,-3.29434391362348,4.78971430338867));
#70083=CARTESIAN_POINT('Ctrl Pts',(47.5280926306563,-5.18094841424352,2.63663392572076));
#70084=CARTESIAN_POINT('Ctrl Pts',(47.6286625406143,-5.8111773843185,-0.155827909244348));
#70085=CARTESIAN_POINT('Ctrl Pts',(47.729232450572,-5.03220084112436,-2.91050161035883));
#70086=CARTESIAN_POINT('Ctrl Pts',(47.8298023605298,-3.03291992582039,-4.95938117640456));
#70087=CARTESIAN_POINT('Ctrl Pts',(47.9303722704876,-0.298158539329414,
-5.80561507634972));
#70088=CARTESIAN_POINT('Ctrl Pts',(48.0309421804455,2.50890603628552,-5.24399231792002));
#70089=CARTESIAN_POINT('Ctrl Pts',(48.1315120904031,4.70756305783949,-3.41070593657371));
#70090=CARTESIAN_POINT('Ctrl Pts',(48.2320820003611,5.76464009027266,-0.750326301641742));
#70091=CARTESIAN_POINT('Ctrl Pts',(48.3326519103187,5.42379686318222,2.09200681553594));
#70092=CARTESIAN_POINT('Ctrl Pts',(48.4332218202766,3.76768756572999,4.42703008080563));
#70093=CARTESIAN_POINT('Ctrl Pts',(48.5337917302344,1.19791727692173,5.6885023623944));
#70094=CARTESIAN_POINT('Ctrl Pts',(48.6343616401922,-1.6623469203385,5.57051771792849));
#70095=CARTESIAN_POINT('Ctrl Pts',(48.73493155015,-4.11949342041254,4.10168732212634));
#70096=CARTESIAN_POINT('Ctrl Pts',(48.8355014601078,-5.57766631221463,1.63820128155862));
#70097=CARTESIAN_POINT('Ctrl Pts',(48.9360713700656,-5.68325992471977,-1.22254715957641));
#70098=CARTESIAN_POINT('Ctrl Pts',(49.0366412800234,-4.41066789779351,-3.78682896691783));
#70099=CARTESIAN_POINT('Ctrl Pts',(49.1372111899812,-2.06849270248174,-5.43280800959264));
#70100=CARTESIAN_POINT('Ctrl Pts',(49.2377810999391,0.775290192564016,-5.76133578665817));
#70101=CARTESIAN_POINT('Ctrl Pts',(49.3383510098967,3.43106588330503,-4.69274459498218));
#70102=CARTESIAN_POINT('Ctrl Pts',(49.4389209198547,5.25481105090448,-2.48616687867213));
#70103=CARTESIAN_POINT('Ctrl Pts',(49.5394908298124,5.80426906215165,0.323304165552166));
#70104=CARTESIAN_POINT('Ctrl Pts',(49.6400607397703,4.94619682230831,3.05437422793956));
#70105=CARTESIAN_POINT('Ctrl Pts',(49.740630649728,2.88867611088328,5.04476116934454));
#70106=CARTESIAN_POINT('Ctrl Pts',(49.8412005596858,0.130653929224284,5.81179786985854));
#70107=CARTESIAN_POINT('Ctrl Pts',(49.9417704696436,-2.65905171780094,5.16947858989416));
#70108=CARTESIAN_POINT('Ctrl Pts',(50.0423403796015,-4.80393961224742,3.27356520191584));
#70109=CARTESIAN_POINT('Ctrl Pts',(50.1429102895592,-5.78387628609288,0.583815070451743));
#70110=CARTESIAN_POINT('Ctrl Pts',(50.243480199517,-5.3612279394874,-2.24750971303215));
#70111=CARTESIAN_POINT('Ctrl Pts',(50.3440501094749,-3.63848643265499,-4.53381532582656));
#70112=CARTESIAN_POINT('Ctrl Pts',(50.4446200194326,-1.0334150980172,-5.72067462494628));
#70113=CARTESIAN_POINT('Ctrl Pts',(50.5451899293905,1.82225850829634,-5.52027525203731));
#70114=CARTESIAN_POINT('Ctrl Pts',(50.6457598393482,4.23603599500043,-3.98121388252061));
#70115=CARTESIAN_POINT('Ctrl Pts',(50.7463297493061,5.62257839941823,-1.47671157363573));
#70116=CARTESIAN_POINT('Ctrl Pts',(50.8468996592638,5.64565038205386,1.38589202066021));
#70117=CARTESIAN_POINT('Ctrl Pts',(50.9474695692217,4.29965700697908,3.91241799296163));
#70118=CARTESIAN_POINT('Ctrl Pts',(51.0480394791794,1.91100050897997,5.4901859698914));
#70119=CARTESIAN_POINT('Ctrl Pts',(51.1486093891373,-0.941071967402673,
5.73658857523205));
#70120=CARTESIAN_POINT('Ctrl Pts',(51.249179299095,-3.56493530179192,4.59187338929895));
#70121=CARTESIAN_POINT('Ctrl Pts',(51.3497492090528,-5.32430489429523,2.33363285927715));
#70122=CARTESIAN_POINT('Ctrl Pts',(51.4503191190107,-5.79253513324631,-0.490511630261341));
#70123=CARTESIAN_POINT('Ctrl Pts',(51.5508890289684,-4.85608058876542,-3.19570747170793));
#70124=CARTESIAN_POINT('Ctrl Pts',(51.6514589389262,-2.74203068176238,-5.12594700222191));
#70125=CARTESIAN_POINT('Ctrl Pts',(51.7520288488841,0.036959305149328,-5.81314879725927));
#70126=CARTESIAN_POINT('Ctrl Pts',(51.8525987588419,2.80698669237795,-5.09066701308651));
#70127=CARTESIAN_POINT('Ctrl Pts',(51.9531686687997,4.89632222303964,-3.13370286043244));
#70128=CARTESIAN_POINT('Ctrl Pts',(52.0537385787575,5.79830382950879,-0.41681846170471));
#70129=CARTESIAN_POINT('Ctrl Pts',(52.1543084887152,5.29420174866827,2.4011440551771));
#70130=CARTESIAN_POINT('Ctrl Pts',(52.2548783986731,3.50626030117625,4.63683120565213));
#70131=CARTESIAN_POINT('Ctrl Pts',(52.3554483086308,0.868053748938764,5.74809078027364));
#70132=CARTESIAN_POINT('Ctrl Pts',(52.4560182185887,-1.98065509017138,5.46544328880053));
#70133=CARTESIAN_POINT('Ctrl Pts',(52.5565881285464,-4.34905677491859,3.85743050460308));
#70134=CARTESIAN_POINT('Ctrl Pts',(52.6571580385043,-5.6628159355431,1.31399414362717));
#70135=CARTESIAN_POINT('Ctrl Pts',(52.7577279484621,-5.60334710650831,-1.54808466605653));
#70136=CARTESIAN_POINT('Ctrl Pts',(52.8582978584198,-4.18507142767569,-4.03475427685318));
#70137=CARTESIAN_POINT('Ctrl Pts',(52.9588677683777,-1.75191953024455,-5.54299944875284));
#70138=CARTESIAN_POINT('Ctrl Pts',(53.0594376783355,1.10607134513556,-5.70707202588776));
#70139=CARTESIAN_POINT('Ctrl Pts',(53.1600075882933,3.69584087152237,-4.48718454958579));
#70140=CARTESIAN_POINT('Ctrl Pts',(53.2605774982511,5.38937216792545,-2.1791586826484));
#70141=CARTESIAN_POINT('Ctrl Pts',(53.3611474082089,5.77598535317805,0.657311288835543));
#70142=CARTESIAN_POINT('Ctrl Pts',(53.4617173181667,4.76192706193859,3.33438383883116));
#70143=CARTESIAN_POINT('Ctrl Pts',(53.5622872281245,2.59310555832215,5.2028711778091));
#70144=CARTESIAN_POINT('Ctrl Pts',(53.6628571380823,-0.204541812806597,
5.80966673579904));
#70145=CARTESIAN_POINT('Ctrl Pts',(53.7634270480401,-2.95258796680689,5.00762310982228));
#70146=CARTESIAN_POINT('Ctrl Pts',(53.8639969579978,-4.98463408757047,2.99123519367383));
#70147=CARTESIAN_POINT('Ctrl Pts',(53.9645668679557,-5.8079107192347,0.249475311631604));
#70148=CARTESIAN_POINT('Ctrl Pts',(54.0651367779134,-5.22277402806538,-2.55278210626261));
#70149=CARTESIAN_POINT('Ctrl Pts',(54.1657066878714,-3.37111907823718,-4.73599208528508));
#70150=CARTESIAN_POINT('Ctrl Pts',(54.2662765978291,-0.701970757150338,
-5.77072801277767));
#70151=CARTESIAN_POINT('Ctrl Pts',(54.3668465077869,2.13740507033186,-5.40606745817384));
#70152=CARTESIAN_POINT('Ctrl Pts',(54.4674164177447,4.45846161278591,-3.73044001590026));
#70153=CARTESIAN_POINT('Ctrl Pts',(54.5679863277025,5.69834582588392,-1.15018443868033));
#70154=CARTESIAN_POINT('Ctrl Pts',(54.6685562376603,5.55638456732653,1.70899057466459));
#70155=CARTESIAN_POINT('Ctrl Pts',(54.7691261476182,4.06700779734722,4.15373547526812));
#70156=CARTESIAN_POINT('Ctrl Pts',(54.8696960575759,1.59137933916517,5.59120577878235));
#70157=CARTESIAN_POINT('Ctrl Pts',(54.9702659675337,-1.27014589220361,5.67280824955481));
#70158=CARTESIAN_POINT('Ctrl Pts',(55.0708358774915,-3.82368404225601,4.37876986600632));
#70159=CARTESIAN_POINT('Ctrl Pts',(55.1714057874494,-5.44993865105018,2.02286347478549));
#70160=CARTESIAN_POINT('Ctrl Pts',(55.271975697407,-5.75467287847216,-0.82354625023189));
#70161=CARTESIAN_POINT('Ctrl Pts',(55.372545607365,-4.66373725166594,-3.47032381488753));
#70162=CARTESIAN_POINT('Ctrl Pts',(55.4731155173227,-2.44217762540687,-5.27539828092228));
#70163=CARTESIAN_POINT('Ctrl Pts',(55.5736854272806,0.372273903066788,-5.80150997087913));
#70164=CARTESIAN_POINT('Ctrl Pts',(55.6407320339191,2.18734716132424,-5.21379159096135));
#70165=CARTESIAN_POINT('Ctrl Pts',(55.6742553372383,2.970363104022,-4.72114838740161));
#70166=CARTESIAN_POINT('Ctrl Pts',(55.26731,3.34571636511758,-5.31774159209381));
#70167=CARTESIAN_POINT('Ctrl Pts',(55.2337866966807,2.46375373567184,-5.8726382059394));
#70168=CARTESIAN_POINT('Ctrl Pts',(55.2002633933615,1.44153522376391,-6.20363124162395));
#70169=CARTESIAN_POINT('Ctrl Pts',(55.1667400900422,0.402075493031596,-6.27036202896318));
#70170=CARTESIAN_POINT('Ctrl Pts',(55.1332167867229,-0.637384237700717,
-6.33709281630241));
#70171=CARTESIAN_POINT('Ctrl Pts',(55.0996934834037,-1.69408518725741,-6.13956135529632));
#70172=CARTESIAN_POINT('Ctrl Pts',(55.0661701800844,-2.63948391154636,-5.70193317095775));
#70173=CARTESIAN_POINT('Ctrl Pts',(55.0326468767652,-3.58488263583531,-5.26430498661918));
#70174=CARTESIAN_POINT('Ctrl Pts',(54.9991235734459,-4.41897913485652,-4.58658007894814));
#70175=CARTESIAN_POINT('Ctrl Pts',(54.9656002701266,-5.04082620592946,-3.75084419568217));
#70176=CARTESIAN_POINT('Ctrl Pts',(54.9320769668074,-5.66267327700243,-2.91510831241616));
#70177=CARTESIAN_POINT('Ctrl Pts',(54.898553663488,-6.07227092012711,-1.92136145355521));
#70178=CARTESIAN_POINT('Ctrl Pts',(54.8650303601688,-6.21986269011626,-0.890138111038006));
#70179=CARTESIAN_POINT('Ctrl Pts',(54.8554530504693,-6.26202834654978,-0.595526770785087));
#70180=CARTESIAN_POINT('Ctrl Pts',(54.8458757407699,-6.28280923827804,-0.297856622058228));
#70181=CARTESIAN_POINT('Ctrl Pts',(54.8362984310704,-6.28252994889952,-0.000148679754663761));
#70182=CARTESIAN_POINT('Origin',(37.,0.,0.));
#70183=CARTESIAN_POINT('Origin',(0.6,7.15372402116488,-1.00753790450219));
#70184=CARTESIAN_POINT('',(17.4,7.09390928188606,-1.04180185273915));
#70185=CARTESIAN_POINT('',(0.600000000000001,7.09390928188606,-1.04180185273915));
#70186=CARTESIAN_POINT('',(9.,7.09390928188606,-1.04180185273915));
#70187=CARTESIAN_POINT('',(17.4,6.81486965084448,-1.20164538945516));
#70188=CARTESIAN_POINT('',(17.4,7.15372402116488,-1.00753790450219));
#70189=CARTESIAN_POINT('',(0.6,6.81486965084448,-1.20164538945516));
#70190=CARTESIAN_POINT('',(0.6,6.81486965084448,-1.20164538945516));
#70191=CARTESIAN_POINT('',(0.6,7.15372402116488,-1.00753790450219));
#70192=CARTESIAN_POINT('Origin',(0.6,6.96259081379631,-1.2276926161052));
#70193=CARTESIAN_POINT('',(0.600000000000001,7.02241142370379,-1.4472863559899));
#70194=CARTESIAN_POINT('Origin',(0.600000000000001,0.,0.));
#70195=CARTESIAN_POINT('',(0.6,6.81486965084448,-1.20164538945516));
#70196=CARTESIAN_POINT('Origin',(0.6,6.81486965084448,-1.20164538945516));
#70197=CARTESIAN_POINT('',(17.4,7.02241142370379,-1.4472863559899));
#70198=CARTESIAN_POINT('',(9.,7.02241142370379,-1.4472863559899));
#70199=CARTESIAN_POINT('',(17.4,6.81486965084448,-1.20164538945516));
#70200=CARTESIAN_POINT('Origin',(17.4,6.96259081379631,-1.2276926161052));
#70201=CARTESIAN_POINT('Origin',(17.4,0.,0.));
#70202=CARTESIAN_POINT('Origin',(0.6,6.87008575790567,-2.23446227961486));
#70203=CARTESIAN_POINT('',(17.4,6.80522986674848,-2.25781896101404));
#70204=CARTESIAN_POINT('',(0.600000000000001,6.80522986674848,-2.25781896101404));
#70205=CARTESIAN_POINT('',(9.,6.80522986674848,-2.25781896101404));
#70206=CARTESIAN_POINT('',(17.4,6.50267293583848,-2.36677939181363));
#70207=CARTESIAN_POINT('',(17.4,6.87008575790567,-2.23446227961486));
#70208=CARTESIAN_POINT('',(0.6,6.50267293583848,-2.36677939181363));
#70209=CARTESIAN_POINT('',(0.6,6.50267293583848,-2.36677939181363));
#70210=CARTESIAN_POINT('',(0.6,6.87008575790567,-2.23446227961486));
#70211=CARTESIAN_POINT('Origin',(0.6,6.64362682895637,-2.41808241331248));
#70212=CARTESIAN_POINT('',(0.600000000000001,6.66440657662513,-2.64472777076124));
#70213=CARTESIAN_POINT('Origin',(0.600000000000001,0.,0.));
#70214=CARTESIAN_POINT('',(0.6,6.50267293583848,-2.36677939181363));
#70215=CARTESIAN_POINT('Origin',(0.6,6.50267293583848,-2.36677939181363));
#70216=CARTESIAN_POINT('',(17.4,6.66440657662513,-2.64472777076124));
#70217=CARTESIAN_POINT('',(9.,6.66440657662513,-2.64472777076124));
#70218=CARTESIAN_POINT('',(17.4,6.50267293583848,-2.36677939181363));
#70219=CARTESIAN_POINT('Origin',(17.4,6.64362682895637,-2.41808241331248));
#70220=CARTESIAN_POINT('Origin',(17.4,0.,0.));
#70221=CARTESIAN_POINT('Origin',(0.6,6.37770341532365,-3.39349364905389));
#70222=CARTESIAN_POINT('',(17.4,6.3097769857222,-3.40523338267004));
#70223=CARTESIAN_POINT('',(0.600000000000001,6.3097769857222,-3.40523338267004));
#70224=CARTESIAN_POINT('',(9.,6.3097769857222,-3.40523338267003));
#70225=CARTESIAN_POINT('',(17.4,5.99289579418831,-3.46));
#70226=CARTESIAN_POINT('',(17.4,6.37770341532365,-3.39349364905389));
#70227=CARTESIAN_POINT('',(0.6,5.99289579418831,-3.46));
#70228=CARTESIAN_POINT('',(0.6,5.99289579418831,-3.46));
#70229=CARTESIAN_POINT('',(0.6,6.37770341532365,-3.39349364905389));
#70230=CARTESIAN_POINT('Origin',(0.6,6.12279960475598,-3.535));
#70231=CARTESIAN_POINT('',(0.600000000000001,6.10390710806817,-3.76181047051482));
#70232=CARTESIAN_POINT('Origin',(0.600000000000001,0.,0.));
#70233=CARTESIAN_POINT('',(0.6,5.99289579418831,-3.46));
#70234=CARTESIAN_POINT('Origin',(0.6,5.99289579418831,-3.46));
#70235=CARTESIAN_POINT('',(17.4,6.10390710806817,-3.76181047051482));
#70236=CARTESIAN_POINT('',(9.,6.10390710806817,-3.76181047051482));
#70237=CARTESIAN_POINT('',(17.4,5.99289579418831,-3.46));
#70238=CARTESIAN_POINT('Origin',(17.4,6.12279960475598,-3.535));
#70239=CARTESIAN_POINT('Origin',(17.4,0.,0.));
#70240=CARTESIAN_POINT('Origin',(0.6,5.69153778174065,-4.44941543115707));
#70241=CARTESIAN_POINT('',(17.4,5.62260472388598,-4.44918151112483));
#70242=CARTESIAN_POINT('',(0.600000000000001,5.62260472388598,-4.44918151112483));
#70243=CARTESIAN_POINT('',(9.,5.62260472388598,-4.44918151112483));
#70244=CARTESIAN_POINT('',(17.4,5.30102754638333,-4.44809025903085));
#70245=CARTESIAN_POINT('',(17.4,5.69153778174065,-4.44941543115707));
#70246=CARTESIAN_POINT('',(0.6,5.30102754638333,-4.44809025903085));
#70247=CARTESIAN_POINT('',(0.6,5.30102754638333,-4.44809025903085));
#70248=CARTESIAN_POINT('',(0.6,5.69153778174065,-4.44941543115707));
#70249=CARTESIAN_POINT('Origin',(0.6,5.41593421285117,-4.54450840048383));
#70250=CARTESIAN_POINT('',(0.599999999999999,5.35794351075858,-4.76459246268976));
#70251=CARTESIAN_POINT('Origin',(0.600000000000001,0.,0.));
#70252=CARTESIAN_POINT('',(0.6,5.30102754638333,-4.44809025903085));
#70253=CARTESIAN_POINT('Origin',(0.6,5.30102754638333,-4.44809025903085));
#70254=CARTESIAN_POINT('',(17.4,5.35794351075858,-4.76459246268976));
#70255=CARTESIAN_POINT('',(9.,5.35794351075858,-4.76459246268976));
#70256=CARTESIAN_POINT('',(17.4,5.30102754638333,-4.44809025903085));
#70257=CARTESIAN_POINT('Origin',(17.4,5.41593421285117,-4.54450840048383));
#70258=CARTESIAN_POINT('Origin',(17.4,0.,0.));
#70259=CARTESIAN_POINT('Origin',(0.6,4.83243765271656,-5.37014397689739));
#70260=CARTESIAN_POINT('',(17.4,4.76459246268975,-5.35794351075858));
#70261=CARTESIAN_POINT('',(0.600000000000001,4.76459246268975,-5.35794351075858));
#70262=CARTESIAN_POINT('',(9.,4.76459246268975,-5.35794351075858));
#70263=CARTESIAN_POINT('',(17.4,4.44809025903085,-5.30102754638333));
#70264=CARTESIAN_POINT('',(17.4,4.83243765271656,-5.37014397689739));
#70265=CARTESIAN_POINT('',(0.6,4.44809025903085,-5.30102754638333));
#70266=CARTESIAN_POINT('',(0.6,4.44809025903085,-5.30102754638333));
#70267=CARTESIAN_POINT('',(0.6,4.83243765271656,-5.37014397689739));
#70268=CARTESIAN_POINT('Origin',(0.6,4.54450840048383,-5.41593421285118));
#70269=CARTESIAN_POINT('',(0.600000000000001,4.44918151112483,-5.62260472388598));
#70270=CARTESIAN_POINT('Origin',(0.600000000000001,0.,0.));
#70271=CARTESIAN_POINT('',(0.6,4.44809025903085,-5.30102754638333));
#70272=CARTESIAN_POINT('Origin',(0.6,4.44809025903085,-5.30102754638333));
#70273=CARTESIAN_POINT('',(17.4,4.44918151112483,-5.62260472388598));
#70274=CARTESIAN_POINT('',(9.,4.44918151112483,-5.62260472388598));
#70275=CARTESIAN_POINT('',(17.4,4.44809025903085,-5.30102754638333));
#70276=CARTESIAN_POINT('Origin',(17.4,4.54450840048383,-5.41593421285118));
#70277=CARTESIAN_POINT('Origin',(17.4,0.,0.));
#70278=CARTESIAN_POINT('Origin',(0.6,3.82650635094611,-6.12770341532365));
#70279=CARTESIAN_POINT('',(17.4,3.76181047051482,-6.10390710806817));
#70280=CARTESIAN_POINT('',(0.599999999999999,3.76181047051482,-6.10390710806817));
#70281=CARTESIAN_POINT('',(9.,3.76181047051482,-6.10390710806817));
#70282=CARTESIAN_POINT('',(17.4,3.46,-5.99289579418831));
#70283=CARTESIAN_POINT('',(17.4,3.82650635094611,-6.12770341532365));
#70284=CARTESIAN_POINT('',(0.6,3.46,-5.99289579418831));
#70285=CARTESIAN_POINT('',(0.6,3.46,-5.99289579418831));
#70286=CARTESIAN_POINT('',(0.6,3.82650635094611,-6.12770341532365));
#70287=CARTESIAN_POINT('Origin',(0.6,3.535,-6.12279960475598));
#70288=CARTESIAN_POINT('',(0.599999999999999,3.40523338267003,-6.30977698572221));
#70289=CARTESIAN_POINT('Origin',(0.600000000000001,0.,0.));
#70290=CARTESIAN_POINT('',(0.6,3.46,-5.99289579418831));
#70291=CARTESIAN_POINT('Origin',(0.6,3.46,-5.99289579418831));
#70292=CARTESIAN_POINT('',(17.4,3.40523338267003,-6.30977698572221));
#70293=CARTESIAN_POINT('',(9.,3.40523338267003,-6.30977698572221));
#70294=CARTESIAN_POINT('',(17.4,3.46,-5.99289579418831));
#70295=CARTESIAN_POINT('Origin',(17.4,3.535,-6.12279960475598));
#70296=CARTESIAN_POINT('Origin',(17.4,0.,0.));
#70297=CARTESIAN_POINT('Origin',(0.6,2.7043085900078,-6.69907568624284));
#70298=CARTESIAN_POINT('',(17.4,2.64472777076123,-6.66440657662513));
#70299=CARTESIAN_POINT('',(0.599999999999999,2.64472777076123,-6.66440657662513));
#70300=CARTESIAN_POINT('',(9.,2.64472777076123,-6.66440657662513));
#70301=CARTESIAN_POINT('',(17.4,2.36677939181362,-6.50267293583849));
#70302=CARTESIAN_POINT('',(17.4,2.7043085900078,-6.69907568624284));
#70303=CARTESIAN_POINT('',(0.6,2.36677939181362,-6.50267293583849));
#70304=CARTESIAN_POINT('',(0.6,2.36677939181362,-6.50267293583849));
#70305=CARTESIAN_POINT('',(0.6,2.7043085900078,-6.69907568624284));
#70306=CARTESIAN_POINT('Origin',(0.6,2.41808241331247,-6.64362682895637));
#70307=CARTESIAN_POINT('',(0.600000000000001,2.25781896101403,-6.80522986674848));
#70308=CARTESIAN_POINT('Origin',(0.600000000000001,0.,0.));
#70309=CARTESIAN_POINT('',(0.6,2.36677939181362,-6.50267293583849));
#70310=CARTESIAN_POINT('Origin',(0.6,2.36677939181362,-6.50267293583849));
#70311=CARTESIAN_POINT('',(17.4,2.25781896101403,-6.80522986674848));
#70312=CARTESIAN_POINT('',(9.,2.25781896101403,-6.80522986674848));
#70313=CARTESIAN_POINT('',(17.4,2.36677939181362,-6.50267293583849));
#70314=CARTESIAN_POINT('Origin',(17.4,2.41808241331247,-6.64362682895637));
#70315=CARTESIAN_POINT('Origin',(17.4,0.,0.));
#70316=CARTESIAN_POINT('Origin',(0.6,1.49994178100829,-7.06689993233141));
#70317=CARTESIAN_POINT('',(17.4,1.44728635598989,-7.02241142370379));
#70318=CARTESIAN_POINT('',(0.600000000000001,1.44728635598989,-7.02241142370379));
#70319=CARTESIAN_POINT('',(9.,1.44728635598989,-7.02241142370379));
#70320=CARTESIAN_POINT('',(17.4,1.20164538945516,-6.81486965084448));
#70321=CARTESIAN_POINT('',(17.4,1.49994178100829,-7.06689993233141));
#70322=CARTESIAN_POINT('',(0.6,1.20164538945516,-6.81486965084448));
#70323=CARTESIAN_POINT('',(0.6,1.20164538945516,-6.81486965084448));
#70324=CARTESIAN_POINT('',(0.6,1.49994178100829,-7.06689993233141));
#70325=CARTESIAN_POINT('Origin',(0.6,1.22769261610519,-6.96259081379631));
#70326=CARTESIAN_POINT('',(0.600000000000001,1.04180185273915,-7.09390928188606));
#70327=CARTESIAN_POINT('Origin',(0.600000000000001,0.,0.));
#70328=CARTESIAN_POINT('',(0.6,1.20164538945516,-6.81486965084448));
#70329=CARTESIAN_POINT('Origin',(0.6,1.20164538945516,-6.81486965084448));
#70330=CARTESIAN_POINT('',(17.4,1.04180185273915,-7.09390928188606));
#70331=CARTESIAN_POINT('',(9.,1.04180185273915,-7.09390928188607));
#70332=CARTESIAN_POINT('',(17.4,1.20164538945516,-6.81486965084448));
#70333=CARTESIAN_POINT('Origin',(17.4,1.22769261610519,-6.96259081379631));
#70334=CARTESIAN_POINT('Origin',(17.4,0.,0.));
#70335=CARTESIAN_POINT('Origin',(0.6,0.249999999999999,-7.22));
#70336=CARTESIAN_POINT('',(17.4,0.205869877654039,-7.16704385318485));
#70337=CARTESIAN_POINT('',(0.599999999999999,0.205869877654039,-7.16704385318485));
#70338=CARTESIAN_POINT('',(9.,0.205869877654039,-7.16704385318485));
#70339=CARTESIAN_POINT('',(17.4,-1.27118337751495E-15,-6.92));
#70340=CARTESIAN_POINT('',(17.4,0.249999999999999,-7.22));
#70341=CARTESIAN_POINT('',(0.6,-1.27118337751495E-15,-6.92));
#70342=CARTESIAN_POINT('',(0.6,-1.27118337751495E-15,-6.92));
#70343=CARTESIAN_POINT('',(0.6,0.249999999999999,-7.22));
#70344=CARTESIAN_POINT('Origin',(0.6,-1.29873793049577E-15,-7.07));
#70345=CARTESIAN_POINT('',(0.600000000000001,-0.20586987765404,-7.16704385318485));
#70346=CARTESIAN_POINT('Origin',(0.600000000000001,0.,0.));
#70347=CARTESIAN_POINT('',(0.6,-1.27118337751495E-15,-6.92));
#70348=CARTESIAN_POINT('Origin',(0.6,-1.27118337751495E-15,-6.92));
#70349=CARTESIAN_POINT('',(17.4,-0.20586987765404,-7.16704385318485));
#70350=CARTESIAN_POINT('',(9.,-0.20586987765404,-7.16704385318485));
#70351=CARTESIAN_POINT('',(17.4,-1.27118337751495E-15,-6.92));
#70352=CARTESIAN_POINT('Origin',(17.4,-1.29873793049577E-15,-7.07));
#70353=CARTESIAN_POINT('Origin',(17.4,0.,0.));
#70354=CARTESIAN_POINT('Origin',(0.6,-1.00753790450219,-7.15372402116488));
#70355=CARTESIAN_POINT('',(17.4,-1.04180185273915,-7.09390928188606));
#70356=CARTESIAN_POINT('',(0.600000000000001,-1.04180185273915,-7.09390928188606));
#70357=CARTESIAN_POINT('',(9.,-1.04180185273915,-7.09390928188606));
#70358=CARTESIAN_POINT('',(17.4,-1.20164538945516,-6.81486965084448));
#70359=CARTESIAN_POINT('',(17.4,-1.00753790450219,-7.15372402116488));
#70360=CARTESIAN_POINT('',(0.6,-1.20164538945516,-6.81486965084448));
#70361=CARTESIAN_POINT('',(0.6,-1.20164538945516,-6.81486965084448));
#70362=CARTESIAN_POINT('',(0.6,-1.00753790450219,-7.15372402116488));
#70363=CARTESIAN_POINT('Origin',(0.6,-1.2276926161052,-6.96259081379631));
#70364=CARTESIAN_POINT('',(0.600000000000001,-1.4472863559899,-7.02241142370379));
#70365=CARTESIAN_POINT('Origin',(0.600000000000001,0.,0.));
#70366=CARTESIAN_POINT('',(0.6,-1.20164538945516,-6.81486965084448));
#70367=CARTESIAN_POINT('Origin',(0.6,-1.20164538945516,-6.81486965084448));
#70368=CARTESIAN_POINT('',(17.4,-1.4472863559899,-7.02241142370379));
#70369=CARTESIAN_POINT('',(9.,-1.4472863559899,-7.02241142370379));
#70370=CARTESIAN_POINT('',(17.4,-1.20164538945516,-6.81486965084448));
#70371=CARTESIAN_POINT('Origin',(17.4,-1.2276926161052,-6.96259081379631));
#70372=CARTESIAN_POINT('Origin',(17.4,0.,0.));
#70373=CARTESIAN_POINT('Origin',(0.6,-2.23446227961486,-6.87008575790567));
#70374=CARTESIAN_POINT('',(17.4,-2.25781896101404,-6.80522986674848));
#70375=CARTESIAN_POINT('',(0.600000000000001,-2.25781896101404,-6.80522986674848));
#70376=CARTESIAN_POINT('',(9.,-2.25781896101404,-6.80522986674847));
#70377=CARTESIAN_POINT('',(17.4,-2.36677939181363,-6.50267293583848));
#70378=CARTESIAN_POINT('',(17.4,-2.23446227961486,-6.87008575790567));
#70379=CARTESIAN_POINT('',(0.6,-2.36677939181363,-6.50267293583848));
#70380=CARTESIAN_POINT('',(0.6,-2.36677939181363,-6.50267293583848));
#70381=CARTESIAN_POINT('',(0.6,-2.23446227961486,-6.87008575790567));
#70382=CARTESIAN_POINT('Origin',(0.6,-2.41808241331248,-6.64362682895637));
#70383=CARTESIAN_POINT('',(0.600000000000001,-2.64472777076124,-6.66440657662513));
#70384=CARTESIAN_POINT('Origin',(0.600000000000001,0.,0.));
#70385=CARTESIAN_POINT('',(0.6,-2.36677939181363,-6.50267293583848));
#70386=CARTESIAN_POINT('Origin',(0.6,-2.36677939181363,-6.50267293583848));
#70387=CARTESIAN_POINT('',(17.4,-2.64472777076124,-6.66440657662513));
#70388=CARTESIAN_POINT('',(9.,-2.64472777076124,-6.66440657662513));
#70389=CARTESIAN_POINT('',(17.4,-2.36677939181363,-6.50267293583848));
#70390=CARTESIAN_POINT('Origin',(17.4,-2.41808241331248,-6.64362682895637));
#70391=CARTESIAN_POINT('Origin',(17.4,0.,0.));
#70392=CARTESIAN_POINT('Origin',(0.6,-3.39349364905389,-6.37770341532365));
#70393=CARTESIAN_POINT('',(17.4,-3.40523338267004,-6.3097769857222));
#70394=CARTESIAN_POINT('',(0.600000000000001,-3.40523338267004,-6.3097769857222));
#70395=CARTESIAN_POINT('',(9.,-3.40523338267003,-6.3097769857222));
#70396=CARTESIAN_POINT('',(17.4,-3.46,-5.99289579418831));
#70397=CARTESIAN_POINT('',(17.4,-3.39349364905389,-6.37770341532365));
#70398=CARTESIAN_POINT('',(0.6,-3.46,-5.99289579418831));
#70399=CARTESIAN_POINT('',(0.6,-3.46,-5.99289579418831));
#70400=CARTESIAN_POINT('',(0.6,-3.39349364905389,-6.37770341532365));
#70401=CARTESIAN_POINT('Origin',(0.6,-3.535,-6.12279960475598));
#70402=CARTESIAN_POINT('',(0.600000000000001,-3.76181047051482,-6.10390710806817));
#70403=CARTESIAN_POINT('Origin',(0.600000000000001,0.,0.));
#70404=CARTESIAN_POINT('',(0.6,-3.46,-5.99289579418831));
#70405=CARTESIAN_POINT('Origin',(0.6,-3.46,-5.99289579418831));
#70406=CARTESIAN_POINT('',(17.4,-3.76181047051482,-6.10390710806817));
#70407=CARTESIAN_POINT('',(9.,-3.76181047051482,-6.10390710806817));
#70408=CARTESIAN_POINT('',(17.4,-3.46,-5.99289579418831));
#70409=CARTESIAN_POINT('Origin',(17.4,-3.535,-6.12279960475598));
#70410=CARTESIAN_POINT('Origin',(17.4,0.,0.));
#70411=CARTESIAN_POINT('Origin',(0.6,-4.44941543115707,-5.69153778174066));
#70412=CARTESIAN_POINT('',(17.4,-4.44918151112483,-5.62260472388598));
#70413=CARTESIAN_POINT('',(0.599999999999999,-4.44918151112483,-5.62260472388598));
#70414=CARTESIAN_POINT('',(9.,-4.44918151112483,-5.62260472388598));
#70415=CARTESIAN_POINT('',(17.4,-4.44809025903085,-5.30102754638333));
#70416=CARTESIAN_POINT('',(17.4,-4.44941543115707,-5.69153778174066));
#70417=CARTESIAN_POINT('',(0.6,-4.44809025903085,-5.30102754638333));
#70418=CARTESIAN_POINT('',(0.6,-4.44809025903085,-5.30102754638333));
#70419=CARTESIAN_POINT('',(0.6,-4.44941543115707,-5.69153778174066));
#70420=CARTESIAN_POINT('Origin',(0.6,-4.54450840048383,-5.41593421285117));
#70421=CARTESIAN_POINT('',(0.599999999999999,-4.76459246268976,-5.35794351075858));
#70422=CARTESIAN_POINT('Origin',(0.600000000000001,0.,0.));
#70423=CARTESIAN_POINT('',(0.6,-4.44809025903085,-5.30102754638333));
#70424=CARTESIAN_POINT('Origin',(0.6,-4.44809025903085,-5.30102754638333));
#70425=CARTESIAN_POINT('',(17.4,-4.76459246268976,-5.35794351075858));
#70426=CARTESIAN_POINT('',(9.,-4.76459246268976,-5.35794351075858));
#70427=CARTESIAN_POINT('',(17.4,-4.44809025903085,-5.30102754638333));
#70428=CARTESIAN_POINT('Origin',(17.4,-4.54450840048383,-5.41593421285117));
#70429=CARTESIAN_POINT('Origin',(17.4,0.,0.));
#70430=CARTESIAN_POINT('Origin',(0.6,-5.37014397689739,-4.83243765271656));
#70431=CARTESIAN_POINT('',(17.4,-5.35794351075858,-4.76459246268975));
#70432=CARTESIAN_POINT('',(0.599999999999999,-5.35794351075858,-4.76459246268975));
#70433=CARTESIAN_POINT('',(9.,-5.35794351075858,-4.76459246268975));
#70434=CARTESIAN_POINT('',(17.4,-5.30102754638333,-4.44809025903085));
#70435=CARTESIAN_POINT('',(17.4,-5.37014397689739,-4.83243765271656));
#70436=CARTESIAN_POINT('',(0.6,-5.30102754638333,-4.44809025903085));
#70437=CARTESIAN_POINT('',(0.6,-5.30102754638333,-4.44809025903085));
#70438=CARTESIAN_POINT('',(0.6,-5.37014397689739,-4.83243765271656));
#70439=CARTESIAN_POINT('Origin',(0.6,-5.41593421285118,-4.54450840048383));
#70440=CARTESIAN_POINT('',(0.599999999999999,-5.62260472388598,-4.44918151112483));
#70441=CARTESIAN_POINT('Origin',(0.600000000000001,0.,0.));
#70442=CARTESIAN_POINT('',(0.6,-5.30102754638333,-4.44809025903085));
#70443=CARTESIAN_POINT('Origin',(0.6,-5.30102754638333,-4.44809025903085));
#70444=CARTESIAN_POINT('',(17.4,-5.62260472388598,-4.44918151112483));
#70445=CARTESIAN_POINT('',(9.,-5.62260472388598,-4.44918151112483));
#70446=CARTESIAN_POINT('',(17.4,-5.30102754638333,-4.44809025903085));
#70447=CARTESIAN_POINT('Origin',(17.4,-5.41593421285118,-4.54450840048383));
#70448=CARTESIAN_POINT('Origin',(17.4,0.,0.));
#70449=CARTESIAN_POINT('Origin',(0.6,-6.12770341532365,-3.82650635094611));
#70450=CARTESIAN_POINT('',(17.4,-6.10390710806817,-3.76181047051481));
#70451=CARTESIAN_POINT('',(0.599999999999999,-6.10390710806817,-3.76181047051481));
#70452=CARTESIAN_POINT('',(9.,-6.10390710806817,-3.76181047051481));
#70453=CARTESIAN_POINT('',(17.4,-5.99289579418832,-3.46));
#70454=CARTESIAN_POINT('',(17.4,-6.12770341532365,-3.82650635094611));
#70455=CARTESIAN_POINT('',(0.6,-5.99289579418832,-3.46));
#70456=CARTESIAN_POINT('',(0.6,-5.99289579418832,-3.46));
#70457=CARTESIAN_POINT('',(0.6,-6.12770341532365,-3.82650635094611));
#70458=CARTESIAN_POINT('Origin',(0.6,-6.12279960475598,-3.535));
#70459=CARTESIAN_POINT('',(0.600000000000001,-6.30977698572221,-3.40523338267003));
#70460=CARTESIAN_POINT('Origin',(0.600000000000001,0.,0.));
#70461=CARTESIAN_POINT('',(0.6,-5.99289579418832,-3.46));
#70462=CARTESIAN_POINT('Origin',(0.6,-5.99289579418832,-3.46));
#70463=CARTESIAN_POINT('',(17.4,-6.30977698572221,-3.40523338267003));
#70464=CARTESIAN_POINT('',(9.,-6.30977698572221,-3.40523338267003));
#70465=CARTESIAN_POINT('',(17.4,-5.99289579418832,-3.46));
#70466=CARTESIAN_POINT('Origin',(17.4,-6.12279960475598,-3.535));
#70467=CARTESIAN_POINT('Origin',(17.4,0.,0.));
#70468=CARTESIAN_POINT('Origin',(0.6,-6.69907568624284,-2.7043085900078));
#70469=CARTESIAN_POINT('',(17.4,-6.66440657662513,-2.64472777076123));
#70470=CARTESIAN_POINT('',(0.600000000000001,-6.66440657662513,-2.64472777076123));
#70471=CARTESIAN_POINT('',(9.,-6.66440657662513,-2.64472777076123));
#70472=CARTESIAN_POINT('',(17.4,-6.50267293583849,-2.36677939181363));
#70473=CARTESIAN_POINT('',(17.4,-6.69907568624284,-2.7043085900078));
#70474=CARTESIAN_POINT('',(0.6,-6.50267293583849,-2.36677939181363));
#70475=CARTESIAN_POINT('',(0.6,-6.50267293583849,-2.36677939181363));
#70476=CARTESIAN_POINT('',(0.6,-6.69907568624284,-2.7043085900078));
#70477=CARTESIAN_POINT('Origin',(0.6,-6.64362682895637,-2.41808241331248));
#70478=CARTESIAN_POINT('',(0.599999999999999,-6.80522986674848,-2.25781896101403));
#70479=CARTESIAN_POINT('Origin',(0.600000000000001,0.,0.));
#70480=CARTESIAN_POINT('',(0.6,-6.50267293583849,-2.36677939181363));
#70481=CARTESIAN_POINT('Origin',(0.6,-6.50267293583849,-2.36677939181363));
#70482=CARTESIAN_POINT('',(17.4,-6.80522986674848,-2.25781896101403));
#70483=CARTESIAN_POINT('',(9.,-6.80522986674848,-2.25781896101403));
#70484=CARTESIAN_POINT('',(17.4,-6.50267293583849,-2.36677939181363));
#70485=CARTESIAN_POINT('Origin',(17.4,-6.64362682895637,-2.41808241331248));
#70486=CARTESIAN_POINT('Origin',(17.4,0.,0.));
#70487=CARTESIAN_POINT('Origin',(0.6,-7.06689993233141,-1.49994178100829));
#70488=CARTESIAN_POINT('',(17.4,-7.02241142370379,-1.44728635598989));
#70489=CARTESIAN_POINT('',(0.600000000000001,-7.02241142370379,-1.44728635598989));
#70490=CARTESIAN_POINT('',(9.,-7.02241142370379,-1.44728635598989));
#70491=CARTESIAN_POINT('',(17.4,-6.81486965084448,-1.20164538945516));
#70492=CARTESIAN_POINT('',(17.4,-7.06689993233141,-1.49994178100829));
#70493=CARTESIAN_POINT('',(0.6,-6.81486965084448,-1.20164538945516));
#70494=CARTESIAN_POINT('',(0.6,-6.81486965084448,-1.20164538945516));
#70495=CARTESIAN_POINT('',(0.6,-7.06689993233141,-1.49994178100829));
#70496=CARTESIAN_POINT('Origin',(0.6,-6.96259081379631,-1.2276926161052));
#70497=CARTESIAN_POINT('',(0.599999999999999,-7.09390928188607,-1.04180185273915));
#70498=CARTESIAN_POINT('Origin',(0.600000000000001,0.,0.));
#70499=CARTESIAN_POINT('',(0.6,-6.81486965084448,-1.20164538945516));
#70500=CARTESIAN_POINT('Origin',(0.6,-6.81486965084448,-1.20164538945516));
#70501=CARTESIAN_POINT('',(17.4,-7.09390928188607,-1.04180185273915));
#70502=CARTESIAN_POINT('',(9.,-7.09390928188607,-1.04180185273915));
#70503=CARTESIAN_POINT('',(17.4,-6.81486965084448,-1.20164538945516));
#70504=CARTESIAN_POINT('Origin',(17.4,-6.96259081379631,-1.2276926161052));
#70505=CARTESIAN_POINT('Origin',(17.4,0.,0.));
#70506=CARTESIAN_POINT('Origin',(0.6,-7.22,-0.249999999999999));
#70507=CARTESIAN_POINT('',(17.4,-7.16704385318485,-0.205869877654039));
#70508=CARTESIAN_POINT('',(0.599999999999999,-7.16704385318485,-0.205869877654039));
#70509=CARTESIAN_POINT('',(9.,-7.16704385318485,-0.205869877654039));
#70510=CARTESIAN_POINT('',(17.4,-6.92,8.47455585009968E-16));
#70511=CARTESIAN_POINT('',(17.4,-7.22,-0.249999999999999));
#70512=CARTESIAN_POINT('',(0.6,-6.92,8.47455585009968E-16));
#70513=CARTESIAN_POINT('',(0.6,-6.92,8.47455585009968E-16));
#70514=CARTESIAN_POINT('',(0.6,-7.22,-0.249999999999999));
#70515=CARTESIAN_POINT('Origin',(0.6,-7.07,8.65825286997179E-16));
#70516=CARTESIAN_POINT('',(0.600000000000001,-7.17,-8.78071754988652E-16));
#70517=CARTESIAN_POINT('Origin',(0.600000000000001,0.,0.));
#70518=CARTESIAN_POINT('',(0.600000000000001,-7.16704385318485,0.20586987765404));
#70519=CARTESIAN_POINT('',(0.6,-6.92,8.47455585009968E-16));
#70520=CARTESIAN_POINT('Origin',(0.600000000000001,0.,0.));
#70521=CARTESIAN_POINT('Origin',(0.6,-6.92,8.47455585009968E-16));
#70522=CARTESIAN_POINT('',(17.4,-7.16704385318485,0.20586987765404));
#70523=CARTESIAN_POINT('',(9.,-7.16704385318485,0.20586987765404));
#70524=CARTESIAN_POINT('',(17.4,-6.92,8.47455585009968E-16));
#70525=CARTESIAN_POINT('Origin',(17.4,-7.07,8.65825286997179E-16));
#70526=CARTESIAN_POINT('',(17.4,-7.17,-8.78071754988652E-16));
#70527=CARTESIAN_POINT('Origin',(17.4,0.,0.));
#70528=CARTESIAN_POINT('Origin',(17.4,0.,0.));
#70529=CARTESIAN_POINT('Origin',(0.6,-7.15372402116487,1.00753790450219));
#70530=CARTESIAN_POINT('',(17.4,-7.09390928188606,1.04180185273915));
#70531=CARTESIAN_POINT('',(0.599999999999999,-7.09390928188606,1.04180185273915));
#70532=CARTESIAN_POINT('',(9.,-7.09390928188606,1.04180185273915));
#70533=CARTESIAN_POINT('',(17.4,-6.81486965084448,1.20164538945516));
#70534=CARTESIAN_POINT('',(17.4,-7.15372402116487,1.00753790450219));
#70535=CARTESIAN_POINT('',(0.6,-6.81486965084448,1.20164538945516));
#70536=CARTESIAN_POINT('',(0.6,-6.81486965084448,1.20164538945516));
#70537=CARTESIAN_POINT('',(0.6,-7.15372402116487,1.00753790450219));
#70538=CARTESIAN_POINT('Origin',(0.6,-6.96259081379631,1.2276926161052));
#70539=CARTESIAN_POINT('',(0.600000000000001,-7.02241142370379,1.4472863559899));
#70540=CARTESIAN_POINT('Origin',(0.600000000000001,0.,0.));
#70541=CARTESIAN_POINT('',(0.6,-6.81486965084448,1.20164538945516));
#70542=CARTESIAN_POINT('Origin',(0.6,-6.81486965084448,1.20164538945516));
#70543=CARTESIAN_POINT('',(17.4,-7.02241142370379,1.4472863559899));
#70544=CARTESIAN_POINT('',(9.,-7.02241142370379,1.4472863559899));
#70545=CARTESIAN_POINT('',(17.4,-6.81486965084448,1.20164538945516));
#70546=CARTESIAN_POINT('Origin',(17.4,-6.96259081379631,1.2276926161052));
#70547=CARTESIAN_POINT('Origin',(17.4,0.,0.));
#70548=CARTESIAN_POINT('Origin',(0.6,-6.87008575790568,2.23446227961485));
#70549=CARTESIAN_POINT('',(17.4,-6.80522986674848,2.25781896101404));
#70550=CARTESIAN_POINT('',(0.599999999999999,-6.80522986674848,2.25781896101404));
#70551=CARTESIAN_POINT('',(9.,-6.80522986674848,2.25781896101404));
#70552=CARTESIAN_POINT('',(17.4,-6.50267293583849,2.36677939181363));
#70553=CARTESIAN_POINT('',(17.4,-6.87008575790568,2.23446227961485));
#70554=CARTESIAN_POINT('',(0.6,-6.50267293583849,2.36677939181363));
#70555=CARTESIAN_POINT('',(0.6,-6.50267293583849,2.36677939181363));
#70556=CARTESIAN_POINT('',(0.6,-6.87008575790568,2.23446227961485));
#70557=CARTESIAN_POINT('Origin',(0.6,-6.64362682895637,2.41808241331248));
#70558=CARTESIAN_POINT('',(0.600000000000001,-6.66440657662513,2.64472777076123));
#70559=CARTESIAN_POINT('Origin',(0.600000000000001,0.,0.));
#70560=CARTESIAN_POINT('',(0.6,-6.50267293583849,2.36677939181363));
#70561=CARTESIAN_POINT('Origin',(0.6,-6.50267293583849,2.36677939181363));
#70562=CARTESIAN_POINT('',(17.4,-6.66440657662513,2.64472777076123));
#70563=CARTESIAN_POINT('',(9.,-6.66440657662513,2.64472777076123));
#70564=CARTESIAN_POINT('',(17.4,-6.50267293583849,2.36677939181363));
#70565=CARTESIAN_POINT('Origin',(17.4,-6.64362682895637,2.41808241331248));
#70566=CARTESIAN_POINT('Origin',(17.4,0.,0.));
#70567=CARTESIAN_POINT('Origin',(0.6,-6.37770341532365,3.39349364905389));
#70568=CARTESIAN_POINT('',(17.4,-6.30977698572221,3.40523338267003));
#70569=CARTESIAN_POINT('',(0.600000000000001,-6.30977698572221,3.40523338267003));
#70570=CARTESIAN_POINT('',(9.,-6.30977698572221,3.40523338267003));
#70571=CARTESIAN_POINT('',(17.4,-5.99289579418832,3.46));
#70572=CARTESIAN_POINT('',(17.4,-6.37770341532365,3.39349364905389));
#70573=CARTESIAN_POINT('',(0.6,-5.99289579418832,3.46));
#70574=CARTESIAN_POINT('',(0.6,-5.99289579418832,3.46));
#70575=CARTESIAN_POINT('',(0.6,-6.37770341532365,3.39349364905389));
#70576=CARTESIAN_POINT('Origin',(0.6,-6.12279960475598,3.535));
#70577=CARTESIAN_POINT('',(0.600000000000001,-6.10390710806817,3.76181047051481));
#70578=CARTESIAN_POINT('Origin',(0.600000000000001,0.,0.));
#70579=CARTESIAN_POINT('',(0.6,-5.99289579418832,3.46));
#70580=CARTESIAN_POINT('Origin',(0.6,-5.99289579418832,3.46));
#70581=CARTESIAN_POINT('',(17.4,-6.10390710806817,3.76181047051481));
#70582=CARTESIAN_POINT('',(9.,-6.10390710806817,3.76181047051481));
#70583=CARTESIAN_POINT('',(17.4,-5.99289579418832,3.46));
#70584=CARTESIAN_POINT('Origin',(17.4,-6.12279960475598,3.535));
#70585=CARTESIAN_POINT('Origin',(17.4,0.,0.));
#70586=CARTESIAN_POINT('Origin',(0.6,-5.69153778174066,4.44941543115707));
#70587=CARTESIAN_POINT('',(17.4,-5.62260472388598,4.44918151112483));
#70588=CARTESIAN_POINT('',(0.599999999999999,-5.62260472388598,4.44918151112483));
#70589=CARTESIAN_POINT('',(9.,-5.62260472388598,4.44918151112483));
#70590=CARTESIAN_POINT('',(17.4,-5.30102754638333,4.44809025903085));
#70591=CARTESIAN_POINT('',(17.4,-5.69153778174066,4.44941543115707));
#70592=CARTESIAN_POINT('',(0.6,-5.30102754638333,4.44809025903085));
#70593=CARTESIAN_POINT('',(0.6,-5.30102754638333,4.44809025903085));
#70594=CARTESIAN_POINT('',(0.6,-5.69153778174066,4.44941543115707));
#70595=CARTESIAN_POINT('Origin',(0.6,-5.41593421285117,4.54450840048383));
#70596=CARTESIAN_POINT('',(0.599999999999999,-5.35794351075858,4.76459246268976));
#70597=CARTESIAN_POINT('Origin',(0.600000000000001,0.,0.));
#70598=CARTESIAN_POINT('',(0.6,-5.30102754638333,4.44809025903085));
#70599=CARTESIAN_POINT('Origin',(0.6,-5.30102754638333,4.44809025903085));
#70600=CARTESIAN_POINT('',(17.4,-5.35794351075858,4.76459246268976));
#70601=CARTESIAN_POINT('',(9.,-5.35794351075858,4.76459246268976));
#70602=CARTESIAN_POINT('',(17.4,-5.30102754638333,4.44809025903085));
#70603=CARTESIAN_POINT('Origin',(17.4,-5.41593421285117,4.54450840048383));
#70604=CARTESIAN_POINT('Origin',(17.4,0.,0.));
#70605=CARTESIAN_POINT('Origin',(0.6,-4.83243765271656,5.37014397689739));
#70606=CARTESIAN_POINT('',(17.4,-4.76459246268975,5.35794351075858));
#70607=CARTESIAN_POINT('',(0.599999999999999,-4.76459246268975,5.35794351075858));
#70608=CARTESIAN_POINT('',(9.,-4.76459246268975,5.35794351075858));
#70609=CARTESIAN_POINT('',(17.4,-4.44809025903085,5.30102754638333));
#70610=CARTESIAN_POINT('',(17.4,-4.83243765271656,5.37014397689739));
#70611=CARTESIAN_POINT('',(0.6,-4.44809025903085,5.30102754638333));
#70612=CARTESIAN_POINT('',(0.6,-4.44809025903085,5.30102754638333));
#70613=CARTESIAN_POINT('',(0.6,-4.83243765271656,5.37014397689739));
#70614=CARTESIAN_POINT('Origin',(0.6,-4.54450840048383,5.41593421285117));
#70615=CARTESIAN_POINT('',(0.599999999999999,-4.44918151112483,5.62260472388598));
#70616=CARTESIAN_POINT('Origin',(0.600000000000001,0.,0.));
#70617=CARTESIAN_POINT('',(0.6,-4.44809025903085,5.30102754638333));
#70618=CARTESIAN_POINT('Origin',(0.6,-4.44809025903085,5.30102754638333));
#70619=CARTESIAN_POINT('',(17.4,-4.44918151112483,5.62260472388598));
#70620=CARTESIAN_POINT('',(9.,-4.44918151112483,5.62260472388598));
#70621=CARTESIAN_POINT('',(17.4,-4.44809025903085,5.30102754638333));
#70622=CARTESIAN_POINT('Origin',(17.4,-4.54450840048383,5.41593421285117));
#70623=CARTESIAN_POINT('Origin',(17.4,0.,0.));
#70624=CARTESIAN_POINT('Origin',(0.6,-3.82650635094611,6.12770341532365));
#70625=CARTESIAN_POINT('',(17.4,-3.76181047051481,6.10390710806817));
#70626=CARTESIAN_POINT('',(0.600000000000001,-3.76181047051481,6.10390710806817));
#70627=CARTESIAN_POINT('',(9.,-3.76181047051481,6.10390710806817));
#70628=CARTESIAN_POINT('',(17.4,-3.46,5.99289579418832));
#70629=CARTESIAN_POINT('',(17.4,-3.82650635094611,6.12770341532365));
#70630=CARTESIAN_POINT('',(0.6,-3.46,5.99289579418832));
#70631=CARTESIAN_POINT('',(0.6,-3.46,5.99289579418832));
#70632=CARTESIAN_POINT('',(0.6,-3.82650635094611,6.12770341532365));
#70633=CARTESIAN_POINT('Origin',(0.6,-3.535,6.12279960475598));
#70634=CARTESIAN_POINT('',(0.599999999999999,-3.40523338267003,6.30977698572221));
#70635=CARTESIAN_POINT('Origin',(0.600000000000001,0.,0.));
#70636=CARTESIAN_POINT('',(0.6,-3.46,5.99289579418832));
#70637=CARTESIAN_POINT('Origin',(0.6,-3.46,5.99289579418832));
#70638=CARTESIAN_POINT('',(17.4,-3.40523338267003,6.30977698572221));
#70639=CARTESIAN_POINT('',(9.,-3.40523338267003,6.30977698572221));
#70640=CARTESIAN_POINT('',(17.4,-3.46,5.99289579418832));
#70641=CARTESIAN_POINT('Origin',(17.4,-3.535,6.12279960475598));
#70642=CARTESIAN_POINT('Origin',(17.4,0.,0.));
#70643=CARTESIAN_POINT('Origin',(0.6,-2.7043085900078,6.69907568624284));
#70644=CARTESIAN_POINT('',(17.4,-2.64472777076123,6.66440657662513));
#70645=CARTESIAN_POINT('',(0.599999999999999,-2.64472777076123,6.66440657662513));
#70646=CARTESIAN_POINT('',(9.,-2.64472777076123,6.66440657662513));
#70647=CARTESIAN_POINT('',(17.4,-2.36677939181363,6.50267293583849));
#70648=CARTESIAN_POINT('',(17.4,-2.7043085900078,6.69907568624284));
#70649=CARTESIAN_POINT('',(0.6,-2.36677939181363,6.50267293583849));
#70650=CARTESIAN_POINT('',(0.6,-2.36677939181363,6.50267293583849));
#70651=CARTESIAN_POINT('',(0.6,-2.7043085900078,6.69907568624284));
#70652=CARTESIAN_POINT('Origin',(0.6,-2.41808241331248,6.64362682895637));
#70653=CARTESIAN_POINT('',(0.599999999999999,-2.25781896101403,6.80522986674848));
#70654=CARTESIAN_POINT('Origin',(0.600000000000001,0.,0.));
#70655=CARTESIAN_POINT('',(0.6,-2.36677939181363,6.50267293583849));
#70656=CARTESIAN_POINT('Origin',(0.6,-2.36677939181363,6.50267293583849));
#70657=CARTESIAN_POINT('',(17.4,-2.25781896101403,6.80522986674848));
#70658=CARTESIAN_POINT('',(9.,-2.25781896101403,6.80522986674848));
#70659=CARTESIAN_POINT('',(17.4,-2.36677939181363,6.50267293583849));
#70660=CARTESIAN_POINT('Origin',(17.4,-2.41808241331248,6.64362682895637));
#70661=CARTESIAN_POINT('Origin',(17.4,0.,0.));
#70662=CARTESIAN_POINT('Origin',(0.6,-1.49994178100829,7.06689993233141));
#70663=CARTESIAN_POINT('',(17.4,-1.4472863559899,7.02241142370379));
#70664=CARTESIAN_POINT('',(0.600000000000001,-1.4472863559899,7.02241142370379));
#70665=CARTESIAN_POINT('',(9.,-1.4472863559899,7.02241142370379));
#70666=CARTESIAN_POINT('',(17.4,-1.20164538945516,6.81486965084448));
#70667=CARTESIAN_POINT('',(17.4,-1.49994178100829,7.06689993233141));
#70668=CARTESIAN_POINT('',(0.6,-1.20164538945516,6.81486965084448));
#70669=CARTESIAN_POINT('',(0.6,-1.20164538945516,6.81486965084448));
#70670=CARTESIAN_POINT('',(0.6,-1.49994178100829,7.06689993233141));
#70671=CARTESIAN_POINT('Origin',(0.6,-1.2276926161052,6.96259081379631));
#70672=CARTESIAN_POINT('',(0.600000000000001,-1.04180185273915,7.09390928188606));
#70673=CARTESIAN_POINT('Origin',(0.600000000000001,0.,0.));
#70674=CARTESIAN_POINT('',(0.6,-1.20164538945516,6.81486965084448));
#70675=CARTESIAN_POINT('Origin',(0.6,-1.20164538945516,6.81486965084448));
#70676=CARTESIAN_POINT('',(17.4,-1.04180185273915,7.09390928188606));
#70677=CARTESIAN_POINT('',(9.,-1.04180185273915,7.09390928188606));
#70678=CARTESIAN_POINT('',(17.4,-1.20164538945516,6.81486965084448));
#70679=CARTESIAN_POINT('Origin',(17.4,-1.2276926161052,6.96259081379631));
#70680=CARTESIAN_POINT('Origin',(17.4,0.,0.));
#70681=CARTESIAN_POINT('Origin',(0.6,-0.25,7.22));
#70682=CARTESIAN_POINT('',(17.4,-0.20586987765404,7.16704385318485));
#70683=CARTESIAN_POINT('',(0.600000000000001,-0.20586987765404,7.16704385318485));
#70684=CARTESIAN_POINT('',(9.,-0.20586987765404,7.16704385318485));
#70685=CARTESIAN_POINT('',(17.4,4.23727792504984E-16,6.92));
#70686=CARTESIAN_POINT('',(17.4,-0.25,7.22));
#70687=CARTESIAN_POINT('',(0.6,4.23727792504984E-16,6.92));
#70688=CARTESIAN_POINT('',(0.6,4.23727792504984E-16,6.92));
#70689=CARTESIAN_POINT('',(0.6,-0.25,7.22));
#70690=CARTESIAN_POINT('Origin',(0.6,4.32912643498589E-16,7.07));
#70691=CARTESIAN_POINT('',(0.600000000000001,0.20586987765404,7.16704385318485));
#70692=CARTESIAN_POINT('Origin',(0.600000000000001,0.,0.));
#70693=CARTESIAN_POINT('',(0.6,4.23727792504984E-16,6.92));
#70694=CARTESIAN_POINT('Origin',(0.6,4.23727792504984E-16,6.92));
#70695=CARTESIAN_POINT('',(17.4,0.20586987765404,7.16704385318485));
#70696=CARTESIAN_POINT('',(9.,0.205869877654041,7.16704385318485));
#70697=CARTESIAN_POINT('',(17.4,4.23727792504984E-16,6.92));
#70698=CARTESIAN_POINT('Origin',(17.4,4.32912643498589E-16,7.07));
#70699=CARTESIAN_POINT('Origin',(17.4,0.,0.));
#70700=CARTESIAN_POINT('Origin',(0.6,1.00753790450219,7.15372402116488));
#70701=CARTESIAN_POINT('',(17.4,1.04180185273915,7.09390928188606));
#70702=CARTESIAN_POINT('',(0.600000000000001,1.04180185273915,7.09390928188606));
#70703=CARTESIAN_POINT('',(9.,1.04180185273915,7.09390928188606));
#70704=CARTESIAN_POINT('',(17.4,1.20164538945516,6.81486965084448));
#70705=CARTESIAN_POINT('',(17.4,1.00753790450219,7.15372402116488));
#70706=CARTESIAN_POINT('',(0.6,1.20164538945516,6.81486965084448));
#70707=CARTESIAN_POINT('',(0.6,1.20164538945516,6.81486965084448));
#70708=CARTESIAN_POINT('',(0.6,1.00753790450219,7.15372402116488));
#70709=CARTESIAN_POINT('Origin',(0.6,1.2276926161052,6.96259081379631));
#70710=CARTESIAN_POINT('',(0.600000000000001,1.4472863559899,7.02241142370379));
#70711=CARTESIAN_POINT('Origin',(0.600000000000001,0.,0.));
#70712=CARTESIAN_POINT('',(0.6,1.20164538945516,6.81486965084448));
#70713=CARTESIAN_POINT('Origin',(0.6,1.20164538945516,6.81486965084448));
#70714=CARTESIAN_POINT('',(17.4,1.4472863559899,7.02241142370379));
#70715=CARTESIAN_POINT('',(9.,1.4472863559899,7.02241142370379));
#70716=CARTESIAN_POINT('',(17.4,1.20164538945516,6.81486965084448));
#70717=CARTESIAN_POINT('Origin',(17.4,1.2276926161052,6.96259081379631));
#70718=CARTESIAN_POINT('Origin',(17.4,0.,0.));
#70719=CARTESIAN_POINT('Origin',(0.6,2.23446227961485,6.87008575790568));
#70720=CARTESIAN_POINT('',(17.4,2.25781896101404,6.80522986674848));
#70721=CARTESIAN_POINT('',(0.600000000000001,2.25781896101404,6.80522986674848));
#70722=CARTESIAN_POINT('',(9.,2.25781896101404,6.80522986674848));
#70723=CARTESIAN_POINT('',(17.4,2.36677939181363,6.50267293583849));
#70724=CARTESIAN_POINT('',(17.4,2.23446227961485,6.87008575790568));
#70725=CARTESIAN_POINT('',(0.6,2.36677939181363,6.50267293583849));
#70726=CARTESIAN_POINT('',(0.6,2.36677939181363,6.50267293583849));
#70727=CARTESIAN_POINT('',(0.6,2.23446227961485,6.87008575790568));
#70728=CARTESIAN_POINT('Origin',(0.6,2.41808241331248,6.64362682895637));
#70729=CARTESIAN_POINT('',(0.600000000000001,2.64472777076123,6.66440657662513));
#70730=CARTESIAN_POINT('Origin',(0.600000000000001,0.,0.));
#70731=CARTESIAN_POINT('',(0.6,2.36677939181363,6.50267293583849));
#70732=CARTESIAN_POINT('Origin',(0.6,2.36677939181363,6.50267293583849));
#70733=CARTESIAN_POINT('',(17.4,2.64472777076123,6.66440657662513));
#70734=CARTESIAN_POINT('',(9.,2.64472777076123,6.66440657662513));
#70735=CARTESIAN_POINT('',(17.4,2.36677939181363,6.50267293583849));
#70736=CARTESIAN_POINT('Origin',(17.4,2.41808241331248,6.64362682895637));
#70737=CARTESIAN_POINT('Origin',(17.4,0.,0.));
#70738=CARTESIAN_POINT('Origin',(0.6,3.39349364905389,6.37770341532365));
#70739=CARTESIAN_POINT('',(17.4,3.40523338267003,6.30977698572221));
#70740=CARTESIAN_POINT('',(0.599999999999999,3.40523338267003,6.30977698572221));
#70741=CARTESIAN_POINT('',(9.,3.40523338267003,6.30977698572221));
#70742=CARTESIAN_POINT('',(17.4,3.46,5.99289579418831));
#70743=CARTESIAN_POINT('',(17.4,3.39349364905389,6.37770341532365));
#70744=CARTESIAN_POINT('',(0.6,3.46,5.99289579418831));
#70745=CARTESIAN_POINT('',(0.6,3.46,5.99289579418831));
#70746=CARTESIAN_POINT('',(0.6,3.39349364905389,6.37770341532365));
#70747=CARTESIAN_POINT('Origin',(0.6,3.535,6.12279960475598));
#70748=CARTESIAN_POINT('',(0.599999999999999,3.76181047051482,6.10390710806817));
#70749=CARTESIAN_POINT('Origin',(0.600000000000001,0.,0.));
#70750=CARTESIAN_POINT('',(0.6,3.46,5.99289579418831));
#70751=CARTESIAN_POINT('Origin',(0.6,3.46,5.99289579418831));
#70752=CARTESIAN_POINT('',(17.4,3.76181047051482,6.10390710806817));
#70753=CARTESIAN_POINT('',(9.,3.76181047051482,6.10390710806817));
#70754=CARTESIAN_POINT('',(17.4,3.46,5.99289579418831));
#70755=CARTESIAN_POINT('Origin',(17.4,3.535,6.12279960475598));
#70756=CARTESIAN_POINT('Origin',(17.4,0.,0.));
#70757=CARTESIAN_POINT('Origin',(0.6,4.44941543115707,5.69153778174066));
#70758=CARTESIAN_POINT('',(17.4,4.44918151112483,5.62260472388598));
#70759=CARTESIAN_POINT('',(0.599999999999999,4.44918151112483,5.62260472388598));
#70760=CARTESIAN_POINT('',(9.,4.44918151112483,5.62260472388598));
#70761=CARTESIAN_POINT('',(17.4,4.44809025903085,5.30102754638333));
#70762=CARTESIAN_POINT('',(17.4,4.44941543115707,5.69153778174066));
#70763=CARTESIAN_POINT('',(0.6,4.44809025903085,5.30102754638333));
#70764=CARTESIAN_POINT('',(0.6,4.44809025903085,5.30102754638333));
#70765=CARTESIAN_POINT('',(0.6,4.44941543115707,5.69153778174066));
#70766=CARTESIAN_POINT('Origin',(0.6,4.54450840048383,5.41593421285117));
#70767=CARTESIAN_POINT('',(0.599999999999999,4.76459246268975,5.35794351075858));
#70768=CARTESIAN_POINT('Origin',(0.600000000000001,0.,0.));
#70769=CARTESIAN_POINT('',(0.6,4.44809025903085,5.30102754638333));
#70770=CARTESIAN_POINT('Origin',(0.6,4.44809025903085,5.30102754638333));
#70771=CARTESIAN_POINT('',(17.4,4.76459246268975,5.35794351075858));
#70772=CARTESIAN_POINT('',(9.,4.76459246268975,5.35794351075858));
#70773=CARTESIAN_POINT('',(17.4,4.44809025903085,5.30102754638333));
#70774=CARTESIAN_POINT('Origin',(17.4,4.54450840048383,5.41593421285117));
#70775=CARTESIAN_POINT('Origin',(17.4,0.,0.));
#70776=CARTESIAN_POINT('Origin',(0.6,5.37014397689739,4.83243765271656));
#70777=CARTESIAN_POINT('',(17.4,5.35794351075858,4.76459246268975));
#70778=CARTESIAN_POINT('',(0.599999999999999,5.35794351075858,4.76459246268975));
#70779=CARTESIAN_POINT('',(9.,5.35794351075858,4.76459246268975));
#70780=CARTESIAN_POINT('',(17.4,5.30102754638333,4.44809025903085));
#70781=CARTESIAN_POINT('',(17.4,5.37014397689739,4.83243765271656));
#70782=CARTESIAN_POINT('',(0.6,5.30102754638333,4.44809025903085));
#70783=CARTESIAN_POINT('',(0.6,5.30102754638333,4.44809025903085));
#70784=CARTESIAN_POINT('',(0.6,5.37014397689739,4.83243765271656));
#70785=CARTESIAN_POINT('Origin',(0.6,5.41593421285118,4.54450840048383));
#70786=CARTESIAN_POINT('',(0.599999999999999,5.62260472388598,4.44918151112483));
#70787=CARTESIAN_POINT('Origin',(0.600000000000001,0.,0.));
#70788=CARTESIAN_POINT('',(0.6,5.30102754638333,4.44809025903085));
#70789=CARTESIAN_POINT('Origin',(0.6,5.30102754638333,4.44809025903085));
#70790=CARTESIAN_POINT('',(17.4,5.62260472388598,4.44918151112483));
#70791=CARTESIAN_POINT('',(9.,5.62260472388598,4.44918151112483));
#70792=CARTESIAN_POINT('',(17.4,5.30102754638333,4.44809025903085));
#70793=CARTESIAN_POINT('Origin',(17.4,5.41593421285118,4.54450840048383));
#70794=CARTESIAN_POINT('Origin',(17.4,0.,0.));
#70795=CARTESIAN_POINT('Origin',(0.6,6.12770341532365,3.82650635094611));
#70796=CARTESIAN_POINT('',(17.4,6.10390710806817,3.76181047051481));
#70797=CARTESIAN_POINT('',(0.600000000000001,6.10390710806817,3.76181047051481));
#70798=CARTESIAN_POINT('',(9.,6.10390710806817,3.76181047051481));
#70799=CARTESIAN_POINT('',(17.4,5.99289579418832,3.46));
#70800=CARTESIAN_POINT('',(17.4,6.12770341532365,3.82650635094611));
#70801=CARTESIAN_POINT('',(0.6,5.99289579418832,3.46));
#70802=CARTESIAN_POINT('',(0.6,5.99289579418832,3.46));
#70803=CARTESIAN_POINT('',(0.6,6.12770341532365,3.82650635094611));
#70804=CARTESIAN_POINT('Origin',(0.6,6.12279960475598,3.535));
#70805=CARTESIAN_POINT('',(0.600000000000001,6.30977698572221,3.40523338267003));
#70806=CARTESIAN_POINT('Origin',(0.600000000000001,0.,0.));
#70807=CARTESIAN_POINT('',(0.6,5.99289579418832,3.46));
#70808=CARTESIAN_POINT('Origin',(0.6,5.99289579418832,3.46));
#70809=CARTESIAN_POINT('',(17.4,6.30977698572221,3.40523338267003));
#70810=CARTESIAN_POINT('',(9.,6.30977698572221,3.40523338267003));
#70811=CARTESIAN_POINT('',(17.4,5.99289579418832,3.46));
#70812=CARTESIAN_POINT('Origin',(17.4,6.12279960475598,3.535));
#70813=CARTESIAN_POINT('Origin',(17.4,0.,0.));
#70814=CARTESIAN_POINT('Origin',(0.6,6.69907568624284,2.7043085900078));
#70815=CARTESIAN_POINT('',(17.4,6.66440657662513,2.64472777076123));
#70816=CARTESIAN_POINT('',(0.599999999999999,6.66440657662513,2.64472777076123));
#70817=CARTESIAN_POINT('',(9.,6.66440657662513,2.64472777076123));
#70818=CARTESIAN_POINT('',(17.4,6.50267293583849,2.36677939181363));
#70819=CARTESIAN_POINT('',(17.4,6.69907568624284,2.7043085900078));
#70820=CARTESIAN_POINT('',(0.6,6.50267293583849,2.36677939181363));
#70821=CARTESIAN_POINT('',(0.6,6.50267293583849,2.36677939181363));
#70822=CARTESIAN_POINT('',(0.6,6.69907568624284,2.7043085900078));
#70823=CARTESIAN_POINT('Origin',(0.6,6.64362682895637,2.41808241331248));
#70824=CARTESIAN_POINT('',(0.599999999999999,6.80522986674848,2.25781896101403));
#70825=CARTESIAN_POINT('Origin',(0.600000000000001,0.,0.));
#70826=CARTESIAN_POINT('',(0.6,6.50267293583849,2.36677939181363));
#70827=CARTESIAN_POINT('Origin',(0.6,6.50267293583849,2.36677939181363));
#70828=CARTESIAN_POINT('',(17.4,6.80522986674848,2.25781896101403));
#70829=CARTESIAN_POINT('',(9.,6.80522986674848,2.25781896101403));
#70830=CARTESIAN_POINT('',(17.4,6.50267293583849,2.36677939181363));
#70831=CARTESIAN_POINT('Origin',(17.4,6.64362682895637,2.41808241331248));
#70832=CARTESIAN_POINT('Origin',(17.4,0.,0.));
#70833=CARTESIAN_POINT('Origin',(0.6,7.06689993233141,1.49994178100829));
#70834=CARTESIAN_POINT('',(17.4,7.02241142370379,1.4472863559899));
#70835=CARTESIAN_POINT('',(0.600000000000001,7.02241142370379,1.4472863559899));
#70836=CARTESIAN_POINT('',(9.,7.02241142370379,1.4472863559899));
#70837=CARTESIAN_POINT('',(17.4,6.81486965084448,1.20164538945516));
#70838=CARTESIAN_POINT('',(17.4,7.06689993233141,1.49994178100829));
#70839=CARTESIAN_POINT('',(0.6,6.81486965084448,1.20164538945516));
#70840=CARTESIAN_POINT('',(0.6,6.81486965084448,1.20164538945516));
#70841=CARTESIAN_POINT('',(0.6,7.06689993233141,1.49994178100829));
#70842=CARTESIAN_POINT('Origin',(0.6,6.96259081379631,1.2276926161052));
#70843=CARTESIAN_POINT('',(0.600000000000001,7.09390928188606,1.04180185273915));
#70844=CARTESIAN_POINT('Origin',(0.600000000000001,0.,0.));
#70845=CARTESIAN_POINT('',(0.6,6.81486965084448,1.20164538945516));
#70846=CARTESIAN_POINT('Origin',(0.6,6.81486965084448,1.20164538945516));
#70847=CARTESIAN_POINT('',(17.4,7.09390928188606,1.04180185273915));
#70848=CARTESIAN_POINT('',(9.,7.09390928188606,1.04180185273915));
#70849=CARTESIAN_POINT('',(17.4,6.81486965084448,1.20164538945516));
#70850=CARTESIAN_POINT('Origin',(17.4,6.96259081379631,1.2276926161052));
#70851=CARTESIAN_POINT('Origin',(17.4,0.,0.));
#70852=CARTESIAN_POINT('Origin',(0.6,7.22,0.25));
#70853=CARTESIAN_POINT('',(17.4,7.16704385318485,0.20586987765404));
#70854=CARTESIAN_POINT('',(0.600000000000001,7.16704385318485,0.20586987765404));
#70855=CARTESIAN_POINT('',(9.,7.16704385318485,0.20586987765404));
#70856=CARTESIAN_POINT('',(17.4,6.92,0.));
#70857=CARTESIAN_POINT('',(17.4,7.22,0.25));
#70858=CARTESIAN_POINT('',(0.6,6.92,0.));
#70859=CARTESIAN_POINT('',(0.6,6.92,0.));
#70860=CARTESIAN_POINT('',(0.6,7.22,0.25));
#70861=CARTESIAN_POINT('Origin',(0.6,7.07,0.));
#70862=CARTESIAN_POINT('',(0.600000000000001,7.16704385318485,-0.20586987765404));
#70863=CARTESIAN_POINT('Origin',(0.600000000000001,0.,0.));
#70864=CARTESIAN_POINT('',(0.6,6.92,0.));
#70865=CARTESIAN_POINT('Origin',(0.6,6.92,0.));
#70866=CARTESIAN_POINT('',(17.4,7.16704385318485,-0.20586987765404));
#70867=CARTESIAN_POINT('',(9.,7.16704385318485,-0.205869877654039));
#70868=CARTESIAN_POINT('',(17.4,6.92,0.));
#70869=CARTESIAN_POINT('Origin',(17.4,7.07,0.));
#70870=CARTESIAN_POINT('Origin',(17.4,0.,0.));
#70871=CARTESIAN_POINT('Origin',(9.,0.,0.));
#70872=CARTESIAN_POINT('',(18.,-7.17,-8.78071754988652E-16));
#70873=CARTESIAN_POINT('Origin',(18.,0.,0.));
#70874=CARTESIAN_POINT('',(9.,-7.17,-8.78071754988652E-16));
#70875=CARTESIAN_POINT('',(9.,-7.17,-8.78071754988652E-16));
#70876=CARTESIAN_POINT('Origin',(18.4,0.,0.));
#70877=CARTESIAN_POINT('',(18.4,-6.76,-8.27861236223611E-16));
#71611=UNCERTAINTY_MEASURE_WITH_UNIT(LENGTH_MEASURE(0.01),#71629,
'DISTANCE_ACCURACY_VALUE',
'Maximum model space distance between geometric entities at asserted c
onnectivities');
#71613=UNCERTAINTY_MEASURE_WITH_UNIT(LENGTH_MEASURE(0.01),#71629,
'DISTANCE_ACCURACY_VALUE',
'Maximum model space distance between geometric entities at asserted c
onnectivities');
#71626=(
GEOMETRIC_REPRESENTATION_CONTEXT(3)
GLOBAL_UNCERTAINTY_ASSIGNED_CONTEXT((#71611))
GLOBAL_UNIT_ASSIGNED_CONTEXT((#71629,#71631,#71632))
REPRESENTATION_CONTEXT('','3D')
);
#71628=(
GEOMETRIC_REPRESENTATION_CONTEXT(3)
GLOBAL_UNCERTAINTY_ASSIGNED_CONTEXT((#71613))
GLOBAL_UNIT_ASSIGNED_CONTEXT((#71629,#71631,#71632))
REPRESENTATION_CONTEXT('','3D')
);
#71629=(
LENGTH_UNIT()
NAMED_UNIT(*)
SI_UNIT(.MILLI.,.METRE.)
);
#71631=(
NAMED_UNIT(*)
PLANE_ANGLE_UNIT()
SI_UNIT($,.RADIAN.)
);
#71632=(
NAMED_UNIT(*)
SI_UNIT($,.STERADIAN.)
SOLID_ANGLE_UNIT()
);
#71645=SHAPE_DEFINITION_REPRESENTATION(#71659,#71694);
#71659=PRODUCT_DEFINITION_SHAPE('',$,#71709);
#71694=SHAPE_REPRESENTATION('',(#37269),#71626);
#71696=PRODUCT_DEFINITION_CONTEXT('part definition',#71740,'design');
#71709=PRODUCT_DEFINITION('2026-10-25-00-23-49-479',
'02_Wheel_Stud_1-2-20_UNF_Knurled',#71723,#71696);
#71723=PRODUCT_DEFINITION_FORMATION('',$,#71754);
#71740=APPLICATION_CONTEXT(
'Core Data for Automotive Mechanical Design Process');
#71741=PRODUCT_CONTEXT('part definition',#71740,'mechanical');
#71754=PRODUCT('2026-10-25-00-23-49-479',
'02_Wheel_Stud_1-2-20_UNF_Knurled',$,(#71741));
#71819=COLOUR_RGB('Black',0.12,0.14,0.17);
#71820=FILL_AREA_STYLE_COLOUR('',#71819);
#71821=FILL_AREA_STYLE('',(#71820));
#71822=SURFACE_STYLE_FILL_AREA(#71821);
#71823=SURFACE_SIDE_STYLE('',(#71822));
#71824=SURFACE_STYLE_USAGE(.BOTH.,#71823);
#71825=PRESENTATION_STYLE_ASSIGNMENT((#71824));
ENDSEC;
END-ISO-10303-21;
